ISO-10303-21;
HEADER;
/* Generated by software containing ST-Developer
 * from STEP Tools, Inc. (www.steptools.com) 
 */

FILE_DESCRIPTION(
/* description */ (''),
/* implementation_level */ '2;1');

FILE_NAME(
/* name */ 'Screw_02.step',
/* time_stamp */ '2026-10-06T13:05:37-07:00',
/* author */ (''),
/* organization */ (''),
/* preprocessor_version */ 'ST-DEVELOPER v20.2',
/* originating_system */ 'Autodesk Translation Framework v15.15.0.0',
/* authorisation */ '');

FILE_SCHEMA (('AUTOMOTIVE_DESIGN { 1 0 10303 214 3 1 1 }'));
ENDSEC;

DATA;
#10=MECHANICAL_DESIGN_GEOMETRIC_PRESENTATION_REPRESENTATION('',(#142),#28055);
#54=ELLIPSE('',#4033,3.36109563026061,2.90329889035631);
#55=ELLIPSE('',#4034,2.84121050972126,2.43735261139454);
#56=ELLIPSE('',#4052,3.33206993022602,2.82346550068506);
#57=ELLIPSE('',#4053,2.87565474083181,2.48077736727696);
#66=B_SPLINE_SURFACE_WITH_KNOTS('',3,3,((#24618,#24619,#24620,#24621),(#24622,
#24623,#24624,#24625),(#24626,#24627,#24628,#24629),(#24630,#24631,#24632,
#24633)),.UNSPECIFIED.,.F.,.F.,.F.,(4,4),(4,4),(0.066620174713851,0.0820126057383863),
(8.314732749858,8.70158673567856),.UNSPECIFIED.);
#67=B_SPLINE_SURFACE_WITH_KNOTS('',3,3,((#24640,#24641,#24642,#24643,#24644,
#24645),(#24646,#24647,#24648,#24649,#24650,#24651),(#24652,#24653,#24654,
#24655,#24656,#24657),(#24658,#24659,#24660,#24661,#24662,#24663)),
 .UNSPECIFIED.,.F.,.F.,.F.,(4,4),(4,1,1,4),(-0.000175214539722031,0.0820126057383863),
(47.6103505270742,48.3332993342991,49.0560729269844,49.7790217342094),
 .UNSPECIFIED.);
#68=B_SPLINE_SURFACE_WITH_KNOTS('',3,3,((#24719,#24720,#24721,#24722,#24723,
#24724),(#24725,#24726,#24727,#24728,#24729,#24730),(#24731,#24732,#24733,
#24734,#24735,#24736),(#24737,#24738,#24739,#24740,#24741,#24742)),
 .UNSPECIFIED.,.F.,.F.,.F.,(4,4),(4,1,1,4),(-0.000176040298938268,0.0820126057383863),
(41.3271643941354,42.0501140271196,42.7728876198048,43.495837252789),
 .UNSPECIFIED.);
#69=B_SPLINE_SURFACE_WITH_KNOTS('',3,3,((#24749,#24750,#24751,#24752,#24753,
#24754),(#24755,#24756,#24757,#24758,#24759,#24760),(#24761,#24762,#24763,
#24764,#24765,#24766),(#24767,#24768,#24769,#24770,#24771,#24772)),
 .UNSPECIFIED.,.F.,.F.,.F.,(4,4),(4,1,1,4),(-0.000176780710812022,0.0820126057383863),
(35.0439783465439,35.76692871994,36.4897023126252,37.2126526860213),
 .UNSPECIFIED.);
#70=B_SPLINE_SURFACE_WITH_KNOTS('',3,3,((#24779,#24780,#24781,#24782,#24783,
#24784),(#24785,#24786,#24787,#24788,#24789,#24790),(#24791,#24792,#24793,
#24794,#24795,#24796),(#24797,#24798,#24799,#24800,#24801,#24802)),
 .UNSPECIFIED.,.F.,.F.,.F.,(4,4),(4,1,1,4),(-0.000177449278394063,0.0820126057383863),
(28.7607923707967,29.4837434127604,30.2065170054456,30.9294680474093),
 .UNSPECIFIED.);
#71=B_SPLINE_SURFACE_WITH_KNOTS('',3,3,((#24809,#24810,#24811,#24812,#24813,
#24814),(#24815,#24816,#24817,#24818,#24819,#24820),(#24821,#24822,#24823,
#24824,#24825,#24826),(#24827,#24828,#24829,#24830,#24831,#24832)),
 .UNSPECIFIED.,.F.,.F.,.F.,(4,4),(4,1,1,4),(-0.000178056708344039,0.0820126057383863),
(22.4776064561872,23.2005581055808,23.9233316982661,24.6462833476596),
 .UNSPECIFIED.);
#72=B_SPLINE_SURFACE_WITH_KNOTS('',3,3,((#24839,#24840,#24841,#24842,#24843,
#24844),(#24845,#24846,#24847,#24848,#24849,#24850),(#24851,#24852,#24853,
#24854,#24855,#24856),(#24857,#24858,#24859,#24860,#24861,#24862)),
 .UNSPECIFIED.,.F.,.F.,.F.,(4,4),(4,1,1,4),(-0.000178611609329685,0.0820126057383863),
(16.1944205941067,16.9173727984012,17.6401463910865,18.363098595381),
 .UNSPECIFIED.);
#73=B_SPLINE_SURFACE_WITH_KNOTS('',3,3,((#24869,#24870,#24871,#24872,#24873,
#24874),(#24875,#24876,#24877,#24878,#24879,#24880),(#24881,#24882,#24883,
#24884,#24885,#24886),(#24887,#24888,#24889,#24890,#24891,#24892)),
 .UNSPECIFIED.,.F.,.F.,.F.,(4,4),(4,1,1,4),(-0.000156396744294902,0.0821188966323171),
(9.98287940740301,10.6818311637994,11.3807829201958,12.0798910733364),
 .UNSPECIFIED.);
#74=B_SPLINE_SURFACE_WITH_KNOTS('',3,3,((#24952,#24953,#24954,#24955,#24956,
#24957),(#24958,#24959,#24960,#24961,#24962,#24963),(#24964,#24965,#24966,
#24967,#24968,#24969),(#24970,#24971,#24972,#24973,#24974,#24975)),
 .UNSPECIFIED.,.F.,.F.,.F.,(4,4),(4,1,1,4),(-0.000175639065612779,0.0820126057383863),
(44.4687574489585,45.1917066807094,45.9144802733946,46.6374295051455),
 .UNSPECIFIED.);
#75=B_SPLINE_SURFACE_WITH_KNOTS('',3,3,((#24982,#24983,#24984,#24985,#24986,
#24987),(#24988,#24989,#24990,#24991,#24992,#24993),(#24994,#24995,#24996,
#24997,#24998,#24999),(#25000,#25001,#25002,#25003,#25004,#25005)),
 .UNSPECIFIED.,.F.,.F.,.F.,(4,4),(4,1,1,4),(-0.000176420253877423,0.0820126057383863),
(38.1855713605906,38.9085213735298,39.631294966215,40.3542449791542),
 .UNSPECIFIED.);
#76=B_SPLINE_SURFACE_WITH_KNOTS('',3,3,((#25012,#25013,#25014,#25015,#25016,
#25017),(#25018,#25019,#25020,#25021,#25022,#25023),(#25024,#25025,#25026,
#25027,#25028,#25029),(#25030,#25031,#25032,#25033,#25034,#25035)),
 .UNSPECIFIED.,.F.,.F.,.F.,(4,4),(4,1,1,4),(-0.000177123249794933,0.0820126057383863),
(31.9023853504151,32.6253360663502,33.3481096590354,34.0710603749705),
 .UNSPECIFIED.);
#77=B_SPLINE_SURFACE_WITH_KNOTS('',3,3,((#25042,#25043,#25044,#25045,#25046,
#25047),(#25048,#25049,#25050,#25051,#25052,#25053),(#25054,#25055,#25056,
#25057,#25058,#25059),(#25060,#25061,#25062,#25063,#25064,#25065)),
 .UNSPECIFIED.,.F.,.F.,.F.,(4,4),(4,1,1,4),(-0.000177760054985351,0.0820126057383863),
(25.6191994064303,26.3421507591706,27.0649243518558,27.7878757045961),
 .UNSPECIFIED.);
#78=B_SPLINE_SURFACE_WITH_KNOTS('',3,3,((#25072,#25073,#25074,#25075,#25076,
#25077),(#25078,#25079,#25080,#25081,#25082,#25083),(#25084,#25085,#25086,
#25087,#25088,#25089),(#25090,#25091,#25092,#25093,#25094,#25095)),
 .UNSPECIFIED.,.F.,.F.,.F.,(4,4),(4,1,1,4),(-0.000178340254205606,0.0820126057383863),
(19.3360135190516,20.058965451991,20.7817390446763,21.5046909776157),
 .UNSPECIFIED.);
#79=B_SPLINE_SURFACE_WITH_KNOTS('',3,3,((#25102,#25103,#25104,#25105,#25106,
#25107),(#25108,#25109,#25110,#25111,#25112,#25113),(#25114,#25115,#25116,
#25117,#25118,#25119),(#25120,#25121,#25122,#25123,#25124,#25125)),
 .UNSPECIFIED.,.F.,.F.,.F.,(4,4),(4,1,1,4),(-0.000178871603495943,0.0820126057383863),
(13.0528276805227,13.7757801448114,14.4985537374967,15.2215062017854),
 .UNSPECIFIED.);
#80=B_SPLINE_SURFACE_WITH_KNOTS('',3,3,((#25323,#25324,#25325,#25326,#25327,
#25328),(#25329,#25330,#25331,#25332,#25333,#25334),(#25335,#25336,#25337,
#25338,#25339,#25340),(#25341,#25342,#25343,#25344,#25345,#25346)),
 .UNSPECIFIED.,.F.,.F.,.F.,(4,4),(4,1,1,4),(0.,0.0821885306368104),(47.6103498167155,
48.3332993342991,49.0560729269844,49.7790224445681),.UNSPECIFIED.);
#81=B_SPLINE_SURFACE_WITH_KNOTS('',3,3,((#25347,#25348,#25349,#25350,#25351,
#25352),(#25353,#25354,#25355,#25356,#25357,#25358),(#25359,#25360,#25361,
#25362,#25363,#25364),(#25365,#25366,#25367,#25368,#25369,#25370)),
 .UNSPECIFIED.,.F.,.F.,.F.,(4,4),(4,1,1,4),(0.,0.0821892826429367),(41.3271637575297,
42.0501140271195,42.7728876198048,43.4958378893947),.UNSPECIFIED.);
#82=B_SPLINE_SURFACE_WITH_KNOTS('',3,3,((#25371,#25372,#25373,#25374,#25375,
#25376),(#25377,#25378,#25379,#25380,#25381,#25382),(#25383,#25384,#25385,
#25386,#25387,#25388),(#25389,#25390,#25391,#25392,#25393,#25394)),
 .UNSPECIFIED.,.F.,.F.,.F.,(4,4),(4,1,1,4),(0.,0.0821899610193562),(35.0439777719737,
35.76692871994,36.4897023126252,37.2126532605915),.UNSPECIFIED.);
#83=B_SPLINE_SURFACE_WITH_KNOTS('',3,3,((#25395,#25396,#25397,#25398,#25399,
#25400),(#25401,#25402,#25403,#25404,#25405,#25406),(#25407,#25408,#25409,
#25410,#25411,#25412),(#25413,#25414,#25415,#25416,#25417,#25418)),
 .UNSPECIFIED.,.F.,.F.,.F.,(4,4),(4,1,1,4),(0.,0.0821905768332721),(28.7607918489802,
29.4837434127604,30.2065170054456,30.9294685692258),.UNSPECIFIED.);
#84=B_SPLINE_SURFACE_WITH_KNOTS('',3,3,((#25419,#25420,#25421,#25422,#25423,
#25424),(#25425,#25426,#25427,#25428,#25429,#25430),(#25431,#25432,#25433,
#25434,#25435,#25436),(#25437,#25438,#25439,#25440,#25441,#25442)),
 .UNSPECIFIED.,.F.,.F.,.F.,(4,4),(4,1,1,4),(0.,0.0821911389659494),(22.4776059796679,
23.2005581055808,23.9233316982661,24.6462838241789),.UNSPECIFIED.);
#85=B_SPLINE_SURFACE_WITH_KNOTS('',3,3,((#25443,#25444,#25445,#25446,#25447,
#25448),(#25449,#25450,#25451,#25452,#25453,#25454),(#25455,#25456,#25457,
#25458,#25459,#25460),(#25461,#25462,#25463,#25464,#25465,#25466)),
 .UNSPECIFIED.,.F.,.F.,.F.,(4,4),(4,1,1,4),(0.,0.0821916546351816),(16.1944201568192,
16.9173727984012,17.6401463910865,18.3630990326685),.UNSPECIFIED.);
#86=B_SPLINE_SURFACE_WITH_KNOTS('',3,3,((#25467,#25468,#25469,#25470,#25471,
#25472),(#25473,#25474,#25475,#25476,#25477,#25478),(#25479,#25480,#25481,
#25482,#25483,#25484),(#25485,#25486,#25487,#25488,#25489,#25490)),
 .UNSPECIFIED.,.F.,.F.,.F.,(4,4),(4,1,1,4),(-9.65518509377315E-5,0.0821438972802576),
(50.7519871036618,51.4243296588263,52.0965409224489,52.7687521860715),
 .UNSPECIFIED.);
#87=B_SPLINE_SURFACE_WITH_KNOTS('',3,3,((#25491,#25492,#25493,#25494,#25495,
#25496),(#25497,#25498,#25499,#25500,#25501,#25502),(#25503,#25504,#25505,
#25506,#25507,#25508),(#25509,#25510,#25511,#25512,#25513,#25514)),
 .UNSPECIFIED.,.F.,.F.,.F.,(4,4),(4,1,1,4),(0.,0.08218891663892),(44.4687567771236,
45.1917066807094,45.9144802733946,46.6374301769804),.UNSPECIFIED.);
#88=B_SPLINE_SURFACE_WITH_KNOTS('',3,3,((#25515,#25516,#25517,#25518,#25519,
#25520),(#25521,#25522,#25523,#25524,#25525,#25526),(#25527,#25528,#25529,
#25530,#25531,#25532),(#25533,#25534,#25535,#25536,#25537,#25538)),
 .UNSPECIFIED.,.F.,.F.,.F.,(4,4),(4,1,1,4),(0.,0.0821896302845616),(38.1855707562983,
38.9085213735298,39.631294966215,40.3542455834465),.UNSPECIFIED.);
#89=B_SPLINE_SURFACE_WITH_KNOTS('',3,3,((#25539,#25540,#25541,#25542,#25543,
#25544),(#25545,#25546,#25547,#25548,#25549,#25550),(#25551,#25552,#25553,
#25554,#25555,#25556),(#25557,#25558,#25559,#25560,#25561,#25562)),
 .UNSPECIFIED.,.F.,.F.,.F.,(4,4),(4,1,1,4),(0.,0.0821902761472763),(31.902384803256,
32.6253360663502,33.3481096590354,34.0710609221296),.UNSPECIFIED.);
#90=B_SPLINE_SURFACE_WITH_KNOTS('',3,3,((#25563,#25564,#25565,#25566,#25567,
#25568),(#25569,#25570,#25571,#25572,#25573,#25574),(#25575,#25576,#25577,
#25578,#25579,#25580),(#25581,#25582,#25583,#25584,#25585,#25586)),
 .UNSPECIFIED.,.F.,.F.,.F.,(4,4),(4,1,1,4),(0.,0.0821908641246751),(25.619198908099,
26.3421507591706,27.0649243518559,27.7878762029274),.UNSPECIFIED.);
#91=B_SPLINE_SURFACE_WITH_KNOTS('',3,3,((#25587,#25588,#25589,#25590,#25591,
#25592),(#25593,#25594,#25595,#25596,#25597,#25598),(#25599,#25600,#25601,
#25602,#25603,#25604),(#25605,#25606,#25607,#25608,#25609,#25610)),
 .UNSPECIFIED.,.F.,.F.,.F.,(4,4),(4,1,1,4),(0.,0.0821914022112513),(19.3360130628329,
20.058965451991,20.7817390446763,21.5046914338344),.UNSPECIFIED.);
#92=B_SPLINE_SURFACE_WITH_KNOTS('',3,3,((#25611,#25612,#25613,#25614,#25615,
#25616),(#25617,#25618,#25619,#25620,#25621,#25622),(#25623,#25624,#25625,
#25626,#25627,#25628),(#25629,#25630,#25631,#25632,#25633,#25634)),
 .UNSPECIFIED.,.F.,.F.,.F.,(4,4),(4,1,1,4),(0.,0.0821918969420234),(13.0528272609226,
13.7757801448114,14.4985537374967,15.2215066213855),.UNSPECIFIED.);
#93=B_SPLINE_SURFACE_WITH_KNOTS('',3,3,((#25636,#25637,#25638,#25639),(#25640,
#25641,#25642,#25643),(#25644,#25645,#25646,#25647),(#25648,#25649,#25650,
#25651)),.UNSPECIFIED.,.F.,.F.,.F.,(4,4),(4,4),(0.0663734465876268,0.0820126057383863),
(11.6152142277547,12.0797346765921),.UNSPECIFIED.);
#122=SHAPE_REPRESENTATION_RELATIONSHIP('SRR','None',#28099,#132);
#132=ADVANCED_BREP_SHAPE_REPRESENTATION('',(#152),#28051);
#142=STYLED_ITEM('',(#28152),#152);
#152=MANIFOLD_SOLID_BREP('Body1',#3683);
#196=FACE_BOUND('',#785,.T.);
#237=PLANE('',#4015);
#238=PLANE('',#4016);
#239=PLANE('',#4035);
#240=PLANE('',#4057);
#241=PLANE('',#4058);
#355=CIRCLE('',#4018,3.22275);
#356=CIRCLE('',#4032,3.22275);
#357=CIRCLE('',#4036,3.933);
#358=CIRCLE('',#4039,3.933);
#359=CIRCLE('',#4055,5.);
#360=CIRCLE('',#4056,5.);
#495=FACE_OUTER_BOUND('',#724,.T.);
#496=FACE_OUTER_BOUND('',#725,.T.);
#497=FACE_OUTER_BOUND('',#726,.T.);
#498=FACE_OUTER_BOUND('',#727,.T.);
#499=FACE_OUTER_BOUND('',#728,.T.);
#500=FACE_OUTER_BOUND('',#729,.T.);
#501=FACE_OUTER_BOUND('',#730,.T.);
#502=FACE_OUTER_BOUND('',#731,.T.);
#503=FACE_OUTER_BOUND('',#732,.T.);
#504=FACE_OUTER_BOUND('',#733,.T.);
#505=FACE_OUTER_BOUND('',#734,.T.);
#506=FACE_OUTER_BOUND('',#735,.T.);
#507=FACE_OUTER_BOUND('',#736,.T.);
#508=FACE_OUTER_BOUND('',#737,.T.);
#509=FACE_OUTER_BOUND('',#738,.T.);
#510=FACE_OUTER_BOUND('',#739,.T.);
#511=FACE_OUTER_BOUND('',#740,.T.);
#512=FACE_OUTER_BOUND('',#741,.T.);
#513=FACE_OUTER_BOUND('',#742,.T.);
#514=FACE_OUTER_BOUND('',#743,.T.);
#515=FACE_OUTER_BOUND('',#744,.T.);
#516=FACE_OUTER_BOUND('',#745,.T.);
#517=FACE_OUTER_BOUND('',#746,.T.);
#518=FACE_OUTER_BOUND('',#747,.T.);
#519=FACE_OUTER_BOUND('',#748,.T.);
#520=FACE_OUTER_BOUND('',#749,.T.);
#521=FACE_OUTER_BOUND('',#750,.T.);
#522=FACE_OUTER_BOUND('',#751,.T.);
#523=FACE_OUTER_BOUND('',#752,.T.);
#524=FACE_OUTER_BOUND('',#753,.T.);
#525=FACE_OUTER_BOUND('',#754,.T.);
#526=FACE_OUTER_BOUND('',#755,.T.);
#527=FACE_OUTER_BOUND('',#756,.T.);
#528=FACE_OUTER_BOUND('',#757,.T.);
#529=FACE_OUTER_BOUND('',#758,.T.);
#530=FACE_OUTER_BOUND('',#759,.T.);
#531=FACE_OUTER_BOUND('',#760,.T.);
#532=FACE_OUTER_BOUND('',#761,.T.);
#533=FACE_OUTER_BOUND('',#762,.T.);
#534=FACE_OUTER_BOUND('',#763,.T.);
#535=FACE_OUTER_BOUND('',#764,.T.);
#536=FACE_OUTER_BOUND('',#765,.T.);
#537=FACE_OUTER_BOUND('',#766,.T.);
#538=FACE_OUTER_BOUND('',#767,.T.);
#539=FACE_OUTER_BOUND('',#768,.T.);
#540=FACE_OUTER_BOUND('',#769,.T.);
#541=FACE_OUTER_BOUND('',#770,.T.);
#542=FACE_OUTER_BOUND('',#771,.T.);
#543=FACE_OUTER_BOUND('',#772,.T.);
#544=FACE_OUTER_BOUND('',#773,.T.);
#545=FACE_OUTER_BOUND('',#774,.T.);
#546=FACE_OUTER_BOUND('',#775,.T.);
#547=FACE_OUTER_BOUND('',#776,.T.);
#548=FACE_OUTER_BOUND('',#777,.T.);
#549=FACE_OUTER_BOUND('',#778,.T.);
#550=FACE_OUTER_BOUND('',#779,.T.);
#551=FACE_OUTER_BOUND('',#780,.T.);
#552=FACE_OUTER_BOUND('',#781,.T.);
#553=FACE_OUTER_BOUND('',#782,.T.);
#554=FACE_OUTER_BOUND('',#783,.T.);
#555=FACE_OUTER_BOUND('',#784,.T.);
#556=FACE_OUTER_BOUND('',#786,.T.);
#724=EDGE_LOOP('',(#2928,#2929,#2930,#2931,#2932,#2933,#2934,#2935,#2936,
#2937,#2938,#2939,#2940,#2941,#2942,#2943,#2944,#2945,#2946,#2947,#2948,
#2949,#2950,#2951,#2952,#2953,#2954,#2955,#2956,#2957,#2958,#2959,#2960,
#2961,#2962,#2963,#2964,#2965,#2966,#2967,#2968,#2969,#2970,#2971,#2972,
#2973,#2974,#2975,#2976,#2977,#2978,#2979,#2980,#2981,#2982));
#725=EDGE_LOOP('',(#2983,#2984,#2985,#2986,#2987,#2988,#2989,#2990,#2991,
#2992,#2993,#2994,#2995,#2996,#2997,#2998,#2999,#3000,#3001,#3002,#3003,
#3004,#3005,#3006,#3007,#3008,#3009,#3010,#3011,#3012,#3013,#3014,#3015,
#3016,#3017,#3018,#3019,#3020,#3021,#3022,#3023,#3024,#3025,#3026,#3027,
#3028,#3029,#3030,#3031,#3032,#3033,#3034,#3035,#3036,#3037));
#726=EDGE_LOOP('',(#3038,#3039,#3040));
#727=EDGE_LOOP('',(#3041,#3042,#3043,#3044));
#728=EDGE_LOOP('',(#3045,#3046,#3047,#3048));
#729=EDGE_LOOP('',(#3049,#3050,#3051,#3052));
#730=EDGE_LOOP('',(#3053,#3054,#3055,#3056));
#731=EDGE_LOOP('',(#3057,#3058,#3059,#3060));
#732=EDGE_LOOP('',(#3061,#3062,#3063,#3064));
#733=EDGE_LOOP('',(#3065,#3066,#3067,#3068));
#734=EDGE_LOOP('',(#3069,#3070,#3071,#3072));
#735=EDGE_LOOP('',(#3073,#3074,#3075,#3076));
#736=EDGE_LOOP('',(#3077,#3078,#3079,#3080));
#737=EDGE_LOOP('',(#3081,#3082,#3083,#3084));
#738=EDGE_LOOP('',(#3085,#3086,#3087,#3088));
#739=EDGE_LOOP('',(#3089,#3090,#3091,#3092));
#740=EDGE_LOOP('',(#3093,#3094,#3095));
#741=EDGE_LOOP('',(#3096,#3097,#3098,#3099,#3100));
#742=EDGE_LOOP('',(#3101,#3102,#3103,#3104));
#743=EDGE_LOOP('',(#3105,#3106,#3107,#3108));
#744=EDGE_LOOP('',(#3109,#3110,#3111,#3112));
#745=EDGE_LOOP('',(#3113,#3114,#3115,#3116));
#746=EDGE_LOOP('',(#3117,#3118,#3119,#3120));
#747=EDGE_LOOP('',(#3121,#3122,#3123,#3124,#3125));
#748=EDGE_LOOP('',(#3126,#3127,#3128,#3129));
#749=EDGE_LOOP('',(#3130,#3131,#3132,#3133));
#750=EDGE_LOOP('',(#3134,#3135,#3136,#3137));
#751=EDGE_LOOP('',(#3138,#3139,#3140,#3141));
#752=EDGE_LOOP('',(#3142,#3143,#3144,#3145));
#753=EDGE_LOOP('',(#3146,#3147,#3148,#3149));
#754=EDGE_LOOP('',(#3150,#3151,#3152,#3153,#3154,#3155));
#755=EDGE_LOOP('',(#3156,#3157,#3158));
#756=EDGE_LOOP('',(#3159,#3160,#3161,#3162));
#757=EDGE_LOOP('',(#3163,#3164,#3165,#3166));
#758=EDGE_LOOP('',(#3167,#3168,#3169,#3170));
#759=EDGE_LOOP('',(#3171,#3172,#3173,#3174));
#760=EDGE_LOOP('',(#3175,#3176,#3177,#3178));
#761=EDGE_LOOP('',(#3179,#3180,#3181,#3182));
#762=EDGE_LOOP('',(#3183,#3184,#3185,#3186));
#763=EDGE_LOOP('',(#3187,#3188,#3189,#3190));
#764=EDGE_LOOP('',(#3191,#3192,#3193,#3194));
#765=EDGE_LOOP('',(#3195,#3196,#3197,#3198));
#766=EDGE_LOOP('',(#3199,#3200,#3201,#3202));
#767=EDGE_LOOP('',(#3203,#3204,#3205,#3206));
#768=EDGE_LOOP('',(#3207,#3208,#3209,#3210));
#769=EDGE_LOOP('',(#3211,#3212,#3213,#3214));
#770=EDGE_LOOP('',(#3215,#3216,#3217,#3218));
#771=EDGE_LOOP('',(#3219,#3220,#3221,#3222));
#772=EDGE_LOOP('',(#3223,#3224,#3225,#3226));
#773=EDGE_LOOP('',(#3227,#3228,#3229,#3230));
#774=EDGE_LOOP('',(#3231,#3232,#3233,#3234));
#775=EDGE_LOOP('',(#3235,#3236,#3237,#3238,#3239));
#776=EDGE_LOOP('',(#3240,#3241,#3242,#3243));
#777=EDGE_LOOP('',(#3244,#3245,#3246,#3247));
#778=EDGE_LOOP('',(#3248,#3249,#3250,#3251));
#779=EDGE_LOOP('',(#3252,#3253,#3254,#3255));
#780=EDGE_LOOP('',(#3256,#3257,#3258,#3259));
#781=EDGE_LOOP('',(#3260,#3261,#3262,#3263,#3264));
#782=EDGE_LOOP('',(#3265,#3266,#3267));
#783=EDGE_LOOP('',(#3268,#3269,#3270,#3271));
#784=EDGE_LOOP('',(#3272));
#785=EDGE_LOOP('',(#3273,#3274,#3275,#3276,#3277,#3278,#3279,#3280));
#786=EDGE_LOOP('',(#3281));
#894=LINE('',#22166,#1052);
#895=LINE('',#22175,#1053);
#896=LINE('',#22186,#1054);
#897=LINE('',#22197,#1055);
#898=LINE('',#22208,#1056);
#899=LINE('',#22219,#1057);
#900=LINE('',#22230,#1058);
#901=LINE('',#22241,#1059);
#902=LINE('',#22252,#1060);
#903=LINE('',#22263,#1061);
#904=LINE('',#22274,#1062);
#905=LINE('',#22285,#1063);
#906=LINE('',#22296,#1064);
#907=LINE('',#22307,#1065);
#908=LINE('',#22309,#1066);
#909=LINE('',#22318,#1067);
#910=LINE('',#22329,#1068);
#911=LINE('',#22340,#1069);
#912=LINE('',#22351,#1070);
#913=LINE('',#22362,#1071);
#914=LINE('',#22373,#1072);
#915=LINE('',#22384,#1073);
#916=LINE('',#22395,#1074);
#917=LINE('',#22406,#1075);
#918=LINE('',#22417,#1076);
#919=LINE('',#22428,#1077);
#920=LINE('',#22439,#1078);
#921=LINE('',#22449,#1079);
#922=LINE('',#22460,#1080);
#923=LINE('',#22471,#1081);
#924=LINE('',#22482,#1082);
#925=LINE('',#22493,#1083);
#926=LINE('',#22504,#1084);
#927=LINE('',#22515,#1085);
#928=LINE('',#22526,#1086);
#929=LINE('',#22537,#1087);
#930=LINE('',#22548,#1088);
#931=LINE('',#22559,#1089);
#932=LINE('',#22570,#1090);
#933=LINE('',#22581,#1091);
#934=LINE('',#22592,#1092);
#935=LINE('',#22594,#1093);
#936=LINE('',#22603,#1094);
#937=LINE('',#22614,#1095);
#938=LINE('',#22625,#1096);
#939=LINE('',#22636,#1097);
#940=LINE('',#22647,#1098);
#941=LINE('',#22658,#1099);
#942=LINE('',#22669,#1100);
#943=LINE('',#22680,#1101);
#944=LINE('',#22691,#1102);
#945=LINE('',#22702,#1103);
#946=LINE('',#22713,#1104);
#947=LINE('',#22724,#1105);
#948=LINE('',#22735,#1106);
#949=LINE('',#22745,#1107);
#950=LINE('',#25657,#1108);
#1052=VECTOR('',#4619,10.);
#1053=VECTOR('',#4620,10.);
#1054=VECTOR('',#4621,10.);
#1055=VECTOR('',#4622,10.);
#1056=VECTOR('',#4623,10.);
#1057=VECTOR('',#4624,10.);
#1058=VECTOR('',#4625,10.);
#1059=VECTOR('',#4626,10.);
#1060=VECTOR('',#4627,10.);
#1061=VECTOR('',#4628,10.);
#1062=VECTOR('',#4629,10.);
#1063=VECTOR('',#4630,10.);
#1064=VECTOR('',#4631,10.);
#1065=VECTOR('',#4632,10.);
#1066=VECTOR('',#4633,10.);
#1067=VECTOR('',#4634,10.);
#1068=VECTOR('',#4635,10.);
#1069=VECTOR('',#4636,10.);
#1070=VECTOR('',#4637,10.);
#1071=VECTOR('',#4638,10.);
#1072=VECTOR('',#4639,10.);
#1073=VECTOR('',#4640,10.);
#1074=VECTOR('',#4641,10.);
#1075=VECTOR('',#4642,10.);
#1076=VECTOR('',#4643,10.);
#1077=VECTOR('',#4644,10.);
#1078=VECTOR('',#4645,10.);
#1079=VECTOR('',#4646,10.);
#1080=VECTOR('',#4649,10.);
#1081=VECTOR('',#4650,10.);
#1082=VECTOR('',#4651,10.);
#1083=VECTOR('',#4652,10.);
#1084=VECTOR('',#4653,10.);
#1085=VECTOR('',#4654,10.);
#1086=VECTOR('',#4655,10.);
#1087=VECTOR('',#4656,10.);
#1088=VECTOR('',#4657,10.);
#1089=VECTOR('',#4658,10.);
#1090=VECTOR('',#4659,10.);
#1091=VECTOR('',#4660,10.);
#1092=VECTOR('',#4661,10.);
#1093=VECTOR('',#4662,10.);
#1094=VECTOR('',#4663,10.);
#1095=VECTOR('',#4664,10.);
#1096=VECTOR('',#4665,10.);
#1097=VECTOR('',#4666,10.);
#1098=VECTOR('',#4667,10.);
#1099=VECTOR('',#4668,10.);
#1100=VECTOR('',#4669,10.);
#1101=VECTOR('',#4670,10.);
#1102=VECTOR('',#4671,10.);
#1103=VECTOR('',#4672,10.);
#1104=VECTOR('',#4673,10.);
#1105=VECTOR('',#4674,10.);
#1106=VECTOR('',#4675,10.);
#1107=VECTOR('',#4676,10.);
#1108=VECTOR('',#4755,5.);
#1274=B_SPLINE_CURVE_WITH_KNOTS('',3,(#22157,#22158,#22159,#22160,#22161,
#22162,#22163,#22164),.UNSPECIFIED.,.F.,.F.,(4,2,2,4),(0.,0.000697892015497008,
0.0143255677369775,0.0286350340362092),.UNSPECIFIED.);
#1275=B_SPLINE_CURVE_WITH_KNOTS('',3,(#22168,#22169,#22170,#22171,#22172,
#22173),.UNSPECIFIED.,.F.,.F.,(4,2,4),(0.,0.0523373446002982,0.104355593610831),
 .UNSPECIFIED.);
#1276=B_SPLINE_CURVE_WITH_KNOTS('',3,(#22177,#22178,#22179,#22180,#22181,
#22182,#22183,#22184),.UNSPECIFIED.,.F.,.F.,(4,2,2,4),(0.,0.00526521584710592,
0.0639602373511304,0.128212067318051),.UNSPECIFIED.);
#1277=B_SPLINE_CURVE_WITH_KNOTS('',3,(#22188,#22189,#22190,#22191,#22192,
#22193,#22194,#22195),.UNSPECIFIED.,.F.,.F.,(4,2,2,4),(0.,0.0627475271162915,
0.120075061733582,0.125236068694296),.UNSPECIFIED.);
#1278=B_SPLINE_CURVE_WITH_KNOTS('',3,(#22199,#22200,#22201,#22202,#22203,
#22204,#22205,#22206),.UNSPECIFIED.,.F.,.F.,(4,2,2,4),(0.,0.00526560282662867,
0.0639612078258487,0.128213120660444),.UNSPECIFIED.);
#1279=B_SPLINE_CURVE_WITH_KNOTS('',3,(#22210,#22211,#22212,#22213,#22214,
#22215,#22216,#22217),.UNSPECIFIED.,.F.,.F.,(4,2,2,4),(0.,0.0627475590562519,
0.120075649624267,0.125237044527633),.UNSPECIFIED.);
#1280=B_SPLINE_CURVE_WITH_KNOTS('',3,(#22221,#22222,#22223,#22224,#22225,
#22226,#22227,#22228),.UNSPECIFIED.,.F.,.F.,(4,2,2,4),(0.,0.00526602648868038,
0.0639622680416072,0.128214273235454),.UNSPECIFIED.);
#1281=B_SPLINE_CURVE_WITH_KNOTS('',3,(#22232,#22233,#22234,#22235,#22236,
#22237,#22238,#22239),.UNSPECIFIED.,.F.,.F.,(4,2,2,4),(0.,0.0627475953399776,
0.120076292215752,0.125238111923284),.UNSPECIFIED.);
#1282=B_SPLINE_CURVE_WITH_KNOTS('',3,(#22243,#22244,#22245,#22246,#22247,
#22248,#22249,#22250),.UNSPECIFIED.,.F.,.F.,(4,2,2,4),(0.,0.00526649276184272,
0.0639634322919596,0.128215541011568),.UNSPECIFIED.);
#1283=B_SPLINE_CURVE_WITH_KNOTS('',3,(#22254,#22255,#22256,#22257,#22258,
#22259,#22260,#22261),.UNSPECIFIED.,.F.,.F.,(4,2,2,4),(0.,0.0627476367935851,
0.120076998293466,0.125239285656593),.UNSPECIFIED.);
#1284=B_SPLINE_CURVE_WITH_KNOTS('',3,(#22265,#22266,#22267,#22268,#22269,
#22270,#22271,#22272),.UNSPECIFIED.,.F.,.F.,(4,2,2,4),(0.,0.00526700898296905,
0.0639647182192301,0.128216943693669),.UNSPECIFIED.);
#1285=B_SPLINE_CURVE_WITH_KNOTS('',3,(#22276,#22277,#22278,#22279,#22280,
#22281,#22282,#22283),.UNSPECIFIED.,.F.,.F.,(4,2,2,4),(0.,0.0627476844547414,
0.120077778736361,0.125240584036134),.UNSPECIFIED.);
#1286=B_SPLINE_CURVE_WITH_KNOTS('',3,(#22287,#22288,#22289,#22290,#22291,
#22292,#22293,#22294),.UNSPECIFIED.,.F.,.F.,(4,2,2,4),(0.,0.0052675843601308,
0.0639661480124282,0.12821850616927),.UNSPECIFIED.);
#1287=B_SPLINE_CURVE_WITH_KNOTS('',3,(#22298,#22299,#22300,#22301,#22302,
#22303,#22304,#22305),.UNSPECIFIED.,.F.,.F.,(4,2,2,4),(0.,0.0627497316200279,
0.120007641766305,0.125309768916132),.UNSPECIFIED.);
#1288=B_SPLINE_CURVE_WITH_KNOTS('',3,(#22311,#22312,#22313,#22314,#22315,
#22316),.UNSPECIFIED.,.F.,.F.,(4,2,4),(1.75570920373614E-15,0.0320055376006011,
0.0638199285984987),.UNSPECIFIED.);
#1289=B_SPLINE_CURVE_WITH_KNOTS('',3,(#22320,#22321,#22322,#22323,#22324,
#22325,#22326,#22327),.UNSPECIFIED.,.F.,.F.,(4,2,2,4),(0.,0.00526977567755582,
0.0639683005470083,0.128217977351555),.UNSPECIFIED.);
#1290=B_SPLINE_CURVE_WITH_KNOTS('',3,(#22331,#22332,#22333,#22334,#22335,
#22336,#22337,#22338),.UNSPECIFIED.,.F.,.F.,(4,2,2,4),(0.,0.062761494454614,
0.120090502459536,0.125241025317951),.UNSPECIFIED.);
#1291=B_SPLINE_CURVE_WITH_KNOTS('',3,(#22342,#22343,#22344,#22345,#22346,
#22347,#22348,#22349),.UNSPECIFIED.,.F.,.F.,(4,2,2,4),(0.,0.00526922229267531,
0.0639669243235216,0.128216474527037),.UNSPECIFIED.);
#1292=B_SPLINE_CURVE_WITH_KNOTS('',3,(#22353,#22354,#22355,#22356,#22357,
#22358,#22359,#22360),.UNSPECIFIED.,.F.,.F.,(4,2,2,4),(0.,0.0627614441556716,
0.120089692527127,0.125239677665907),.UNSPECIFIED.);
#1293=B_SPLINE_CURVE_WITH_KNOTS('',3,(#22364,#22365,#22366,#22367,#22368,
#22369,#22370,#22371),.UNSPECIFIED.,.F.,.F.,(4,2,2,4),(0.,0.0052687245725873,
0.0639656835644766,0.128215122077758),.UNSPECIFIED.);
#1294=B_SPLINE_CURVE_WITH_KNOTS('',3,(#22375,#22376,#22377,#22378,#22379,
#22380,#22381,#22382),.UNSPECIFIED.,.F.,.F.,(4,2,2,4),(0.,0.0627614005096921,
0.120088961436388,0.125238462177896),.UNSPECIFIED.);
#1295=B_SPLINE_CURVE_WITH_KNOTS('',3,(#22386,#22387,#22388,#22389,#22390,
#22391,#22392,#22393),.UNSPECIFIED.,.F.,.F.,(4,2,2,4),(0.,0.00526827403022492,
0.0639645578123657,0.128213897069805),.UNSPECIFIED.);
#1296=B_SPLINE_CURVE_WITH_KNOTS('',3,(#22397,#22398,#22399,#22400,#22401,
#22402,#22403,#22404),.UNSPECIFIED.,.F.,.F.,(4,2,2,4),(0.,0.0627613623859368,
0.12008829741618,0.125237359044329),.UNSPECIFIED.);
#1297=B_SPLINE_CURVE_WITH_KNOTS('',3,(#22408,#22409,#22410,#22411,#22412,
#22413,#22414,#22415),.UNSPECIFIED.,.F.,.F.,(4,2,2,4),(0.,0.0052678638691292,
0.0639635307055346,0.128212781223319),.UNSPECIFIED.);
#1298=B_SPLINE_CURVE_WITH_KNOTS('',3,(#22419,#22420,#22421,#22422,#22423,
#22424,#22425,#22426),.UNSPECIFIED.,.F.,.F.,(4,2,2,4),(0.,0.0627613288883452,
0.120087691004123,0.125236352349363),.UNSPECIFIED.);
#1299=B_SPLINE_CURVE_WITH_KNOTS('',3,(#22430,#22431,#22432,#22433,#22434,
#22435,#22436,#22437),.UNSPECIFIED.,.F.,.F.,(4,2,2,4),(0.,0.00526748857527077,
0.0639625889506368,0.128211759700356),.UNSPECIFIED.);
#1300=B_SPLINE_CURVE_WITH_KNOTS('',3,(#22441,#22442,#22443,#22444,#22445,
#22446,#22447,#22448),.UNSPECIFIED.,.F.,.F.,(4,2,2,4),(0.,0.0627622351934734,
0.120057633553872,0.125268887079596),.UNSPECIFIED.);
#1301=B_SPLINE_CURVE_WITH_KNOTS('',3,(#22453,#22454,#22455,#22456,#22457,
#22458),.UNSPECIFIED.,.F.,.F.,(4,2,4),(0.,0.0498589762945784,0.0999595266847454),
 .UNSPECIFIED.);
#1302=B_SPLINE_CURVE_WITH_KNOTS('',3,(#22462,#22463,#22464,#22465,#22466,
#22467,#22468,#22469),.UNSPECIFIED.,.F.,.F.,(4,2,2,4),(0.,0.0627475125621108,
0.120074786005034,0.125235611253279),.UNSPECIFIED.);
#1303=B_SPLINE_CURVE_WITH_KNOTS('',3,(#22473,#22474,#22475,#22476,#22477,
#22478,#22479,#22480),.UNSPECIFIED.,.F.,.F.,(4,2,2,4),(0.,0.00526540507665305,
0.0639607121557458,0.128212582461846),.UNSPECIFIED.);
#1304=B_SPLINE_CURVE_WITH_KNOTS('',3,(#22484,#22485,#22486,#22487,#22488,
#22489,#22490,#22491),.UNSPECIFIED.,.F.,.F.,(4,2,2,4),(0.,0.0627475425879394,
0.120075349322764,0.125236545975591),.UNSPECIFIED.);
#1305=B_SPLINE_CURVE_WITH_KNOTS('',3,(#22495,#22496,#22497,#22498,#22499,
#22500,#22501,#22502),.UNSPECIFIED.,.F.,.F.,(4,2,2,4),(0.,0.00526580973145337,
0.0639617259034633,0.128213683646694),.UNSPECIFIED.);
#1306=B_SPLINE_CURVE_WITH_KNOTS('',3,(#22506,#22507,#22508,#22509,#22510,
#22511,#22512,#22513),.UNSPECIFIED.,.F.,.F.,(4,2,2,4),(0.,0.0627475766076911,
0.120075963575788,0.12523756592846),.UNSPECIFIED.);
#1307=B_SPLINE_CURVE_WITH_KNOTS('',3,(#22517,#22518,#22519,#22520,#22521,
#22522,#22523,#22524),.UNSPECIFIED.,.F.,.F.,(4,2,2,4),(0.,0.00526625387771515,
0.063962836142632,0.128214891577853),.UNSPECIFIED.);
#1308=B_SPLINE_CURVE_WITH_KNOTS('',3,(#22528,#22529,#22530,#22531,#22532,
#22533,#22534,#22535),.UNSPECIFIED.,.F.,.F.,(4,2,2,4),(0.,0.0627476153613634,
0.120076636694826,0.12523868444785),.UNSPECIFIED.);
#1309=B_SPLINE_CURVE_WITH_KNOTS('',3,(#22539,#22540,#22541,#22542,#22543,
#22544,#22545,#22546),.UNSPECIFIED.,.F.,.F.,(4,2,2,4),(0.,0.00526674410433897,
0.063964058787172,0.128216224084347),.UNSPECIFIED.);
#1310=B_SPLINE_CURVE_WITH_KNOTS('',3,(#22550,#22551,#22552,#22553,#22554,
#22555,#22556,#22557),.UNSPECIFIED.,.F.,.F.,(4,2,2,4),(0.,0.0627476597736949,
0.120077378440881,0.125239917954739),.UNSPECIFIED.);
#1311=B_SPLINE_CURVE_WITH_KNOTS('',3,(#22561,#22562,#22563,#22564,#22565,
#22566,#22567,#22568),.UNSPECIFIED.,.F.,.F.,(4,2,2,4),(0.,0.00526728861301724,
0.0639654135345664,0.128217703164965),.UNSPECIFIED.);
#1312=B_SPLINE_CURVE_WITH_KNOTS('',3,(#22572,#22573,#22574,#22575,#22576,
#22577,#22578,#22579),.UNSPECIFIED.,.F.,.F.,(4,2,2,4),(0.,0.0627477110123208,
0.120078200979348,0.125241286926992),.UNSPECIFIED.);
#1313=B_SPLINE_CURVE_WITH_KNOTS('',3,(#22583,#22584,#22585,#22586,#22587,
#22588,#22589,#22590),.UNSPECIFIED.,.F.,.F.,(4,2,2,4),(0.,0.00526789777186566,
0.0639669253649914,0.128219356862823),.UNSPECIFIED.);
#1314=B_SPLINE_CURVE_WITH_KNOTS('',3,(#22596,#22597,#22598,#22599,#22600,
#22601),.UNSPECIFIED.,.F.,.F.,(4,2,4),(0.,0.0322464693148723,0.0645605482559509),
 .UNSPECIFIED.);
#1315=B_SPLINE_CURVE_WITH_KNOTS('',3,(#22605,#22606,#22607,#22608,#22609,
#22610,#22611,#22612),.UNSPECIFIED.,.F.,.F.,(4,2,2,4),(0.,0.0627615225357567,
0.12009094148456,0.125241756269418),.UNSPECIFIED.);
#1316=B_SPLINE_CURVE_WITH_KNOTS('',3,(#22616,#22617,#22618,#22619,#22620,
#22621,#22622,#22623),.UNSPECIFIED.,.F.,.F.,(4,2,2,4),(0.,0.00526949141755586,
0.0639675940491126,0.128217205528332),.UNSPECIFIED.);
#1317=B_SPLINE_CURVE_WITH_KNOTS('',3,(#22627,#22628,#22629,#22630,#22631,
#22632,#22633,#22634),.UNSPECIFIED.,.F.,.F.,(4,2,2,4),(0.,0.0627614683917021,
0.120090086793172,0.125240333549308),.UNSPECIFIED.);
#1318=B_SPLINE_CURVE_WITH_KNOTS('',3,(#22638,#22639,#22640,#22641,#22642,
#22643,#22644,#22645),.UNSPECIFIED.,.F.,.F.,(4,2,2,4),(0.,0.00526896705103507,
0.0639662884118339,0.128215781088997),.UNSPECIFIED.);
#1319=B_SPLINE_CURVE_WITH_KNOTS('',3,(#22649,#22650,#22651,#22652,#22653,
#22654,#22655,#22656),.UNSPECIFIED.,.F.,.F.,(4,2,2,4),(0.,0.0627614215780341,
0.120089317924044,0.125239054744074),.UNSPECIFIED.);
#1320=B_SPLINE_CURVE_WITH_KNOTS('',3,(#22660,#22661,#22662,#22663,#22664,
#22665,#22666,#22667),.UNSPECIFIED.,.F.,.F.,(4,2,2,4),(0.,0.00526849386310405,
0.0639651074163281,0.128214494876759),.UNSPECIFIED.);
#1321=B_SPLINE_CURVE_WITH_KNOTS('',3,(#22671,#22672,#22673,#22674,#22675,
#22676,#22677,#22678),.UNSPECIFIED.,.F.,.F.,(4,2,2,4),(0.,0.0627613808182858,
0.120088621680663,0.125237897640557),.UNSPECIFIED.);
#1322=B_SPLINE_CURVE_WITH_KNOTS('',3,(#22682,#22683,#22684,#22685,#22686,
#22687,#22688,#22689),.UNSPECIFIED.,.F.,.F.,(4,2,2,4),(0.,0.00526806427303071,
0.0639640328250225,0.128213326505552),.UNSPECIFIED.);
#1323=B_SPLINE_CURVE_WITH_KNOTS('',3,(#22693,#22694,#22695,#22696,#22697,
#22698,#22699,#22700),.UNSPECIFIED.,.F.,.F.,(4,2,2,4),(0.,0.0627613451073725,
0.120087987526447,0.125236844511966),.UNSPECIFIED.);
#1324=B_SPLINE_CURVE_WITH_KNOTS('',3,(#22704,#22705,#22706,#22707,#22708,
#22709,#22710,#22711),.UNSPECIFIED.,.F.,.F.,(4,2,2,4),(0.,0.00526767216729547,
0.0639630498969236,0.128212259500237),.UNSPECIFIED.);
#1325=B_SPLINE_CURVE_WITH_KNOTS('',3,(#22715,#22716,#22717,#22718,#22719,
#22720,#22721,#22722),.UNSPECIFIED.,.F.,.F.,(4,2,2,4),(0.,0.0627613136441549,
0.120087406937392,0.125235881024186),.UNSPECIFIED.);
#1326=B_SPLINE_CURVE_WITH_KNOTS('',3,(#22726,#22727,#22728,#22729,#22730,
#22731,#22732,#22733),.UNSPECIFIED.,.F.,.F.,(4,2,2,4),(0.,0.00526731255574918,
0.0639621465613893,0.128211280360621),.UNSPECIFIED.);
#1327=B_SPLINE_CURVE_WITH_KNOTS('',3,(#22737,#22738,#22739,#22740,#22741,
#22742,#22743,#22744),.UNSPECIFIED.,.F.,.F.,(4,2,2,4),(0.,0.0104628362527636,
0.0207308659069718,0.0209057471409188),.UNSPECIFIED.);
#1328=B_SPLINE_CURVE_WITH_KNOTS('',3,(#22748,#22749,#22750,#22751,#22752,
#22753,#22754,#22755,#22756,#22757,#22758,#22759,#22760,#22761,#22762,#22763,
#22764,#22765,#22766,#22767,#22768,#22769,#22770,#22771,#22772,#22773,#22774,
#22775,#22776,#22777,#22778,#22779,#22780,#22781,#22782,#22783,#22784),
 .UNSPECIFIED.,.F.,.F.,(4,3,3,3,3,3,3,3,3,3,3,3,4),(50.7521183952037,50.8495790953441,
50.9470219254028,51.0444588598502,51.1419334813167,51.2394182564582,51.3369688385417,
51.4243296588263,51.5251265267957,51.6212969234942,51.7174260205839,51.8135342633692,
51.827517130704),.UNSPECIFIED.);
#1329=B_SPLINE_CURVE_WITH_KNOTS('',3,(#22787,#22788,#22789,#22790,#22791,
#22792,#22793,#22794,#22795,#22796,#22797,#22798,#22799,#22800,#22801,#22802,
#22803,#22804,#22805,#22806,#22807,#22808,#22809,#22810,#22811,#22812,#22813,
#22814,#22815,#22816,#22817,#22818,#22819,#22820,#22821,#22822,#22823,#22824,
#22825,#22826,#22827,#22828,#22829,#22830,#22831,#22832,#22833,#22834,#22835,
#22836,#22837,#22838,#22839,#22840,#22841,#22842,#22843,#22844,#22845,#22846,
#22847,#22848,#22849,#22850,#22851,#22852,#22853,#22854,#22855,#22856,#22857,
#22858,#22859),.UNSPECIFIED.,.F.,.F.,(4,3,3,3,3,3,3,3,3,3,3,3,3,3,3,3,3,
3,3,3,3,3,3,3,4),(47.6105257416139,47.7077041422575,47.8048611288827,47.9020100199129,
47.999164126441,48.0963691196497,48.1935970979194,48.2908967620636,48.3332993342991,
48.4283008104292,48.5232388584473,48.6181347145911,48.7130095721038,48.8079167672776,
48.9028389899736,48.9978424868404,49.0560729269844,49.1533688574346,49.2506064158459,
49.3477990026261,49.4449599775623,49.5421169168093,49.6392652595687,49.7364384779762,
49.7788465196697),.UNSPECIFIED.);
#1330=B_SPLINE_CURVE_WITH_KNOTS('',3,(#22860,#22861,#22862,#22863,#22864,
#22865,#22866,#22867,#22868,#22869,#22870,#22871,#22872,#22873,#22874,#22875,
#22876,#22877,#22878,#22879,#22880,#22881,#22882,#22883,#22884,#22885,#22886,
#22887,#22888,#22889,#22890,#22891,#22892,#22893,#22894,#22895,#22896,#22897,
#22898,#22899,#22900,#22901,#22902,#22903,#22904,#22905,#22906,#22907,#22908,
#22909,#22910,#22911,#22912,#22913,#22914,#22915,#22916,#22917,#22918,#22919,
#22920,#22921,#22922,#22923,#22924,#22925,#22926,#22927,#22928,#22929,#22930,
#22931,#22932),.UNSPECIFIED.,.F.,.F.,(4,3,3,3,3,3,3,3,3,3,3,3,3,3,3,3,3,
3,3,3,3,3,3,3,4),(47.6105257416139,47.7076886147176,47.8048298475205,47.9019628289092,
47.9991009402533,48.0962899832716,48.1935020701131,48.2907860931928,48.3332993342991,
48.4283243574566,48.523286131773,48.6182058374566,48.7131046117988,48.8080356576868,
48.9029816882567,48.9980087284196,49.0560729269844,49.153353193078,49.2505749096157,
49.3477515476114,49.4448965372306,49.5420376028857,49.6391701728657,49.736327918173,
49.7788465196697),.UNSPECIFIED.);
#1331=B_SPLINE_CURVE_WITH_KNOTS('',3,(#22934,#22935,#22936,#22937,#22938,
#22939,#22940,#22941,#22942,#22943,#22944,#22945,#22946,#22947,#22948,#22949,
#22950,#22951,#22952,#22953,#22954,#22955,#22956,#22957,#22958,#22959,#22960,
#22961,#22962,#22963,#22964,#22965,#22966,#22967,#22968,#22969,#22970,#22971,
#22972,#22973,#22974,#22975,#22976,#22977,#22978,#22979,#22980,#22981,#22982,
#22983,#22984,#22985,#22986,#22987,#22988,#22989,#22990,#22991,#22992,#22993,
#22994,#22995,#22996,#22997,#22998,#22999,#23000,#23001,#23002,#23003,#23004,
#23005,#23006),.UNSPECIFIED.,.F.,.F.,(4,3,3,3,3,3,3,3,3,3,3,3,3,3,3,3,3,
3,3,3,3,3,3,3,4),(44.4689330880241,44.5660877812095,44.6632207148829,44.7603453149378,
44.8574749996526,44.9546556391961,45.0518593530952,45.1491351344189,45.1917066807094,
45.2867442474327,45.3817186612472,45.4766510723439,45.5715625880392,45.6665063398916,
45.7614650533526,45.8565046349539,45.9144802733946,46.011752285669,46.1089656554364,
46.2061338907896,46.3032704588545,46.4004031621129,46.4975274228661,46.5946770168463,
46.6372538660799),.UNSPECIFIED.);
#1332=B_SPLINE_CURVE_WITH_KNOTS('',3,(#23007,#23008,#23009,#23010,#23011,
#23012,#23013,#23014,#23015,#23016,#23017,#23018,#23019,#23020,#23021,#23022,
#23023,#23024,#23025,#23026,#23027,#23028,#23029,#23030,#23031,#23032,#23033,
#23034,#23035,#23036,#23037,#23038,#23039,#23040,#23041,#23042,#23043,#23044,
#23045,#23046,#23047,#23048,#23049,#23050,#23051,#23052,#23053,#23054,#23055,
#23056,#23057,#23058,#23059,#23060,#23061,#23062,#23063,#23064,#23065,#23066,
#23067,#23068,#23069,#23070,#23071,#23072,#23073,#23074,#23075,#23076,#23077,
#23078,#23079),.UNSPECIFIED.,.F.,.F.,(4,3,3,3,3,3,3,3,3,3,3,3,3,3,3,3,3,
3,3,3,3,3,3,3,4),(44.4689330880241,44.5661021364053,44.6632496344749,44.7603889431301,
44.8575334158252,44.954728802457,45.0519472096645,45.149237453745,45.1917066807094,
45.2867222998457,45.3816745984183,45.4765847790615,45.5714740014621,45.6663955218626,
45.7613320441279,45.8563496818008,45.9144802733946,46.0117667696916,46.1089947868675,
46.2061777678908,46.3033291149719,46.4004764935731,46.4976153363918,46.5947792353533,
46.6372538660799),.UNSPECIFIED.);
#1333=B_SPLINE_CURVE_WITH_KNOTS('',3,(#23081,#23082,#23083,#23084,#23085,
#23086,#23087,#23088,#23089,#23090,#23091,#23092,#23093,#23094,#23095,#23096,
#23097,#23098,#23099,#23100,#23101,#23102,#23103,#23104,#23105,#23106,#23107,
#23108,#23109,#23110,#23111,#23112,#23113,#23114,#23115,#23116,#23117,#23118,
#23119,#23120,#23121,#23122,#23123,#23124,#23125,#23126,#23127,#23128,#23129,
#23130,#23131,#23132,#23133,#23134,#23135,#23136,#23137,#23138,#23139,#23140,
#23141,#23142,#23143,#23144,#23145,#23146,#23147,#23148,#23149,#23150,#23151,
#23152,#23153),.UNSPECIFIED.,.F.,.F.,(4,3,3,3,3,3,3,3,3,3,3,3,3,3,3,3,3,
3,3,3,3,3,3,3,4),(41.3273404344343,41.4245008426539,41.5216395746521,41.6187700304753,
41.7159056026232,41.8130921134644,41.9103016773613,42.0075832170803,42.0501140271196,
42.1451428193501,42.2401083915334,42.3350319148704,42.4299345176583,42.5248693813708,
42.6198192228509,42.7148500314578,42.7728876198048,42.8701653988873,42.9673846003622,
43.0645587064248,43.1617011583864,43.2588397041862,43.3559697703269,43.4531250593715,
43.4956612124901),.UNSPECIFIED.);
#1334=B_SPLINE_CURVE_WITH_KNOTS('',3,(#23154,#23155,#23156,#23157,#23158,
#23159,#23160,#23161,#23162,#23163,#23164,#23165,#23166,#23167,#23168,#23169,
#23170,#23171,#23172,#23173,#23174,#23175,#23176,#23177,#23178,#23179,#23180,
#23181,#23182,#23183,#23184,#23185,#23186,#23187,#23188,#23189,#23190,#23191,
#23192,#23193,#23194,#23195,#23196,#23197,#23198,#23199,#23200,#23201,#23202,
#23203,#23204,#23205,#23206,#23207,#23208,#23209,#23210,#23211,#23212,#23213,
#23214,#23215,#23216,#23217,#23218,#23219,#23220,#23221,#23222,#23223,#23224,
#23225,#23226),.UNSPECIFIED.,.F.,.F.,(4,3,3,3,3,3,3,3,3,3,3,3,3,3,3,3,3,
3,3,3,3,3,3,3,4),(41.3273404344343,41.4244875449837,41.5216127854883,41.6187296160768,
41.7158514891715,41.8130243381864,41.9102202895791,42.0074884295393,42.0501140271195,
42.1451633170348,42.2401495439751,42.3350938299693,42.4300172542117,42.5249728814293,
42.6199434485318,42.7149947512481,42.7728876198048,42.8701519796663,42.9673576112281,
43.0645180568829,43.1616468179474,43.2587717692632,43.3558883274192,43.4530303652185,
43.4956612124901),.UNSPECIFIED.);
#1335=B_SPLINE_CURVE_WITH_KNOTS('',3,(#23228,#23229,#23230,#23231,#23232,
#23233,#23234,#23235,#23236,#23237,#23238,#23239,#23240,#23241,#23242,#23243,
#23244,#23245,#23246,#23247,#23248,#23249,#23250,#23251,#23252,#23253,#23254,
#23255,#23256,#23257,#23258,#23259,#23260,#23261,#23262,#23263,#23264,#23265,
#23266,#23267,#23268,#23269,#23270,#23271,#23272,#23273,#23274,#23275,#23276,
#23277,#23278,#23279,#23280,#23281,#23282,#23283,#23284,#23285,#23286,#23287,
#23288,#23289,#23290,#23291,#23292,#23293,#23294,#23295,#23296,#23297,#23298,
#23299,#23300),.UNSPECIFIED.,.F.,.F.,(4,3,3,3,3,3,3,3,3,3,3,3,3,3,3,3,3,
3,3,3,3,3,3,3,4),(38.1857477808445,38.2828878496606,38.3800059457443,38.4771155609571,
38.5742301793694,38.6713957929425,38.7685845346598,38.8658455770237,38.9085213735298,
39.0035816400817,39.0985789281084,39.1935343331749,39.2884689080497,39.383435654736,
39.478417320826,39.5734795981558,39.631294966215,39.7285522183372,39.8257506628246,
39.9229038738615,40.0200253844543,40.1171431366437,40.2142525415632,40.3113875621596,
40.3540685589003),.UNSPECIFIED.);
#1336=B_SPLINE_CURVE_WITH_KNOTS('',3,(#23301,#23302,#23303,#23304,#23305,
#23306,#23307,#23308,#23309,#23310,#23311,#23312,#23313,#23314,#23315,#23316,
#23317,#23318,#23319,#23320,#23321,#23322,#23323,#23324,#23325,#23326,#23327,
#23328,#23329,#23330,#23331,#23332,#23333,#23334,#23335,#23336,#23337,#23338,
#23339,#23340,#23341,#23342,#23343,#23344,#23345,#23346,#23347,#23348,#23349,
#23350,#23351,#23352,#23353,#23354,#23355,#23356,#23357,#23358,#23359,#23360,
#23361,#23362,#23363,#23364,#23365,#23366,#23367,#23368,#23369,#23370,#23371,
#23372,#23373),.UNSPECIFIED.,.F.,.F.,(4,3,3,3,3,3,3,3,3,3,3,3,3,3,3,3,3,
3,3,3,3,3,3,3,4),(38.1857477808445,38.2829001906186,38.3800308075986,38.4771530679947,
38.5742804003744,38.6714586939732,38.7686600703952,38.8659335507706,38.9085213735298,
39.0035624604914,39.0985404215215,39.1934763983655,39.2883914899063,39.3833388076511,
39.4783010804979,39.5733441817229,39.631294966215,39.7285646742001,39.8257757138043,
39.9229416034566,40.0200758205865,40.1172061894662,40.214328130694,40.3114754492342,
40.3540685589003),.UNSPECIFIED.);
#1337=B_SPLINE_CURVE_WITH_KNOTS('',3,(#23375,#23376,#23377,#23378,#23379,
#23380,#23381,#23382,#23383,#23384,#23385,#23386,#23387,#23388,#23389,#23390,
#23391,#23392,#23393,#23394,#23395,#23396,#23397,#23398,#23399,#23400,#23401,
#23402,#23403,#23404,#23405,#23406,#23407,#23408,#23409,#23410,#23411,#23412,
#23413,#23414,#23415,#23416,#23417,#23418,#23419,#23420,#23421,#23422,#23423,
#23424,#23425,#23426,#23427,#23428,#23429,#23430,#23431,#23432,#23433,#23434,
#23435,#23436,#23437,#23438,#23439,#23440,#23441,#23442,#23443,#23444,#23445,
#23446,#23447),.UNSPECIFIED.,.F.,.F.,(4,3,3,3,3,3,3,3,3,3,3,3,3,3,3,3,3,
3,3,3,3,3,3,3,4),(35.0441551272547,35.1413001185802,35.2384232089616,35.3355378680837,
35.4326575578995,35.5298282294624,35.6270220111843,35.724288015248,35.76692871994,
35.8619813038615,35.956970850126,36.0519184728304,36.1468452432485,36.2418042072995,
36.3367781051034,36.4318327012268,36.4897023126252,36.5869645335255,36.6841680022149,
36.7813262706603,36.8784528497216,36.9755756344637,37.0726900398495,37.1698299658108,
37.2124759053105),.UNSPECIFIED.);
#1338=B_SPLINE_CURVE_WITH_KNOTS('',3,(#23448,#23449,#23450,#23451,#23452,
#23453,#23454,#23455,#23456,#23457,#23458,#23459,#23460,#23461,#23462,#23463,
#23464,#23465,#23466,#23467,#23468,#23469,#23470,#23471,#23472,#23473,#23474,
#23475,#23476,#23477,#23478,#23479,#23480,#23481,#23482,#23483,#23484,#23485,
#23486,#23487,#23488,#23489,#23490,#23491,#23492,#23493,#23494,#23495,#23496,
#23497,#23498,#23499,#23500,#23501,#23502,#23503,#23504,#23505,#23506,#23507,
#23508,#23509,#23510,#23511,#23512,#23513,#23514,#23515,#23516,#23517,#23518,
#23519,#23520),.UNSPECIFIED.,.F.,.F.,(4,3,3,3,3,3,3,3,3,3,3,3,3,3,3,3,3,
3,3,3,3,3,3,3,4),(35.0441551272547,35.1412886454812,35.2384000954,35.3355029983402,
35.4326108677603,35.5297697499161,35.6269517839495,35.7242062225055,35.76692871994,
35.8619992819673,35.9570069448942,36.0519727793798,36.1469178133221,36.2418949897621,
36.336887066271,36.4319596371093,36.4897023126252,36.5869529516101,36.6841447094667,
36.7812911898994,36.8784059553419,36.9755170103548,37.0726197608562,37.1697482536537,
37.2124759053105),.UNSPECIFIED.);
#1339=B_SPLINE_CURVE_WITH_KNOTS('',3,(#23522,#23523,#23524,#23525,#23526,
#23527,#23528,#23529,#23530,#23531,#23532,#23533,#23534,#23535,#23536,#23537,
#23538,#23539,#23540,#23541,#23542,#23543,#23544,#23545,#23546,#23547,#23548,
#23549,#23550,#23551,#23552,#23553,#23554,#23555,#23556,#23557,#23558,#23559,
#23560,#23561,#23562,#23563,#23564,#23565,#23566,#23567,#23568,#23569,#23570,
#23571,#23572,#23573,#23574,#23575,#23576,#23577,#23578,#23579,#23580,#23581,
#23582,#23583,#23584,#23585,#23586,#23587,#23588,#23589,#23590,#23591,#23592,
#23593,#23594),.UNSPECIFIED.,.F.,.F.,(4,3,3,3,3,3,3,3,3,3,3,3,3,3,3,3,3,
3,3,3,3,3,3,3,4),(31.9025624736649,31.9996898883771,32.096795145671,32.193891794287,
32.2909933750212,32.3881459845633,32.4853217678791,32.5825700521498,32.6253360663502,
32.7204163008207,32.8154337110007,32.9104093440756,33.0053642045037,33.1003511798146,
33.1953530369193,33.2904352782913,33.3481096590354,33.4453541351378,33.5425396619171,
33.6396798705364,33.7367883508018,33.8338931655412,33.9309897156823,34.0281121261795,
34.0708832517207),.UNSPECIFIED.);
#1340=B_SPLINE_CURVE_WITH_KNOTS('',3,(#23595,#23596,#23597,#23598,#23599,
#23600,#23601,#23602,#23603,#23604,#23605,#23606,#23607,#23608,#23609,#23610,
#23611,#23612,#23613,#23614,#23615,#23616,#23617,#23618,#23619,#23620,#23621,
#23622,#23623,#23624,#23625,#23626,#23627,#23628,#23629,#23630,#23631,#23632,
#23633,#23634,#23635,#23636,#23637,#23638,#23639,#23640,#23641,#23642,#23643,
#23644,#23645,#23646,#23647,#23648,#23649,#23650,#23651,#23652,#23653,#23654,
#23655,#23656,#23657,#23658,#23659,#23660,#23661,#23662,#23663,#23664,#23665,
#23666,#23667),.UNSPECIFIED.,.F.,.F.,(4,3,3,3,3,3,3,3,3,3,3,3,3,3,3,3,3,
3,3,3,3,3,3,3,4),(31.9025624736649,31.9997005722075,32.0968166692765,32.1939242656021,
32.291036854099,32.3882004430768,32.4853871673618,32.5826462235772,32.6253360663502,
32.7203994206752,32.8153998202737,32.9103583532498,33.0052960649213,33.1002659396212,
33.1952507279387,33.2903160924587,33.3481096590354,33.445364922192,33.5425613555767,
33.6397125422578,33.7368320240988,33.8339477619433,33.9310551653709,34.0281882225514,
34.0708832517207),.UNSPECIFIED.);
#1341=B_SPLINE_CURVE_WITH_KNOTS('',3,(#23669,#23670,#23671,#23672,#23673,
#23674,#23675,#23676,#23677,#23678,#23679,#23680,#23681,#23682,#23683,#23684,
#23685,#23686,#23687,#23688,#23689,#23690,#23691,#23692,#23693,#23694,#23695,
#23696,#23697,#23698,#23699,#23700,#23701,#23702,#23703,#23704,#23705,#23706,
#23707,#23708,#23709,#23710,#23711,#23712,#23713,#23714,#23715,#23716,#23717,
#23718,#23719,#23720,#23721,#23722,#23723,#23724,#23725,#23726,#23727,#23728,
#23729,#23730,#23731,#23732,#23733,#23734,#23735,#23736,#23737,#23738,#23739,
#23740,#23741),.UNSPECIFIED.,.F.,.F.,(4,3,3,3,3,3,3,3,3,3,3,3,3,3,3,3,3,
3,3,3,3,3,3,3,4),(28.7609698200751,28.8581015035,28.9552110918357,29.0523121146564,
29.1494180936432,29.246575090229,29.3437552452973,29.4410078339139,29.4837434127604,
29.5788168740845,29.6738274587129,29.7687962302759,29.8637442096533,29.9587243232585,
30.053719331466,30.148794801035,30.2065170054456,30.3037657918968,30.4009556766901,
30.498100271789,30.5952131478604,30.6923223269791,30.7894232135769,30.886549877952,
30.9292905981309),.UNSPECIFIED.);
#1342=B_SPLINE_CURVE_WITH_KNOTS('',3,(#23742,#23743,#23744,#23745,#23746,
#23747,#23748,#23749,#23750,#23751,#23752,#23753,#23754,#23755,#23756,#23757,
#23758,#23759,#23760,#23761,#23762,#23763,#23764,#23765,#23766,#23767,#23768,
#23769,#23770,#23771,#23772,#23773,#23774,#23775,#23776,#23777,#23778,#23779,
#23780,#23781,#23782,#23783,#23784,#23785,#23786,#23787,#23788,#23789,#23790,
#23791,#23792,#23793,#23794,#23795,#23796,#23797,#23798,#23799,#23800,#23801,
#23802,#23803,#23804,#23805,#23806,#23807,#23808,#23809,#23810,#23811,#23812,
#23813,#23814),.UNSPECIFIED.,.F.,.F.,(4,3,3,3,3,3,3,3,3,3,3,3,3,3,3,3,3,
3,3,3,3,3,3,3,4),(28.7609698200751,28.8580915391914,28.95519101767,29.0522818297916,
29.1493775418228,29.2465242973753,29.3436942469329,29.4409367871068,29.4837434127604,
29.5788327484787,29.6738593304695,29.7688441837639,29.863808290698,29.9588044864641,
30.0538155467294,30.1489068874975,30.2065170054456,30.3037557295149,30.4009354408839,
30.498069796299,30.5951724110685,30.6922714024132,30.7893621664804,30.8864789011626,
30.9292905981309),.UNSPECIFIED.);
#1343=B_SPLINE_CURVE_WITH_KNOTS('',3,(#23816,#23817,#23818,#23819,#23820,
#23821,#23822,#23823,#23824,#23825,#23826,#23827,#23828,#23829,#23830,#23831,
#23832,#23833,#23834,#23835,#23836,#23837,#23838,#23839,#23840,#23841,#23842,
#23843,#23844,#23845,#23846,#23847,#23848,#23849,#23850,#23851,#23852,#23853,
#23854,#23855,#23856,#23857,#23858,#23859,#23860,#23861,#23862,#23863,#23864,
#23865,#23866,#23867,#23868,#23869,#23870,#23871,#23872,#23873,#23874,#23875,
#23876,#23877,#23878,#23879,#23880,#23881,#23882,#23883,#23884,#23885,#23886,
#23887,#23888),.UNSPECIFIED.,.F.,.F.,(4,3,3,3,3,3,3,3,3,3,3,3,3,3,3,3,3,
3,3,3,3,3,3,3,4),(25.6193771664853,25.716493563024,25.813587641087,25.9106729987879,
26.0077632261613,26.1049045105381,26.2020690076394,26.2993061788448,26.3421507591706,
26.4372486713073,26.5322838963633,26.6272774384332,26.7222502589474,26.8172551436848,
26.9122748765366,27.0073747919292,27.0649243518559,27.1621576996185,27.2593319756947,
27.356460860703,27.4535579937485,27.5506515429054,27.6477368997384,27.7448483303182,
27.7876979445411),.UNSPECIFIED.);
#1344=B_SPLINE_CURVE_WITH_KNOTS('',3,(#23889,#23890,#23891,#23892,#23893,
#23894,#23895,#23896,#23897,#23898,#23899,#23900,#23901,#23902,#23903,#23904,
#23905,#23906,#23907,#23908,#23909,#23910,#23911,#23912,#23913,#23914,#23915,
#23916,#23917,#23918,#23919,#23920,#23921,#23922,#23923,#23924,#23925,#23926,
#23927,#23928,#23929,#23930,#23931,#23932,#23933,#23934,#23935,#23936,#23937,
#23938,#23939,#23940,#23941,#23942,#23943,#23944,#23945,#23946,#23947,#23948,
#23949,#23950,#23951,#23952,#23953,#23954,#23955,#23956,#23957,#23958,#23959,
#23960,#23961),.UNSPECIFIED.,.F.,.F.,(4,3,3,3,3,3,3,3,3,3,3,3,3,3,3,3,3,
3,3,3,3,3,3,3,4),(25.6193771664853,25.7165028699044,25.8136063909083,25.9107012859153,
26.0078011033783,26.1049519540998,26.2021259846947,26.2993725432181,26.3421507591706,
26.4372337202794,26.5322538782203,26.6272322735482,26.7221899041007,26.8171796417382,
26.9121842559982,27.0072692234594,27.0649243518558,27.1621670998174,27.2593508793865,
27.3564893294171,27.4535960473819,27.5506991124494,27.6477939241238,27.7449146292726,
27.7876979445411),.UNSPECIFIED.);
#1345=B_SPLINE_CURVE_WITH_KNOTS('',3,(#23963,#23964,#23965,#23966,#23967,
#23968,#23969,#23970,#23971,#23972,#23973,#23974,#23975,#23976,#23977,#23978,
#23979,#23980,#23981,#23982,#23983,#23984,#23985,#23986,#23987,#23988,#23989,
#23990,#23991,#23992,#23993,#23994,#23995,#23996,#23997,#23998,#23999,#24000,
#24001,#24002,#24003,#24004,#24005,#24006,#24007,#24008,#24009,#24010,#24011,
#24012,#24013,#24014,#24015,#24016,#24017,#24018,#24019,#24020,#24021,#24022,
#24023,#24024,#24025,#24026,#24027,#24028,#24029,#24030,#24031,#24032,#24033,
#24034,#24035),.UNSPECIFIED.,.F.,.F.,(4,3,3,3,3,3,3,3,3,3,3,3,3,3,3,3,3,
3,3,3,3,3,3,3,4),(22.4777845128955,22.5749046335756,22.6720024902499,22.7690916643597,
22.866185729313,22.9633308418649,23.060499154063,23.1577400819812,23.2005581055808,
23.2956500094129,23.3906791794585,23.4856666344857,23.5806333505766,23.6756321481368,
23.7706458052989,23.8657397136487,23.9233316982661,24.0205688078678,24.11774688703,
24.2148795996717,24.3119805682513,24.4090779252588,24.5061670654776,24.6032822072728,
24.6461052909513),.UNSPECIFIED.);
#1346=B_SPLINE_CURVE_WITH_KNOTS('',3,(#24036,#24037,#24038,#24039,#24040,
#24041,#24042,#24043,#24044,#24045,#24046,#24047,#24048,#24049,#24050,#24051,
#24052,#24053,#24054,#24055,#24056,#24057,#24058,#24059,#24060,#24061,#24062,
#24063,#24064,#24065,#24066,#24067,#24068,#24069,#24070,#24071,#24072,#24073,
#24074,#24075,#24076,#24077,#24078,#24079,#24080,#24081,#24082,#24083,#24084,
#24085,#24086,#24087,#24088,#24089,#24090,#24091,#24092,#24093,#24094,#24095,
#24096,#24097,#24098,#24099,#24100,#24101,#24102,#24103,#24104,#24105,#24106,
#24107,#24108),.UNSPECIFIED.,.F.,.F.,(4,3,3,3,3,3,3,3,3,3,3,3,3,3,3,3,3,
3,3,3,3,3,3,3,4),(22.4777845128955,22.5748959286778,22.671984953073,22.7690652064669,
22.8661503011054,22.9632864651105,23.0604458591832,23.1576780052064,23.2005581055808,
23.2956641108984,23.390707492164,23.4857092336619,23.5806902770408,23.6757033613676,
23.7707312782682,23.865839285105,23.9233316982661,24.0205600140509,24.1177292031745,
24.2148529685625,24.311944971558,24.4090334278485,24.5061137246012,24.6032201917074,
24.6461052909513),.UNSPECIFIED.);
#1347=B_SPLINE_CURVE_WITH_KNOTS('',3,(#24110,#24111,#24112,#24113,#24114,
#24115,#24116,#24117,#24118,#24119,#24120,#24121,#24122,#24123,#24124,#24125,
#24126,#24127,#24128,#24129,#24130,#24131,#24132,#24133,#24134,#24135,#24136,
#24137,#24138,#24139,#24140,#24141,#24142,#24143,#24144,#24145,#24146,#24147,
#24148,#24149,#24150,#24151,#24152,#24153,#24154,#24155,#24156,#24157,#24158,
#24159,#24160,#24161,#24162,#24163,#24164,#24165,#24166,#24167,#24168,#24169,
#24170,#24171,#24172,#24173,#24174,#24175,#24176,#24177,#24178,#24179,#24180,
#24181,#24182),.UNSPECIFIED.,.F.,.F.,(4,3,3,3,3,3,3,3,3,3,3,3,3,3,3,3,3,
3,3,3,3,3,3,3,4),(19.3361918593058,19.4332986081893,19.5303828972939,19.6274583678477,
19.7245386528814,19.8216700186272,19.9188246305281,20.0160520670602,20.058965451991,
20.1540791046628,20.2491301929626,20.3441396824075,20.4391284959064,20.5341493283117,
20.6291849785355,20.724300631046,20.7817390446763,20.8789626446681,20.9761270666951,
21.0732460345572,21.1703332304066,21.2674169145724,21.3644924699983,21.4615942863967,
21.5045126373615),.UNSPECIFIED.);
#1348=B_SPLINE_CURVE_WITH_KNOTS('',3,(#24183,#24184,#24185,#24186,#24187,
#24188,#24189,#24190,#24191,#24192,#24193,#24194,#24195,#24196,#24197,#24198,
#24199,#24200,#24201,#24202,#24203,#24204,#24205,#24206,#24207,#24208,#24209,
#24210,#24211,#24212,#24213,#24214,#24215,#24216,#24217,#24218,#24219,#24220,
#24221,#24222,#24223,#24224,#24225,#24226,#24227,#24228,#24229,#24230,#24231,
#24232,#24233,#24234,#24235,#24236,#24237,#24238,#24239,#24240,#24241,#24242,
#24243,#24244,#24245,#24246,#24247,#24248,#24249,#24250,#24251,#24252,#24253,
#24254,#24255),.UNSPECIFIED.,.F.,.F.,(4,3,3,3,3,3,3,3,3,3,3,3,3,3,3,3,3,
3,3,3,3,3,3,3,4),(19.3361918593058,19.4333067607529,19.5303993218462,19.6274831473878,
19.7245718340825,19.8217115815184,19.9188745469029,20.016110209788,20.058965451991,
20.1540657863833,20.2491034525452,20.3440994486475,20.4390747302055,20.5340820690261,
20.6291042513177,20.7242065884507,20.7817390446763,20.8789708820714,20.9761436312549,
21.0732709795444,21.1703665727236,21.267458593156,21.3645424310974,21.461652371774,
21.5045126373615),.UNSPECIFIED.);
#1349=B_SPLINE_CURVE_WITH_KNOTS('',3,(#24257,#24258,#24259,#24260,#24261,
#24262,#24263,#24264,#24265,#24266,#24267,#24268,#24269,#24270,#24271,#24272,
#24273,#24274,#24275,#24276,#24277,#24278,#24279,#24280,#24281,#24282,#24283,
#24284,#24285,#24286,#24287,#24288,#24289,#24290,#24291,#24292,#24293,#24294,
#24295,#24296,#24297,#24298,#24299,#24300,#24301,#24302,#24303,#24304,#24305,
#24306,#24307,#24308,#24309,#24310,#24311,#24312,#24313,#24314,#24315,#24316,
#24317,#24318,#24319,#24320,#24321,#24322,#24323,#24324,#24325,#24326,#24327,
#24328,#24329),.UNSPECIFIED.,.F.,.F.,(4,3,3,3,3,3,3,3,3,3,3,3,3,3,3,3,3,
3,3,3,3,3,3,3,4),(16.194599205716,16.2917092212331,16.3887968248508,16.4858756432112,
16.582959294799,16.6800940191828,16.7772519784781,16.8744827115582,16.9173727984012,
17.0124810914989,17.1075267783859,17.2025308377369,17.2975142055994,17.3925296078208,
17.487559838209,17.5826701323273,17.6401463910865,17.7373732920307,17.8345410508988,
17.9316633768824,18.028753937571,18.1258409620435,18.2229198362103,18.3200249079094,
18.3629199837717),.UNSPECIFIED.);
#1350=B_SPLINE_CURVE_WITH_KNOTS('',3,(#24330,#24331,#24332,#24333,#24334,
#24335,#24336,#24337,#24338,#24339,#24340,#24341,#24342,#24343,#24344,#24345,
#24346,#24347,#24348,#24349,#24350,#24351,#24352,#24353,#24354,#24355,#24356,
#24357,#24358,#24359,#24360,#24361,#24362,#24363,#24364,#24365,#24366,#24367,
#24368,#24369,#24370,#24371,#24372,#24373,#24374,#24375,#24376,#24377,#24378,
#24379,#24380,#24381,#24382,#24383,#24384,#24385,#24386,#24387,#24388,#24389,
#24390,#24391,#24392,#24393,#24394,#24395,#24396,#24397,#24398,#24399,#24400,
#24401,#24402),.UNSPECIFIED.,.F.,.F.,(4,3,3,3,3,3,3,3,3,3,3,3,3,3,3,3,3,
3,3,3,3,3,3,3,4),(16.194599205716,16.2917015764267,16.3887814231217,16.4858524065585,
16.582928179243,16.680055043057,16.7772051679657,16.8744281854468,16.9173727984012,
17.0124936863374,17.1075520664769,17.2025688865374,17.2975650516549,17.3925932147811,
17.4876361817024,17.5827590678518,17.6401463910865,17.7373655661754,17.8345255153633,
17.9316399820084,18.0287226677607,18.125801874859,18.2228729821873,18.3199704356026,
18.3629199837717),.UNSPECIFIED.);
#1351=B_SPLINE_CURVE_WITH_KNOTS('',3,(#24404,#24405,#24406,#24407,#24408,
#24409,#24410,#24411,#24412,#24413,#24414,#24415,#24416,#24417,#24418,#24419,
#24420,#24421,#24422,#24423,#24424,#24425,#24426,#24427,#24428,#24429,#24430,
#24431,#24432,#24433,#24434,#24435,#24436,#24437,#24438,#24439,#24440,#24441,
#24442,#24443,#24444,#24445,#24446,#24447,#24448,#24449,#24450,#24451,#24452,
#24453,#24454,#24455,#24456,#24457,#24458,#24459,#24460,#24461,#24462,#24463,
#24464,#24465,#24466,#24467,#24468,#24469,#24470,#24471,#24472,#24473,#24474,
#24475,#24476),.UNSPECIFIED.,.F.,.F.,(4,3,3,3,3,3,3,3,3,3,3,3,3,3,3,3,3,
3,3,3,3,3,3,3,4),(13.0530065521262,13.1501048107483,13.2471804849447,13.3442472537944,
13.4413187880749,13.5384414230539,13.635587333016,13.7328061991352,13.7757801448114,
13.8709078864207,13.9659731739255,14.0609969381436,14.1560000673363,14.2510351747027,
14.3460850725229,14.4412148107737,14.4985537374967,14.5957687557829,14.692924503326,
14.7900347418324,14.8871131912435,14.9841881931923,15.0812551226574,15.1783484782532,
15.2213273301819),.UNSPECIFIED.);
#1352=B_SPLINE_CURVE_WITH_KNOTS('',3,(#24477,#24478,#24479,#24480,#24481,
#24482,#24483,#24484,#24485,#24486,#24487,#24488,#24489,#24490,#24491,#24492,
#24493,#24494,#24495,#24496,#24497,#24498,#24499,#24500,#24501,#24502,#24503,
#24504,#24505,#24506,#24507,#24508,#24509,#24510,#24511,#24512,#24513,#24514,
#24515,#24516,#24517,#24518,#24519,#24520,#24521,#24522,#24523,#24524,#24525,
#24526,#24527,#24528,#24529,#24530,#24531,#24532,#24533,#24534,#24535,#24536,
#24537,#24538,#24539,#24540,#24541,#24542,#24543,#24544,#24545,#24546,#24547,
#24548,#24549),.UNSPECIFIED.,.F.,.F.,(4,3,3,3,3,3,3,3,3,3,3,3,3,3,3,3,3,
3,3,3,3,3,3,3,4),(13.0530065521262,13.1501119879219,13.2471949446812,13.3442690694918,
13.4413480012277,13.538478016824,13.6356312830718,13.7328573943529,13.7757801448114,
13.8708959610436,13.9659492298102,14.06096091131,14.155951923142,14.2509749476356,
14.3460127857609,14.4411306013495,14.4985537374967,14.5957760104763,14.692939091094,
14.790056709018,14.8871425522508,14.9842248936878,15.081299115065,15.178399622931,
15.2213273301819),.UNSPECIFIED.);
#1353=B_SPLINE_CURVE_WITH_KNOTS('',3,(#24552,#24553,#24554,#24555,#24556,
#24557,#24558,#24559,#24560,#24561,#24562,#24563,#24564,#24565,#24566,#24567,
#24568,#24569,#24570,#24571,#24572,#24573,#24574,#24575,#24576,#24577,#24578,
#24579,#24580,#24581,#24582,#24583,#24584,#24585,#24586,#24587,#24588,#24589,
#24590,#24591,#24592,#24593,#24594,#24595,#24596,#24597,#24598,#24599,#24600,
#24601,#24602,#24603,#24604,#24605,#24606,#24607,#24608,#24609),
 .UNSPECIFIED.,.F.,.F.,(4,3,3,3,3,3,3,3,3,3,3,3,3,3,3,3,3,3,3,4),(10.3759343473738,
10.4776920151116,10.5797615894555,10.6818311637994,10.7772132685231,10.8725374348761,
10.9678238901407,11.0630928222215,11.1583925295894,11.2537087060563,11.349094925203,
11.3807829201958,11.4781327140782,11.5754282226452,11.672682517207,11.7744455570533,
11.8716690282138,11.9688871995782,12.0661275540112,12.0797346765921),
 .UNSPECIFIED.);
#1354=B_SPLINE_CURVE_WITH_KNOTS('',3,(#24612,#24613,#24614,#24615,#24616,
#24617),.UNSPECIFIED.,.F.,.F.,(4,2,4),(-0.150154721215487,-0.0750760525081923,
0.),.UNSPECIFIED.);
#1355=B_SPLINE_CURVE_WITH_KNOTS('',3,(#24635,#24636,#24637,#24638),
 .UNSPECIFIED.,.F.,.F.,(4,4),(0.,0.349249092707648),.UNSPECIFIED.);
#1356=B_SPLINE_CURVE_WITH_KNOTS('',3,(#24665,#24666,#24667,#24668,#24669,
#24670,#24671,#24672,#24673,#24674,#24675,#24676,#24677,#24678,#24679,#24680,
#24681,#24682,#24683,#24684,#24685,#24686,#24687,#24688,#24689,#24690,#24691,
#24692,#24693,#24694,#24695,#24696,#24697,#24698,#24699,#24700,#24701,#24702,
#24703,#24704,#24705,#24706,#24707,#24708,#24709,#24710,#24711,#24712,#24713),
 .UNSPECIFIED.,.F.,.F.,(4,3,3,3,3,3,3,3,3,3,3,3,3,3,3,3,4),(0.,0.0365327394137222,
0.0731538029954259,0.109091394005677,0.13300952667614,0.146488998493649,
0.154604853715662,0.189906058994596,0.204763924687531,0.24043732279748,
0.276031768568226,0.295512148258635,0.303306009056309,0.338045252946507,
0.372662891911848,0.40666751045333,0.414264078313279),.UNSPECIFIED.);
#1357=B_SPLINE_CURVE_WITH_KNOTS('',3,(#24714,#24715,#24716,#24717,#24718),
 .UNSPECIFIED.,.F.,.F.,(4,1,4),(39.5699522859152,40.0185665844411,40.2123859659494),
 .UNSPECIFIED.);
#1358=B_SPLINE_CURVE_WITH_KNOTS('',3,(#24743,#24744,#24745,#24746,#24747,
#24748),.UNSPECIFIED.,.F.,.F.,(4,1,1,4),(33.2867669787356,33.7353812772616,
34.4581548699468,34.9067691684727),.UNSPECIFIED.);
#1359=B_SPLINE_CURVE_WITH_KNOTS('',3,(#24773,#24774,#24775,#24776,#24777,
#24778),.UNSPECIFIED.,.F.,.F.,(4,1,1,4),(27.003581671556,27.452195970082,
28.1749695627672,28.6235838612931),.UNSPECIFIED.);
#1360=B_SPLINE_CURVE_WITH_KNOTS('',3,(#24803,#24804,#24805,#24806,#24807,
#24808),.UNSPECIFIED.,.F.,.F.,(4,1,1,4),(20.7203963643765,21.1690106629024,
21.8917842555876,22.3403985541136),.UNSPECIFIED.);
#1361=B_SPLINE_CURVE_WITH_KNOTS('',3,(#24833,#24834,#24835,#24836,#24837,
#24838),.UNSPECIFIED.,.F.,.F.,(4,1,1,4),(14.4372110571969,14.8858253557228,
15.608598948408,16.057213246934),.UNSPECIFIED.);
#1362=B_SPLINE_CURVE_WITH_KNOTS('',3,(#24863,#24864,#24865,#24866,#24867,
#24868),.UNSPECIFIED.,.F.,.F.,(4,1,1,4),(8.15402575001729,8.60264004854321,
9.32541364122847,9.77402793975438),.UNSPECIFIED.);
#1363=B_SPLINE_CURVE_WITH_KNOTS('',3,(#24893,#24894,#24895,#24896,#24897,
#24898,#24899,#24900,#24901,#24902,#24903,#24904,#24905,#24906,#24907,#24908,
#24909,#24910,#24911,#24912,#24913,#24914,#24915,#24916,#24917,#24918,#24919,
#24920,#24921,#24922,#24923,#24924,#24925,#24926,#24927,#24928,#24929,#24930,
#24931,#24932,#24933,#24934,#24935,#24936,#24937,#24938,#24939,#24940,#24941,
#24942,#24943,#24944,#24945,#24946,#24947,#24948,#24949,#24950),
 .UNSPECIFIED.,.F.,.F.,(4,3,3,3,3,3,3,3,3,3,3,3,3,3,3,3,3,3,3,4),(1.87084044283771,
1.96325029725783,2.05566622969097,2.14812754057612,2.24061018839636,2.33315480194847,
2.36709841394138,2.45784756460922,2.54854382431794,2.63920461494343,2.72984732525151,
2.82051706645472,2.91119807753201,3.00194817584722,3.06605017033776,3.1596597536536,
3.2532033890349,3.34670011823176,3.44015197236434,3.49084263257479),
 .UNSPECIFIED.);
#1364=B_SPLINE_CURVE_WITH_KNOTS('',3,(#24976,#24977,#24978,#24979,#24980,
#24981),.UNSPECIFIED.,.F.,.F.,(4,1,1,4),(36.4283596323254,36.8769739308513,
37.5997475235366,38.0483618220625),.UNSPECIFIED.);
#1365=B_SPLINE_CURVE_WITH_KNOTS('',3,(#25006,#25007,#25008,#25009,#25010,
#25011),.UNSPECIFIED.,.F.,.F.,(4,1,1,4),(30.1451743251458,30.5937886236718,
31.316562216357,31.7651765148829),.UNSPECIFIED.);
#1366=B_SPLINE_CURVE_WITH_KNOTS('',3,(#25036,#25037,#25038,#25039,#25040,
#25041),.UNSPECIFIED.,.F.,.F.,(4,1,1,4),(23.8619890179663,24.3106033164922,
25.0333769091774,25.4819912077033),.UNSPECIFIED.);
#1367=B_SPLINE_CURVE_WITH_KNOTS('',3,(#25066,#25067,#25068,#25069,#25070,
#25071),.UNSPECIFIED.,.F.,.F.,(4,1,1,4),(17.5788037107867,18.0274180093126,
18.7501916019978,19.1988059005238),.UNSPECIFIED.);
#1368=B_SPLINE_CURVE_WITH_KNOTS('',3,(#25096,#25097,#25098,#25099,#25100,
#25101),.UNSPECIFIED.,.F.,.F.,(4,1,1,4),(11.2956184036071,11.744232702133,
12.4670062948183,12.9156205933442),.UNSPECIFIED.);
#1369=B_SPLINE_CURVE_WITH_KNOTS('',3,(#25126,#25127,#25128,#25129,#25130,
#25131),.UNSPECIFIED.,.F.,.F.,(4,1,1,4),(5.0124330964275,5.46104739495341,
6.18382098763867,6.63243528616458),.UNSPECIFIED.);
#1370=B_SPLINE_CURVE_WITH_KNOTS('',3,(#25133,#25134,#25135,#25136,#25137,
#25138,#25139,#25140,#25141,#25142,#25143,#25144,#25145,#25146,#25147,#25148,
#25149,#25150,#25151,#25152,#25153,#25154,#25155,#25156,#25157,#25158,#25159,
#25160,#25161,#25162,#25163,#25164,#25165,#25166,#25167,#25168,#25169,#25170,
#25171,#25172,#25173,#25174,#25175),.UNSPECIFIED.,.F.,.F.,(4,3,3,3,3,3,
3,3,3,3,3,3,3,3,4),(0.,0.0319679902674501,0.0642900427206058,0.0886933568687708,
0.117718239582565,0.124682181362639,0.131745609822757,0.164253554230972,
0.197241305800025,0.230517869135345,0.25235595445092,0.259992045647903,
0.264659623072051,0.29882382302699,0.320892418579125),.UNSPECIFIED.);
#1371=B_SPLINE_CURVE_WITH_KNOTS('',3,(#25180,#25181,#25182,#25183,#25184,
#25185),.UNSPECIFIED.,.F.,.F.,(4,1,1,4),(-3.33195380826789,-2.88333950974197,
-2.16056591705671,-2.06120159751576),.UNSPECIFIED.);
#1372=B_SPLINE_CURVE_WITH_KNOTS('',3,(#25188,#25189,#25190,#25191,#25192,
#25193,#25194,#25195,#25196,#25197,#25198,#25199,#25200,#25201,#25202,#25203,
#25204,#25205,#25206,#25207,#25208,#25209,#25210,#25211,#25212,#25213,#25214,
#25215,#25216,#25217,#25218,#25219,#25220,#25221,#25222,#25223,#25224,#25225,
#25226,#25227,#25228,#25229,#25230,#25231,#25232,#25233,#25234,#25235,#25236,
#25237,#25238,#25239,#25240,#25241,#25242,#25243,#25244,#25245),
 .UNSPECIFIED.,.F.,.F.,(4,3,3,3,3,3,3,3,3,3,3,3,3,3,3,3,3,3,3,4),(-41.0310632895362,
-40.9388473190672,-40.8466422252189,-40.754407737536,-40.6621654402305,
-40.5698612720643,-40.4813266946942,-40.3903969656387,-40.2995162802569,
-40.2086677147606,-40.1178343757824,-40.0269750194882,-39.9361025632024,
-39.8451701195949,-39.8091154310716,-39.7151490717192,-39.6212411951498,
-39.5273766833117,-39.4335563138008,-39.4110634616083),.UNSPECIFIED.);
#1373=B_SPLINE_CURVE_WITH_KNOTS('',3,(#25247,#25248,#25249,#25250,#25251,
#25252),.UNSPECIFIED.,.F.,.F.,(4,1,1,4),(-37.8894729977556,-37.4408586992297,
-36.7180851065444,-36.2694708080185),.UNSPECIFIED.);
#1374=B_SPLINE_CURVE_WITH_KNOTS('',3,(#25254,#25255,#25256,#25257,#25258,
#25259),.UNSPECIFIED.,.F.,.F.,(4,1,1,4),(-34.7478803441658,-34.2992660456399,
-33.5764924529546,-33.1278781544287),.UNSPECIFIED.);
#1375=B_SPLINE_CURVE_WITH_KNOTS('',3,(#25261,#25262,#25263,#25264,#25265,
#25266),.UNSPECIFIED.,.F.,.F.,(4,1,1,4),(-31.606287690576,-31.1576733920501,
-30.4348997993648,-29.9862855008389),.UNSPECIFIED.);
#1376=B_SPLINE_CURVE_WITH_KNOTS('',3,(#25268,#25269,#25270,#25271,#25272,
#25273),.UNSPECIFIED.,.F.,.F.,(4,1,1,4),(-28.4646950369862,-28.0160807384603,
-27.2933071457751,-26.8446928472491),.UNSPECIFIED.);
#1377=B_SPLINE_CURVE_WITH_KNOTS('',3,(#25275,#25276,#25277,#25278,#25279,
#25280),.UNSPECIFIED.,.F.,.F.,(4,1,1,4),(-25.3231023833964,-24.8744880848705,
-24.1517144921853,-23.7031001936593),.UNSPECIFIED.);
#1378=B_SPLINE_CURVE_WITH_KNOTS('',3,(#25282,#25283,#25284,#25285,#25286,
#25287),.UNSPECIFIED.,.F.,.F.,(4,1,1,4),(-22.1815097298066,-21.7328954312807,
-21.0101218385955,-20.5615075400696),.UNSPECIFIED.);
#1379=B_SPLINE_CURVE_WITH_KNOTS('',3,(#25289,#25290,#25291,#25292,#25293,
#25294),.UNSPECIFIED.,.F.,.F.,(4,1,1,4),(-19.0399170762168,-18.5913027776909,
-17.8685291850057,-17.4199148864798),.UNSPECIFIED.);
#1380=B_SPLINE_CURVE_WITH_KNOTS('',3,(#25296,#25297,#25298,#25299,#25300,
#25301),.UNSPECIFIED.,.F.,.F.,(4,1,1,4),(-15.8983244226271,-15.4497101241011,
-14.7269365314159,-14.27832223289),.UNSPECIFIED.);
#1381=B_SPLINE_CURVE_WITH_KNOTS('',3,(#25303,#25304,#25305,#25306,#25307,
#25308),.UNSPECIFIED.,.F.,.F.,(4,1,1,4),(-12.7567317690373,-12.3081174705113,
-11.5853438778261,-11.1367295793002),.UNSPECIFIED.);
#1382=B_SPLINE_CURVE_WITH_KNOTS('',3,(#25310,#25311,#25312,#25313,#25314,
#25315),.UNSPECIFIED.,.F.,.F.,(4,1,1,4),(-9.61513911544747,-9.16652481692155,
-8.4437512242363,-7.99513692571038),.UNSPECIFIED.);
#1383=B_SPLINE_CURVE_WITH_KNOTS('',3,(#25317,#25318,#25319,#25320,#25321,
#25322),.UNSPECIFIED.,.F.,.F.,(4,1,1,4),(-6.47354646185768,-6.02493216333176,
-5.3021585706465,-4.85354427212059),.UNSPECIFIED.);
#1614=VERTEX_POINT('',#22155);
#1615=VERTEX_POINT('',#22156);
#1616=VERTEX_POINT('',#22165);
#1617=VERTEX_POINT('',#22167);
#1618=VERTEX_POINT('',#22174);
#1619=VERTEX_POINT('',#22176);
#1620=VERTEX_POINT('',#22185);
#1621=VERTEX_POINT('',#22187);
#1622=VERTEX_POINT('',#22196);
#1623=VERTEX_POINT('',#22198);
#1624=VERTEX_POINT('',#22207);
#1625=VERTEX_POINT('',#22209);
#1626=VERTEX_POINT('',#22218);
#1627=VERTEX_POINT('',#22220);
#1628=VERTEX_POINT('',#22229);
#1629=VERTEX_POINT('',#22231);
#1630=VERTEX_POINT('',#22240);
#1631=VERTEX_POINT('',#22242);
#1632=VERTEX_POINT('',#22251);
#1633=VERTEX_POINT('',#22253);
#1634=VERTEX_POINT('',#22262);
#1635=VERTEX_POINT('',#22264);
#1636=VERTEX_POINT('',#22273);
#1637=VERTEX_POINT('',#22275);
#1638=VERTEX_POINT('',#22284);
#1639=VERTEX_POINT('',#22286);
#1640=VERTEX_POINT('',#22295);
#1641=VERTEX_POINT('',#22297);
#1642=VERTEX_POINT('',#22306);
#1643=VERTEX_POINT('',#22308);
#1644=VERTEX_POINT('',#22310);
#1645=VERTEX_POINT('',#22317);
#1646=VERTEX_POINT('',#22319);
#1647=VERTEX_POINT('',#22328);
#1648=VERTEX_POINT('',#22330);
#1649=VERTEX_POINT('',#22339);
#1650=VERTEX_POINT('',#22341);
#1651=VERTEX_POINT('',#22350);
#1652=VERTEX_POINT('',#22352);
#1653=VERTEX_POINT('',#22361);
#1654=VERTEX_POINT('',#22363);
#1655=VERTEX_POINT('',#22372);
#1656=VERTEX_POINT('',#22374);
#1657=VERTEX_POINT('',#22383);
#1658=VERTEX_POINT('',#22385);
#1659=VERTEX_POINT('',#22394);
#1660=VERTEX_POINT('',#22396);
#1661=VERTEX_POINT('',#22405);
#1662=VERTEX_POINT('',#22407);
#1663=VERTEX_POINT('',#22416);
#1664=VERTEX_POINT('',#22418);
#1665=VERTEX_POINT('',#22427);
#1666=VERTEX_POINT('',#22429);
#1667=VERTEX_POINT('',#22438);
#1668=VERTEX_POINT('',#22440);
#1669=VERTEX_POINT('',#22451);
#1670=VERTEX_POINT('',#22452);
#1671=VERTEX_POINT('',#22459);
#1672=VERTEX_POINT('',#22461);
#1673=VERTEX_POINT('',#22470);
#1674=VERTEX_POINT('',#22472);
#1675=VERTEX_POINT('',#22481);
#1676=VERTEX_POINT('',#22483);
#1677=VERTEX_POINT('',#22492);
#1678=VERTEX_POINT('',#22494);
#1679=VERTEX_POINT('',#22503);
#1680=VERTEX_POINT('',#22505);
#1681=VERTEX_POINT('',#22514);
#1682=VERTEX_POINT('',#22516);
#1683=VERTEX_POINT('',#22525);
#1684=VERTEX_POINT('',#22527);
#1685=VERTEX_POINT('',#22536);
#1686=VERTEX_POINT('',#22538);
#1687=VERTEX_POINT('',#22547);
#1688=VERTEX_POINT('',#22549);
#1689=VERTEX_POINT('',#22558);
#1690=VERTEX_POINT('',#22560);
#1691=VERTEX_POINT('',#22569);
#1692=VERTEX_POINT('',#22571);
#1693=VERTEX_POINT('',#22580);
#1694=VERTEX_POINT('',#22582);
#1695=VERTEX_POINT('',#22591);
#1696=VERTEX_POINT('',#22593);
#1697=VERTEX_POINT('',#22595);
#1698=VERTEX_POINT('',#22602);
#1699=VERTEX_POINT('',#22604);
#1700=VERTEX_POINT('',#22613);
#1701=VERTEX_POINT('',#22615);
#1702=VERTEX_POINT('',#22624);
#1703=VERTEX_POINT('',#22626);
#1704=VERTEX_POINT('',#22635);
#1705=VERTEX_POINT('',#22637);
#1706=VERTEX_POINT('',#22646);
#1707=VERTEX_POINT('',#22648);
#1708=VERTEX_POINT('',#22657);
#1709=VERTEX_POINT('',#22659);
#1710=VERTEX_POINT('',#22668);
#1711=VERTEX_POINT('',#22670);
#1712=VERTEX_POINT('',#22679);
#1713=VERTEX_POINT('',#22681);
#1714=VERTEX_POINT('',#22690);
#1715=VERTEX_POINT('',#22692);
#1716=VERTEX_POINT('',#22701);
#1717=VERTEX_POINT('',#22703);
#1718=VERTEX_POINT('',#22712);
#1719=VERTEX_POINT('',#22714);
#1720=VERTEX_POINT('',#22723);
#1721=VERTEX_POINT('',#22725);
#1722=VERTEX_POINT('',#22734);
#1723=VERTEX_POINT('',#22736);
#1724=VERTEX_POINT('',#22747);
#1725=VERTEX_POINT('',#24551);
#1726=VERTEX_POINT('',#24610);
#1727=VERTEX_POINT('',#24634);
#1728=VERTEX_POINT('',#24664);
#1729=VERTEX_POINT('',#25179);
#1730=VERTEX_POINT('',#25654);
#1731=VERTEX_POINT('',#25656);
#2077=EDGE_CURVE('',#1614,#1615,#1274,.T.);
#2078=EDGE_CURVE('',#1614,#1616,#894,.T.);
#2079=EDGE_CURVE('',#1617,#1616,#1275,.T.);
#2080=EDGE_CURVE('',#1618,#1617,#895,.T.);
#2081=EDGE_CURVE('',#1619,#1618,#1276,.T.);
#2082=EDGE_CURVE('',#1620,#1619,#896,.T.);
#2083=EDGE_CURVE('',#1621,#1620,#1277,.T.);
#2084=EDGE_CURVE('',#1622,#1621,#897,.T.);
#2085=EDGE_CURVE('',#1623,#1622,#1278,.T.);
#2086=EDGE_CURVE('',#1624,#1623,#898,.T.);
#2087=EDGE_CURVE('',#1625,#1624,#1279,.T.);
#2088=EDGE_CURVE('',#1626,#1625,#899,.T.);
#2089=EDGE_CURVE('',#1627,#1626,#1280,.T.);
#2090=EDGE_CURVE('',#1628,#1627,#900,.T.);
#2091=EDGE_CURVE('',#1629,#1628,#1281,.T.);
#2092=EDGE_CURVE('',#1630,#1629,#901,.T.);
#2093=EDGE_CURVE('',#1631,#1630,#1282,.T.);
#2094=EDGE_CURVE('',#1632,#1631,#902,.T.);
#2095=EDGE_CURVE('',#1633,#1632,#1283,.T.);
#2096=EDGE_CURVE('',#1634,#1633,#903,.T.);
#2097=EDGE_CURVE('',#1635,#1634,#1284,.T.);
#2098=EDGE_CURVE('',#1636,#1635,#904,.T.);
#2099=EDGE_CURVE('',#1637,#1636,#1285,.T.);
#2100=EDGE_CURVE('',#1638,#1637,#905,.T.);
#2101=EDGE_CURVE('',#1639,#1638,#1286,.T.);
#2102=EDGE_CURVE('',#1640,#1639,#906,.T.);
#2103=EDGE_CURVE('',#1641,#1640,#1287,.T.);
#2104=EDGE_CURVE('',#1642,#1641,#907,.T.);
#2105=EDGE_CURVE('',#1643,#1642,#908,.T.);
#2106=EDGE_CURVE('',#1644,#1643,#1288,.T.);
#2107=EDGE_CURVE('',#1645,#1644,#909,.T.);
#2108=EDGE_CURVE('',#1646,#1645,#1289,.T.);
#2109=EDGE_CURVE('',#1647,#1646,#910,.T.);
#2110=EDGE_CURVE('',#1648,#1647,#1290,.T.);
#2111=EDGE_CURVE('',#1649,#1648,#911,.T.);
#2112=EDGE_CURVE('',#1650,#1649,#1291,.T.);
#2113=EDGE_CURVE('',#1651,#1650,#912,.T.);
#2114=EDGE_CURVE('',#1652,#1651,#1292,.T.);
#2115=EDGE_CURVE('',#1653,#1652,#913,.T.);
#2116=EDGE_CURVE('',#1654,#1653,#1293,.T.);
#2117=EDGE_CURVE('',#1655,#1654,#914,.T.);
#2118=EDGE_CURVE('',#1656,#1655,#1294,.T.);
#2119=EDGE_CURVE('',#1657,#1656,#915,.T.);
#2120=EDGE_CURVE('',#1658,#1657,#1295,.T.);
#2121=EDGE_CURVE('',#1659,#1658,#916,.T.);
#2122=EDGE_CURVE('',#1660,#1659,#1296,.T.);
#2123=EDGE_CURVE('',#1661,#1660,#917,.T.);
#2124=EDGE_CURVE('',#1662,#1661,#1297,.T.);
#2125=EDGE_CURVE('',#1663,#1662,#918,.T.);
#2126=EDGE_CURVE('',#1664,#1663,#1298,.T.);
#2127=EDGE_CURVE('',#1665,#1664,#919,.T.);
#2128=EDGE_CURVE('',#1666,#1665,#1299,.T.);
#2129=EDGE_CURVE('',#1667,#1666,#920,.T.);
#2130=EDGE_CURVE('',#1668,#1667,#1300,.T.);
#2131=EDGE_CURVE('',#1615,#1668,#921,.T.);
#2132=EDGE_CURVE('',#1669,#1670,#1301,.T.);
#2133=EDGE_CURVE('',#1671,#1669,#922,.T.);
#2134=EDGE_CURVE('',#1672,#1671,#1302,.T.);
#2135=EDGE_CURVE('',#1673,#1672,#923,.T.);
#2136=EDGE_CURVE('',#1674,#1673,#1303,.T.);
#2137=EDGE_CURVE('',#1675,#1674,#924,.T.);
#2138=EDGE_CURVE('',#1676,#1675,#1304,.T.);
#2139=EDGE_CURVE('',#1677,#1676,#925,.T.);
#2140=EDGE_CURVE('',#1678,#1677,#1305,.T.);
#2141=EDGE_CURVE('',#1679,#1678,#926,.T.);
#2142=EDGE_CURVE('',#1680,#1679,#1306,.T.);
#2143=EDGE_CURVE('',#1681,#1680,#927,.T.);
#2144=EDGE_CURVE('',#1682,#1681,#1307,.T.);
#2145=EDGE_CURVE('',#1683,#1682,#928,.T.);
#2146=EDGE_CURVE('',#1684,#1683,#1308,.T.);
#2147=EDGE_CURVE('',#1685,#1684,#929,.T.);
#2148=EDGE_CURVE('',#1686,#1685,#1309,.T.);
#2149=EDGE_CURVE('',#1687,#1686,#930,.T.);
#2150=EDGE_CURVE('',#1688,#1687,#1310,.T.);
#2151=EDGE_CURVE('',#1689,#1688,#931,.T.);
#2152=EDGE_CURVE('',#1690,#1689,#1311,.T.);
#2153=EDGE_CURVE('',#1691,#1690,#932,.T.);
#2154=EDGE_CURVE('',#1692,#1691,#1312,.T.);
#2155=EDGE_CURVE('',#1693,#1692,#933,.T.);
#2156=EDGE_CURVE('',#1694,#1693,#1313,.T.);
#2157=EDGE_CURVE('',#1695,#1694,#934,.T.);
#2158=EDGE_CURVE('',#1696,#1695,#935,.T.);
#2159=EDGE_CURVE('',#1697,#1696,#1314,.T.);
#2160=EDGE_CURVE('',#1698,#1697,#936,.T.);
#2161=EDGE_CURVE('',#1699,#1698,#1315,.T.);
#2162=EDGE_CURVE('',#1700,#1699,#937,.T.);
#2163=EDGE_CURVE('',#1701,#1700,#1316,.T.);
#2164=EDGE_CURVE('',#1702,#1701,#938,.T.);
#2165=EDGE_CURVE('',#1703,#1702,#1317,.T.);
#2166=EDGE_CURVE('',#1704,#1703,#939,.T.);
#2167=EDGE_CURVE('',#1705,#1704,#1318,.T.);
#2168=EDGE_CURVE('',#1706,#1705,#940,.T.);
#2169=EDGE_CURVE('',#1707,#1706,#1319,.T.);
#2170=EDGE_CURVE('',#1708,#1707,#941,.T.);
#2171=EDGE_CURVE('',#1709,#1708,#1320,.T.);
#2172=EDGE_CURVE('',#1710,#1709,#942,.T.);
#2173=EDGE_CURVE('',#1711,#1710,#1321,.T.);
#2174=EDGE_CURVE('',#1712,#1711,#943,.T.);
#2175=EDGE_CURVE('',#1713,#1712,#1322,.T.);
#2176=EDGE_CURVE('',#1714,#1713,#944,.T.);
#2177=EDGE_CURVE('',#1715,#1714,#1323,.T.);
#2178=EDGE_CURVE('',#1716,#1715,#945,.T.);
#2179=EDGE_CURVE('',#1717,#1716,#1324,.T.);
#2180=EDGE_CURVE('',#1718,#1717,#946,.T.);
#2181=EDGE_CURVE('',#1719,#1718,#1325,.T.);
#2182=EDGE_CURVE('',#1720,#1719,#947,.T.);
#2183=EDGE_CURVE('',#1721,#1720,#1326,.T.);
#2184=EDGE_CURVE('',#1722,#1721,#948,.T.);
#2185=EDGE_CURVE('',#1723,#1722,#1327,.T.);
#2186=EDGE_CURVE('',#1723,#1670,#949,.T.);
#2187=EDGE_CURVE('',#1641,#1724,#1328,.T.);
#2188=EDGE_CURVE('',#1642,#1724,#355,.T.);
#2189=EDGE_CURVE('',#1693,#1644,#1329,.T.);
#2190=EDGE_CURVE('',#1692,#1645,#1330,.T.);
#2191=EDGE_CURVE('',#1637,#1700,#1331,.T.);
#2192=EDGE_CURVE('',#1638,#1699,#1332,.T.);
#2193=EDGE_CURVE('',#1689,#1648,#1333,.T.);
#2194=EDGE_CURVE('',#1688,#1649,#1334,.T.);
#2195=EDGE_CURVE('',#1633,#1704,#1335,.T.);
#2196=EDGE_CURVE('',#1634,#1703,#1336,.T.);
#2197=EDGE_CURVE('',#1685,#1652,#1337,.T.);
#2198=EDGE_CURVE('',#1684,#1653,#1338,.T.);
#2199=EDGE_CURVE('',#1629,#1708,#1339,.T.);
#2200=EDGE_CURVE('',#1630,#1707,#1340,.T.);
#2201=EDGE_CURVE('',#1681,#1656,#1341,.T.);
#2202=EDGE_CURVE('',#1680,#1657,#1342,.T.);
#2203=EDGE_CURVE('',#1625,#1712,#1343,.T.);
#2204=EDGE_CURVE('',#1626,#1711,#1344,.T.);
#2205=EDGE_CURVE('',#1677,#1660,#1345,.T.);
#2206=EDGE_CURVE('',#1676,#1661,#1346,.T.);
#2207=EDGE_CURVE('',#1621,#1716,#1347,.T.);
#2208=EDGE_CURVE('',#1622,#1715,#1348,.T.);
#2209=EDGE_CURVE('',#1673,#1664,#1349,.T.);
#2210=EDGE_CURVE('',#1672,#1665,#1350,.T.);
#2211=EDGE_CURVE('',#1617,#1720,#1351,.T.);
#2212=EDGE_CURVE('',#1618,#1719,#1352,.T.);
#2213=EDGE_CURVE('',#1725,#1668,#1353,.T.);
#2214=EDGE_CURVE('',#1726,#1725,#356,.T.);
#2215=EDGE_CURVE('',#1726,#1615,#1354,.T.);
#2216=EDGE_CURVE('',#1727,#1722,#1355,.T.);
#2217=EDGE_CURVE('',#1723,#1727,#54,.T.);
#2218=EDGE_CURVE('',#1728,#1643,#1356,.T.);
#2219=EDGE_CURVE('',#1694,#1728,#1357,.T.);
#2220=EDGE_CURVE('',#1690,#1647,#1358,.T.);
#2221=EDGE_CURVE('',#1686,#1651,#1359,.T.);
#2222=EDGE_CURVE('',#1682,#1655,#1360,.T.);
#2223=EDGE_CURVE('',#1678,#1659,#1361,.T.);
#2224=EDGE_CURVE('',#1674,#1663,#1362,.T.);
#2225=EDGE_CURVE('',#1669,#1667,#1363,.T.);
#2226=EDGE_CURVE('',#1725,#1670,#55,.T.);
#2227=EDGE_CURVE('',#1639,#1698,#1364,.T.);
#2228=EDGE_CURVE('',#1635,#1702,#1365,.T.);
#2229=EDGE_CURVE('',#1631,#1706,#1366,.T.);
#2230=EDGE_CURVE('',#1627,#1710,#1367,.T.);
#2231=EDGE_CURVE('',#1623,#1714,#1368,.T.);
#2232=EDGE_CURVE('',#1619,#1718,#1369,.T.);
#2233=EDGE_CURVE('',#1724,#1696,#1370,.T.);
#2234=EDGE_CURVE('',#1695,#1728,#357,.F.);
#2235=EDGE_CURVE('',#1721,#1729,#1371,.T.);
#2236=EDGE_CURVE('',#1727,#1729,#358,.T.);
#2237=EDGE_CURVE('',#1697,#1640,#1372,.T.);
#2238=EDGE_CURVE('',#1646,#1691,#1373,.T.);
#2239=EDGE_CURVE('',#1701,#1636,#1374,.T.);
#2240=EDGE_CURVE('',#1650,#1687,#1375,.T.);
#2241=EDGE_CURVE('',#1705,#1632,#1376,.T.);
#2242=EDGE_CURVE('',#1654,#1683,#1377,.T.);
#2243=EDGE_CURVE('',#1709,#1628,#1378,.T.);
#2244=EDGE_CURVE('',#1658,#1679,#1379,.T.);
#2245=EDGE_CURVE('',#1713,#1624,#1380,.T.);
#2246=EDGE_CURVE('',#1662,#1675,#1381,.T.);
#2247=EDGE_CURVE('',#1717,#1620,#1382,.T.);
#2248=EDGE_CURVE('',#1666,#1671,#1383,.T.);
#2249=EDGE_CURVE('',#1729,#1616,#56,.T.);
#2250=EDGE_CURVE('',#1614,#1726,#57,.T.);
#2251=EDGE_CURVE('',#1730,#1730,#359,.T.);
#2252=EDGE_CURVE('',#1730,#1731,#950,.T.);
#2253=EDGE_CURVE('',#1731,#1731,#360,.T.);
#2928=ORIENTED_EDGE('',*,*,#2077,.F.);
#2929=ORIENTED_EDGE('',*,*,#2078,.T.);
#2930=ORIENTED_EDGE('',*,*,#2079,.F.);
#2931=ORIENTED_EDGE('',*,*,#2080,.F.);
#2932=ORIENTED_EDGE('',*,*,#2081,.F.);
#2933=ORIENTED_EDGE('',*,*,#2082,.F.);
#2934=ORIENTED_EDGE('',*,*,#2083,.F.);
#2935=ORIENTED_EDGE('',*,*,#2084,.F.);
#2936=ORIENTED_EDGE('',*,*,#2085,.F.);
#2937=ORIENTED_EDGE('',*,*,#2086,.F.);
#2938=ORIENTED_EDGE('',*,*,#2087,.F.);
#2939=ORIENTED_EDGE('',*,*,#2088,.F.);
#2940=ORIENTED_EDGE('',*,*,#2089,.F.);
#2941=ORIENTED_EDGE('',*,*,#2090,.F.);
#2942=ORIENTED_EDGE('',*,*,#2091,.F.);
#2943=ORIENTED_EDGE('',*,*,#2092,.F.);
#2944=ORIENTED_EDGE('',*,*,#2093,.F.);
#2945=ORIENTED_EDGE('',*,*,#2094,.F.);
#2946=ORIENTED_EDGE('',*,*,#2095,.F.);
#2947=ORIENTED_EDGE('',*,*,#2096,.F.);
#2948=ORIENTED_EDGE('',*,*,#2097,.F.);
#2949=ORIENTED_EDGE('',*,*,#2098,.F.);
#2950=ORIENTED_EDGE('',*,*,#2099,.F.);
#2951=ORIENTED_EDGE('',*,*,#2100,.F.);
#2952=ORIENTED_EDGE('',*,*,#2101,.F.);
#2953=ORIENTED_EDGE('',*,*,#2102,.F.);
#2954=ORIENTED_EDGE('',*,*,#2103,.F.);
#2955=ORIENTED_EDGE('',*,*,#2104,.F.);
#2956=ORIENTED_EDGE('',*,*,#2105,.F.);
#2957=ORIENTED_EDGE('',*,*,#2106,.F.);
#2958=ORIENTED_EDGE('',*,*,#2107,.F.);
#2959=ORIENTED_EDGE('',*,*,#2108,.F.);
#2960=ORIENTED_EDGE('',*,*,#2109,.F.);
#2961=ORIENTED_EDGE('',*,*,#2110,.F.);
#2962=ORIENTED_EDGE('',*,*,#2111,.F.);
#2963=ORIENTED_EDGE('',*,*,#2112,.F.);
#2964=ORIENTED_EDGE('',*,*,#2113,.F.);
#2965=ORIENTED_EDGE('',*,*,#2114,.F.);
#2966=ORIENTED_EDGE('',*,*,#2115,.F.);
#2967=ORIENTED_EDGE('',*,*,#2116,.F.);
#2968=ORIENTED_EDGE('',*,*,#2117,.F.);
#2969=ORIENTED_EDGE('',*,*,#2118,.F.);
#2970=ORIENTED_EDGE('',*,*,#2119,.F.);
#2971=ORIENTED_EDGE('',*,*,#2120,.F.);
#2972=ORIENTED_EDGE('',*,*,#2121,.F.);
#2973=ORIENTED_EDGE('',*,*,#2122,.F.);
#2974=ORIENTED_EDGE('',*,*,#2123,.F.);
#2975=ORIENTED_EDGE('',*,*,#2124,.F.);
#2976=ORIENTED_EDGE('',*,*,#2125,.F.);
#2977=ORIENTED_EDGE('',*,*,#2126,.F.);
#2978=ORIENTED_EDGE('',*,*,#2127,.F.);
#2979=ORIENTED_EDGE('',*,*,#2128,.F.);
#2980=ORIENTED_EDGE('',*,*,#2129,.F.);
#2981=ORIENTED_EDGE('',*,*,#2130,.F.);
#2982=ORIENTED_EDGE('',*,*,#2131,.F.);
#2983=ORIENTED_EDGE('',*,*,#2132,.F.);
#2984=ORIENTED_EDGE('',*,*,#2133,.F.);
#2985=ORIENTED_EDGE('',*,*,#2134,.F.);
#2986=ORIENTED_EDGE('',*,*,#2135,.F.);
#2987=ORIENTED_EDGE('',*,*,#2136,.F.);
#2988=ORIENTED_EDGE('',*,*,#2137,.F.);
#2989=ORIENTED_EDGE('',*,*,#2138,.F.);
#2990=ORIENTED_EDGE('',*,*,#2139,.F.);
#2991=ORIENTED_EDGE('',*,*,#2140,.F.);
#2992=ORIENTED_EDGE('',*,*,#2141,.F.);
#2993=ORIENTED_EDGE('',*,*,#2142,.F.);
#2994=ORIENTED_EDGE('',*,*,#2143,.F.);
#2995=ORIENTED_EDGE('',*,*,#2144,.F.);
#2996=ORIENTED_EDGE('',*,*,#2145,.F.);
#2997=ORIENTED_EDGE('',*,*,#2146,.F.);
#2998=ORIENTED_EDGE('',*,*,#2147,.F.);
#2999=ORIENTED_EDGE('',*,*,#2148,.F.);
#3000=ORIENTED_EDGE('',*,*,#2149,.F.);
#3001=ORIENTED_EDGE('',*,*,#2150,.F.);
#3002=ORIENTED_EDGE('',*,*,#2151,.F.);
#3003=ORIENTED_EDGE('',*,*,#2152,.F.);
#3004=ORIENTED_EDGE('',*,*,#2153,.F.);
#3005=ORIENTED_EDGE('',*,*,#2154,.F.);
#3006=ORIENTED_EDGE('',*,*,#2155,.F.);
#3007=ORIENTED_EDGE('',*,*,#2156,.F.);
#3008=ORIENTED_EDGE('',*,*,#2157,.F.);
#3009=ORIENTED_EDGE('',*,*,#2158,.F.);
#3010=ORIENTED_EDGE('',*,*,#2159,.F.);
#3011=ORIENTED_EDGE('',*,*,#2160,.F.);
#3012=ORIENTED_EDGE('',*,*,#2161,.F.);
#3013=ORIENTED_EDGE('',*,*,#2162,.F.);
#3014=ORIENTED_EDGE('',*,*,#2163,.F.);
#3015=ORIENTED_EDGE('',*,*,#2164,.F.);
#3016=ORIENTED_EDGE('',*,*,#2165,.F.);
#3017=ORIENTED_EDGE('',*,*,#2166,.F.);
#3018=ORIENTED_EDGE('',*,*,#2167,.F.);
#3019=ORIENTED_EDGE('',*,*,#2168,.F.);
#3020=ORIENTED_EDGE('',*,*,#2169,.F.);
#3021=ORIENTED_EDGE('',*,*,#2170,.F.);
#3022=ORIENTED_EDGE('',*,*,#2171,.F.);
#3023=ORIENTED_EDGE('',*,*,#2172,.F.);
#3024=ORIENTED_EDGE('',*,*,#2173,.F.);
#3025=ORIENTED_EDGE('',*,*,#2174,.F.);
#3026=ORIENTED_EDGE('',*,*,#2175,.F.);
#3027=ORIENTED_EDGE('',*,*,#2176,.F.);
#3028=ORIENTED_EDGE('',*,*,#2177,.F.);
#3029=ORIENTED_EDGE('',*,*,#2178,.F.);
#3030=ORIENTED_EDGE('',*,*,#2179,.F.);
#3031=ORIENTED_EDGE('',*,*,#2180,.F.);
#3032=ORIENTED_EDGE('',*,*,#2181,.F.);
#3033=ORIENTED_EDGE('',*,*,#2182,.F.);
#3034=ORIENTED_EDGE('',*,*,#2183,.F.);
#3035=ORIENTED_EDGE('',*,*,#2184,.F.);
#3036=ORIENTED_EDGE('',*,*,#2185,.F.);
#3037=ORIENTED_EDGE('',*,*,#2186,.T.);
#3038=ORIENTED_EDGE('',*,*,#2104,.T.);
#3039=ORIENTED_EDGE('',*,*,#2187,.T.);
#3040=ORIENTED_EDGE('',*,*,#2188,.F.);
#3041=ORIENTED_EDGE('',*,*,#2107,.T.);
#3042=ORIENTED_EDGE('',*,*,#2189,.F.);
#3043=ORIENTED_EDGE('',*,*,#2155,.T.);
#3044=ORIENTED_EDGE('',*,*,#2190,.T.);
#3045=ORIENTED_EDGE('',*,*,#2100,.T.);
#3046=ORIENTED_EDGE('',*,*,#2191,.T.);
#3047=ORIENTED_EDGE('',*,*,#2162,.T.);
#3048=ORIENTED_EDGE('',*,*,#2192,.F.);
#3049=ORIENTED_EDGE('',*,*,#2111,.T.);
#3050=ORIENTED_EDGE('',*,*,#2193,.F.);
#3051=ORIENTED_EDGE('',*,*,#2151,.T.);
#3052=ORIENTED_EDGE('',*,*,#2194,.T.);
#3053=ORIENTED_EDGE('',*,*,#2096,.T.);
#3054=ORIENTED_EDGE('',*,*,#2195,.T.);
#3055=ORIENTED_EDGE('',*,*,#2166,.T.);
#3056=ORIENTED_EDGE('',*,*,#2196,.F.);
#3057=ORIENTED_EDGE('',*,*,#2115,.T.);
#3058=ORIENTED_EDGE('',*,*,#2197,.F.);
#3059=ORIENTED_EDGE('',*,*,#2147,.T.);
#3060=ORIENTED_EDGE('',*,*,#2198,.T.);
#3061=ORIENTED_EDGE('',*,*,#2092,.T.);
#3062=ORIENTED_EDGE('',*,*,#2199,.T.);
#3063=ORIENTED_EDGE('',*,*,#2170,.T.);
#3064=ORIENTED_EDGE('',*,*,#2200,.F.);
#3065=ORIENTED_EDGE('',*,*,#2119,.T.);
#3066=ORIENTED_EDGE('',*,*,#2201,.F.);
#3067=ORIENTED_EDGE('',*,*,#2143,.T.);
#3068=ORIENTED_EDGE('',*,*,#2202,.T.);
#3069=ORIENTED_EDGE('',*,*,#2088,.T.);
#3070=ORIENTED_EDGE('',*,*,#2203,.T.);
#3071=ORIENTED_EDGE('',*,*,#2174,.T.);
#3072=ORIENTED_EDGE('',*,*,#2204,.F.);
#3073=ORIENTED_EDGE('',*,*,#2123,.T.);
#3074=ORIENTED_EDGE('',*,*,#2205,.F.);
#3075=ORIENTED_EDGE('',*,*,#2139,.T.);
#3076=ORIENTED_EDGE('',*,*,#2206,.T.);
#3077=ORIENTED_EDGE('',*,*,#2084,.T.);
#3078=ORIENTED_EDGE('',*,*,#2207,.T.);
#3079=ORIENTED_EDGE('',*,*,#2178,.T.);
#3080=ORIENTED_EDGE('',*,*,#2208,.F.);
#3081=ORIENTED_EDGE('',*,*,#2127,.T.);
#3082=ORIENTED_EDGE('',*,*,#2209,.F.);
#3083=ORIENTED_EDGE('',*,*,#2135,.T.);
#3084=ORIENTED_EDGE('',*,*,#2210,.T.);
#3085=ORIENTED_EDGE('',*,*,#2080,.T.);
#3086=ORIENTED_EDGE('',*,*,#2211,.T.);
#3087=ORIENTED_EDGE('',*,*,#2182,.T.);
#3088=ORIENTED_EDGE('',*,*,#2212,.F.);
#3089=ORIENTED_EDGE('',*,*,#2131,.T.);
#3090=ORIENTED_EDGE('',*,*,#2213,.F.);
#3091=ORIENTED_EDGE('',*,*,#2214,.F.);
#3092=ORIENTED_EDGE('',*,*,#2215,.T.);
#3093=ORIENTED_EDGE('',*,*,#2185,.T.);
#3094=ORIENTED_EDGE('',*,*,#2216,.F.);
#3095=ORIENTED_EDGE('',*,*,#2217,.F.);
#3096=ORIENTED_EDGE('',*,*,#2106,.T.);
#3097=ORIENTED_EDGE('',*,*,#2218,.F.);
#3098=ORIENTED_EDGE('',*,*,#2219,.F.);
#3099=ORIENTED_EDGE('',*,*,#2156,.T.);
#3100=ORIENTED_EDGE('',*,*,#2189,.T.);
#3101=ORIENTED_EDGE('',*,*,#2110,.T.);
#3102=ORIENTED_EDGE('',*,*,#2220,.F.);
#3103=ORIENTED_EDGE('',*,*,#2152,.T.);
#3104=ORIENTED_EDGE('',*,*,#2193,.T.);
#3105=ORIENTED_EDGE('',*,*,#2114,.T.);
#3106=ORIENTED_EDGE('',*,*,#2221,.F.);
#3107=ORIENTED_EDGE('',*,*,#2148,.T.);
#3108=ORIENTED_EDGE('',*,*,#2197,.T.);
#3109=ORIENTED_EDGE('',*,*,#2118,.T.);
#3110=ORIENTED_EDGE('',*,*,#2222,.F.);
#3111=ORIENTED_EDGE('',*,*,#2144,.T.);
#3112=ORIENTED_EDGE('',*,*,#2201,.T.);
#3113=ORIENTED_EDGE('',*,*,#2122,.T.);
#3114=ORIENTED_EDGE('',*,*,#2223,.F.);
#3115=ORIENTED_EDGE('',*,*,#2140,.T.);
#3116=ORIENTED_EDGE('',*,*,#2205,.T.);
#3117=ORIENTED_EDGE('',*,*,#2126,.T.);
#3118=ORIENTED_EDGE('',*,*,#2224,.F.);
#3119=ORIENTED_EDGE('',*,*,#2136,.T.);
#3120=ORIENTED_EDGE('',*,*,#2209,.T.);
#3121=ORIENTED_EDGE('',*,*,#2130,.T.);
#3122=ORIENTED_EDGE('',*,*,#2225,.F.);
#3123=ORIENTED_EDGE('',*,*,#2132,.T.);
#3124=ORIENTED_EDGE('',*,*,#2226,.F.);
#3125=ORIENTED_EDGE('',*,*,#2213,.T.);
#3126=ORIENTED_EDGE('',*,*,#2101,.T.);
#3127=ORIENTED_EDGE('',*,*,#2192,.T.);
#3128=ORIENTED_EDGE('',*,*,#2161,.T.);
#3129=ORIENTED_EDGE('',*,*,#2227,.F.);
#3130=ORIENTED_EDGE('',*,*,#2097,.T.);
#3131=ORIENTED_EDGE('',*,*,#2196,.T.);
#3132=ORIENTED_EDGE('',*,*,#2165,.T.);
#3133=ORIENTED_EDGE('',*,*,#2228,.F.);
#3134=ORIENTED_EDGE('',*,*,#2093,.T.);
#3135=ORIENTED_EDGE('',*,*,#2200,.T.);
#3136=ORIENTED_EDGE('',*,*,#2169,.T.);
#3137=ORIENTED_EDGE('',*,*,#2229,.F.);
#3138=ORIENTED_EDGE('',*,*,#2089,.T.);
#3139=ORIENTED_EDGE('',*,*,#2204,.T.);
#3140=ORIENTED_EDGE('',*,*,#2173,.T.);
#3141=ORIENTED_EDGE('',*,*,#2230,.F.);
#3142=ORIENTED_EDGE('',*,*,#2085,.T.);
#3143=ORIENTED_EDGE('',*,*,#2208,.T.);
#3144=ORIENTED_EDGE('',*,*,#2177,.T.);
#3145=ORIENTED_EDGE('',*,*,#2231,.F.);
#3146=ORIENTED_EDGE('',*,*,#2081,.T.);
#3147=ORIENTED_EDGE('',*,*,#2212,.T.);
#3148=ORIENTED_EDGE('',*,*,#2181,.T.);
#3149=ORIENTED_EDGE('',*,*,#2232,.F.);
#3150=ORIENTED_EDGE('',*,*,#2105,.T.);
#3151=ORIENTED_EDGE('',*,*,#2188,.T.);
#3152=ORIENTED_EDGE('',*,*,#2233,.T.);
#3153=ORIENTED_EDGE('',*,*,#2158,.T.);
#3154=ORIENTED_EDGE('',*,*,#2234,.T.);
#3155=ORIENTED_EDGE('',*,*,#2218,.T.);
#3156=ORIENTED_EDGE('',*,*,#2157,.T.);
#3157=ORIENTED_EDGE('',*,*,#2219,.T.);
#3158=ORIENTED_EDGE('',*,*,#2234,.F.);
#3159=ORIENTED_EDGE('',*,*,#2184,.T.);
#3160=ORIENTED_EDGE('',*,*,#2235,.T.);
#3161=ORIENTED_EDGE('',*,*,#2236,.F.);
#3162=ORIENTED_EDGE('',*,*,#2216,.T.);
#3163=ORIENTED_EDGE('',*,*,#2102,.T.);
#3164=ORIENTED_EDGE('',*,*,#2227,.T.);
#3165=ORIENTED_EDGE('',*,*,#2160,.T.);
#3166=ORIENTED_EDGE('',*,*,#2237,.T.);
#3167=ORIENTED_EDGE('',*,*,#2109,.T.);
#3168=ORIENTED_EDGE('',*,*,#2238,.T.);
#3169=ORIENTED_EDGE('',*,*,#2153,.T.);
#3170=ORIENTED_EDGE('',*,*,#2220,.T.);
#3171=ORIENTED_EDGE('',*,*,#2098,.T.);
#3172=ORIENTED_EDGE('',*,*,#2228,.T.);
#3173=ORIENTED_EDGE('',*,*,#2164,.T.);
#3174=ORIENTED_EDGE('',*,*,#2239,.T.);
#3175=ORIENTED_EDGE('',*,*,#2113,.T.);
#3176=ORIENTED_EDGE('',*,*,#2240,.T.);
#3177=ORIENTED_EDGE('',*,*,#2149,.T.);
#3178=ORIENTED_EDGE('',*,*,#2221,.T.);
#3179=ORIENTED_EDGE('',*,*,#2094,.T.);
#3180=ORIENTED_EDGE('',*,*,#2229,.T.);
#3181=ORIENTED_EDGE('',*,*,#2168,.T.);
#3182=ORIENTED_EDGE('',*,*,#2241,.T.);
#3183=ORIENTED_EDGE('',*,*,#2117,.T.);
#3184=ORIENTED_EDGE('',*,*,#2242,.T.);
#3185=ORIENTED_EDGE('',*,*,#2145,.T.);
#3186=ORIENTED_EDGE('',*,*,#2222,.T.);
#3187=ORIENTED_EDGE('',*,*,#2090,.T.);
#3188=ORIENTED_EDGE('',*,*,#2230,.T.);
#3189=ORIENTED_EDGE('',*,*,#2172,.T.);
#3190=ORIENTED_EDGE('',*,*,#2243,.T.);
#3191=ORIENTED_EDGE('',*,*,#2121,.T.);
#3192=ORIENTED_EDGE('',*,*,#2244,.T.);
#3193=ORIENTED_EDGE('',*,*,#2141,.T.);
#3194=ORIENTED_EDGE('',*,*,#2223,.T.);
#3195=ORIENTED_EDGE('',*,*,#2086,.T.);
#3196=ORIENTED_EDGE('',*,*,#2231,.T.);
#3197=ORIENTED_EDGE('',*,*,#2176,.T.);
#3198=ORIENTED_EDGE('',*,*,#2245,.T.);
#3199=ORIENTED_EDGE('',*,*,#2125,.T.);
#3200=ORIENTED_EDGE('',*,*,#2246,.T.);
#3201=ORIENTED_EDGE('',*,*,#2137,.T.);
#3202=ORIENTED_EDGE('',*,*,#2224,.T.);
#3203=ORIENTED_EDGE('',*,*,#2082,.T.);
#3204=ORIENTED_EDGE('',*,*,#2232,.T.);
#3205=ORIENTED_EDGE('',*,*,#2180,.T.);
#3206=ORIENTED_EDGE('',*,*,#2247,.T.);
#3207=ORIENTED_EDGE('',*,*,#2129,.T.);
#3208=ORIENTED_EDGE('',*,*,#2248,.T.);
#3209=ORIENTED_EDGE('',*,*,#2133,.T.);
#3210=ORIENTED_EDGE('',*,*,#2225,.T.);
#3211=ORIENTED_EDGE('',*,*,#2108,.T.);
#3212=ORIENTED_EDGE('',*,*,#2190,.F.);
#3213=ORIENTED_EDGE('',*,*,#2154,.T.);
#3214=ORIENTED_EDGE('',*,*,#2238,.F.);
#3215=ORIENTED_EDGE('',*,*,#2112,.T.);
#3216=ORIENTED_EDGE('',*,*,#2194,.F.);
#3217=ORIENTED_EDGE('',*,*,#2150,.T.);
#3218=ORIENTED_EDGE('',*,*,#2240,.F.);
#3219=ORIENTED_EDGE('',*,*,#2116,.T.);
#3220=ORIENTED_EDGE('',*,*,#2198,.F.);
#3221=ORIENTED_EDGE('',*,*,#2146,.T.);
#3222=ORIENTED_EDGE('',*,*,#2242,.F.);
#3223=ORIENTED_EDGE('',*,*,#2120,.T.);
#3224=ORIENTED_EDGE('',*,*,#2202,.F.);
#3225=ORIENTED_EDGE('',*,*,#2142,.T.);
#3226=ORIENTED_EDGE('',*,*,#2244,.F.);
#3227=ORIENTED_EDGE('',*,*,#2124,.T.);
#3228=ORIENTED_EDGE('',*,*,#2206,.F.);
#3229=ORIENTED_EDGE('',*,*,#2138,.T.);
#3230=ORIENTED_EDGE('',*,*,#2246,.F.);
#3231=ORIENTED_EDGE('',*,*,#2128,.T.);
#3232=ORIENTED_EDGE('',*,*,#2210,.F.);
#3233=ORIENTED_EDGE('',*,*,#2134,.T.);
#3234=ORIENTED_EDGE('',*,*,#2248,.F.);
#3235=ORIENTED_EDGE('',*,*,#2103,.T.);
#3236=ORIENTED_EDGE('',*,*,#2237,.F.);
#3237=ORIENTED_EDGE('',*,*,#2159,.T.);
#3238=ORIENTED_EDGE('',*,*,#2233,.F.);
#3239=ORIENTED_EDGE('',*,*,#2187,.F.);
#3240=ORIENTED_EDGE('',*,*,#2099,.T.);
#3241=ORIENTED_EDGE('',*,*,#2239,.F.);
#3242=ORIENTED_EDGE('',*,*,#2163,.T.);
#3243=ORIENTED_EDGE('',*,*,#2191,.F.);
#3244=ORIENTED_EDGE('',*,*,#2095,.T.);
#3245=ORIENTED_EDGE('',*,*,#2241,.F.);
#3246=ORIENTED_EDGE('',*,*,#2167,.T.);
#3247=ORIENTED_EDGE('',*,*,#2195,.F.);
#3248=ORIENTED_EDGE('',*,*,#2091,.T.);
#3249=ORIENTED_EDGE('',*,*,#2243,.F.);
#3250=ORIENTED_EDGE('',*,*,#2171,.T.);
#3251=ORIENTED_EDGE('',*,*,#2199,.F.);
#3252=ORIENTED_EDGE('',*,*,#2087,.T.);
#3253=ORIENTED_EDGE('',*,*,#2245,.F.);
#3254=ORIENTED_EDGE('',*,*,#2175,.T.);
#3255=ORIENTED_EDGE('',*,*,#2203,.F.);
#3256=ORIENTED_EDGE('',*,*,#2083,.T.);
#3257=ORIENTED_EDGE('',*,*,#2247,.F.);
#3258=ORIENTED_EDGE('',*,*,#2179,.T.);
#3259=ORIENTED_EDGE('',*,*,#2207,.F.);
#3260=ORIENTED_EDGE('',*,*,#2079,.T.);
#3261=ORIENTED_EDGE('',*,*,#2249,.F.);
#3262=ORIENTED_EDGE('',*,*,#2235,.F.);
#3263=ORIENTED_EDGE('',*,*,#2183,.T.);
#3264=ORIENTED_EDGE('',*,*,#2211,.F.);
#3265=ORIENTED_EDGE('',*,*,#2077,.T.);
#3266=ORIENTED_EDGE('',*,*,#2215,.F.);
#3267=ORIENTED_EDGE('',*,*,#2250,.F.);
#3268=ORIENTED_EDGE('',*,*,#2251,.F.);
#3269=ORIENTED_EDGE('',*,*,#2252,.T.);
#3270=ORIENTED_EDGE('',*,*,#2253,.F.);
#3271=ORIENTED_EDGE('',*,*,#2252,.F.);
#3272=ORIENTED_EDGE('',*,*,#2253,.T.);
#3273=ORIENTED_EDGE('',*,*,#2250,.T.);
#3274=ORIENTED_EDGE('',*,*,#2214,.T.);
#3275=ORIENTED_EDGE('',*,*,#2226,.T.);
#3276=ORIENTED_EDGE('',*,*,#2186,.F.);
#3277=ORIENTED_EDGE('',*,*,#2217,.T.);
#3278=ORIENTED_EDGE('',*,*,#2236,.T.);
#3279=ORIENTED_EDGE('',*,*,#2249,.T.);
#3280=ORIENTED_EDGE('',*,*,#2078,.F.);
#3281=ORIENTED_EDGE('',*,*,#2251,.T.);
#3436=CYLINDRICAL_SURFACE('',#4017,3.22275);
#3437=CYLINDRICAL_SURFACE('',#4019,3.22275);
#3438=CYLINDRICAL_SURFACE('',#4020,3.22275);
#3439=CYLINDRICAL_SURFACE('',#4021,3.22275);
#3440=CYLINDRICAL_SURFACE('',#4022,3.22275);
#3441=CYLINDRICAL_SURFACE('',#4023,3.22275);
#3442=CYLINDRICAL_SURFACE('',#4024,3.22275);
#3443=CYLINDRICAL_SURFACE('',#4025,3.22275);
#3444=CYLINDRICAL_SURFACE('',#4026,3.22275);
#3445=CYLINDRICAL_SURFACE('',#4027,3.22275);
#3446=CYLINDRICAL_SURFACE('',#4028,3.22275);
#3447=CYLINDRICAL_SURFACE('',#4029,3.22275);
#3448=CYLINDRICAL_SURFACE('',#4030,3.22275);
#3449=CYLINDRICAL_SURFACE('',#4031,3.22275);
#3450=CYLINDRICAL_SURFACE('',#4037,3.933);
#3451=CYLINDRICAL_SURFACE('',#4038,3.933);
#3452=CYLINDRICAL_SURFACE('',#4040,3.933);
#3453=CYLINDRICAL_SURFACE('',#4041,3.933);
#3454=CYLINDRICAL_SURFACE('',#4042,3.933);
#3455=CYLINDRICAL_SURFACE('',#4043,3.933);
#3456=CYLINDRICAL_SURFACE('',#4044,3.933);
#3457=CYLINDRICAL_SURFACE('',#4045,3.933);
#3458=CYLINDRICAL_SURFACE('',#4046,3.933);
#3459=CYLINDRICAL_SURFACE('',#4047,3.933);
#3460=CYLINDRICAL_SURFACE('',#4048,3.933);
#3461=CYLINDRICAL_SURFACE('',#4049,3.933);
#3462=CYLINDRICAL_SURFACE('',#4050,3.933);
#3463=CYLINDRICAL_SURFACE('',#4051,3.933);
#3464=CYLINDRICAL_SURFACE('',#4054,5.);
#3587=ADVANCED_FACE('',(#495),#237,.F.);
#3588=ADVANCED_FACE('',(#496),#238,.F.);
#3589=ADVANCED_FACE('',(#497),#3436,.T.);
#3590=ADVANCED_FACE('',(#498),#3437,.T.);
#3591=ADVANCED_FACE('',(#499),#3438,.T.);
#3592=ADVANCED_FACE('',(#500),#3439,.T.);
#3593=ADVANCED_FACE('',(#501),#3440,.T.);
#3594=ADVANCED_FACE('',(#502),#3441,.T.);
#3595=ADVANCED_FACE('',(#503),#3442,.T.);
#3596=ADVANCED_FACE('',(#504),#3443,.T.);
#3597=ADVANCED_FACE('',(#505),#3444,.T.);
#3598=ADVANCED_FACE('',(#506),#3445,.T.);
#3599=ADVANCED_FACE('',(#507),#3446,.T.);
#3600=ADVANCED_FACE('',(#508),#3447,.T.);
#3601=ADVANCED_FACE('',(#509),#3448,.T.);
#3602=ADVANCED_FACE('',(#510),#3449,.T.);
#3603=ADVANCED_FACE('',(#511),#66,.F.);
#3604=ADVANCED_FACE('',(#512),#67,.F.);
#3605=ADVANCED_FACE('',(#513),#68,.F.);
#3606=ADVANCED_FACE('',(#514),#69,.F.);
#3607=ADVANCED_FACE('',(#515),#70,.F.);
#3608=ADVANCED_FACE('',(#516),#71,.F.);
#3609=ADVANCED_FACE('',(#517),#72,.F.);
#3610=ADVANCED_FACE('',(#518),#73,.F.);
#3611=ADVANCED_FACE('',(#519),#74,.F.);
#3612=ADVANCED_FACE('',(#520),#75,.F.);
#3613=ADVANCED_FACE('',(#521),#76,.F.);
#3614=ADVANCED_FACE('',(#522),#77,.F.);
#3615=ADVANCED_FACE('',(#523),#78,.F.);
#3616=ADVANCED_FACE('',(#524),#79,.F.);
#3617=ADVANCED_FACE('',(#525),#239,.T.);
#3618=ADVANCED_FACE('',(#526),#3450,.T.);
#3619=ADVANCED_FACE('',(#527),#3451,.T.);
#3620=ADVANCED_FACE('',(#528),#3452,.T.);
#3621=ADVANCED_FACE('',(#529),#3453,.T.);
#3622=ADVANCED_FACE('',(#530),#3454,.T.);
#3623=ADVANCED_FACE('',(#531),#3455,.T.);
#3624=ADVANCED_FACE('',(#532),#3456,.T.);
#3625=ADVANCED_FACE('',(#533),#3457,.T.);
#3626=ADVANCED_FACE('',(#534),#3458,.T.);
#3627=ADVANCED_FACE('',(#535),#3459,.T.);
#3628=ADVANCED_FACE('',(#536),#3460,.T.);
#3629=ADVANCED_FACE('',(#537),#3461,.T.);
#3630=ADVANCED_FACE('',(#538),#3462,.T.);
#3631=ADVANCED_FACE('',(#539),#3463,.T.);
#3632=ADVANCED_FACE('',(#540),#80,.F.);
#3633=ADVANCED_FACE('',(#541),#81,.F.);
#3634=ADVANCED_FACE('',(#542),#82,.F.);
#3635=ADVANCED_FACE('',(#543),#83,.F.);
#3636=ADVANCED_FACE('',(#544),#84,.F.);
#3637=ADVANCED_FACE('',(#545),#85,.F.);
#3638=ADVANCED_FACE('',(#546),#86,.F.);
#3639=ADVANCED_FACE('',(#547),#87,.F.);
#3640=ADVANCED_FACE('',(#548),#88,.F.);
#3641=ADVANCED_FACE('',(#549),#89,.F.);
#3642=ADVANCED_FACE('',(#550),#90,.F.);
#3643=ADVANCED_FACE('',(#551),#91,.F.);
#3644=ADVANCED_FACE('',(#552),#92,.F.);
#3645=ADVANCED_FACE('',(#553),#93,.F.);
#3646=ADVANCED_FACE('',(#554),#3464,.T.);
#3647=ADVANCED_FACE('',(#555,#196),#240,.T.);
#3648=ADVANCED_FACE('',(#556),#241,.F.);
#3683=CLOSED_SHELL('',(#3587,#3588,#3589,#3590,#3591,#3592,#3593,#3594,
#3595,#3596,#3597,#3598,#3599,#3600,#3601,#3602,#3603,#3604,#3605,#3606,
#3607,#3608,#3609,#3610,#3611,#3612,#3613,#3614,#3615,#3616,#3617,#3618,
#3619,#3620,#3621,#3622,#3623,#3624,#3625,#3626,#3627,#3628,#3629,#3630,
#3631,#3632,#3633,#3634,#3635,#3636,#3637,#3638,#3639,#3640,#3641,#3642,
#3643,#3644,#3645,#3646,#3647,#3648));
#4014=AXIS2_PLACEMENT_3D('',#22153,#4615,#4616);
#4015=AXIS2_PLACEMENT_3D('',#22154,#4617,#4618);
#4016=AXIS2_PLACEMENT_3D('',#22450,#4647,#4648);
#4017=AXIS2_PLACEMENT_3D('',#22746,#4677,#4678);
#4018=AXIS2_PLACEMENT_3D('',#22785,#4679,#4680);
#4019=AXIS2_PLACEMENT_3D('',#22786,#4681,#4682);
#4020=AXIS2_PLACEMENT_3D('',#22933,#4683,#4684);
#4021=AXIS2_PLACEMENT_3D('',#23080,#4685,#4686);
#4022=AXIS2_PLACEMENT_3D('',#23227,#4687,#4688);
#4023=AXIS2_PLACEMENT_3D('',#23374,#4689,#4690);
#4024=AXIS2_PLACEMENT_3D('',#23521,#4691,#4692);
#4025=AXIS2_PLACEMENT_3D('',#23668,#4693,#4694);
#4026=AXIS2_PLACEMENT_3D('',#23815,#4695,#4696);
#4027=AXIS2_PLACEMENT_3D('',#23962,#4697,#4698);
#4028=AXIS2_PLACEMENT_3D('',#24109,#4699,#4700);
#4029=AXIS2_PLACEMENT_3D('',#24256,#4701,#4702);
#4030=AXIS2_PLACEMENT_3D('',#24403,#4703,#4704);
#4031=AXIS2_PLACEMENT_3D('',#24550,#4705,#4706);
#4032=AXIS2_PLACEMENT_3D('',#24611,#4707,#4708);
#4033=AXIS2_PLACEMENT_3D('',#24639,#4709,#4710);
#4034=AXIS2_PLACEMENT_3D('',#24951,#4711,#4712);
#4035=AXIS2_PLACEMENT_3D('',#25132,#4713,#4714);
#4036=AXIS2_PLACEMENT_3D('',#25176,#4715,#4716);
#4037=AXIS2_PLACEMENT_3D('',#25177,#4717,#4718);
#4038=AXIS2_PLACEMENT_3D('',#25178,#4719,#4720);
#4039=AXIS2_PLACEMENT_3D('',#25186,#4721,#4722);
#4040=AXIS2_PLACEMENT_3D('',#25187,#4723,#4724);
#4041=AXIS2_PLACEMENT_3D('',#25246,#4725,#4726);
#4042=AXIS2_PLACEMENT_3D('',#25253,#4727,#4728);
#4043=AXIS2_PLACEMENT_3D('',#25260,#4729,#4730);
#4044=AXIS2_PLACEMENT_3D('',#25267,#4731,#4732);
#4045=AXIS2_PLACEMENT_3D('',#25274,#4733,#4734);
#4046=AXIS2_PLACEMENT_3D('',#25281,#4735,#4736);
#4047=AXIS2_PLACEMENT_3D('',#25288,#4737,#4738);
#4048=AXIS2_PLACEMENT_3D('',#25295,#4739,#4740);
#4049=AXIS2_PLACEMENT_3D('',#25302,#4741,#4742);
#4050=AXIS2_PLACEMENT_3D('',#25309,#4743,#4744);
#4051=AXIS2_PLACEMENT_3D('',#25316,#4745,#4746);
#4052=AXIS2_PLACEMENT_3D('',#25635,#4747,#4748);
#4053=AXIS2_PLACEMENT_3D('',#25652,#4749,#4750);
#4054=AXIS2_PLACEMENT_3D('',#25653,#4751,#4752);
#4055=AXIS2_PLACEMENT_3D('',#25655,#4753,#4754);
#4056=AXIS2_PLACEMENT_3D('',#25658,#4756,#4757);
#4057=AXIS2_PLACEMENT_3D('',#25659,#4758,#4759);
#4058=AXIS2_PLACEMENT_3D('',#25660,#4760,#4761);
#4615=DIRECTION('axis',(0.,0.,1.));
#4616=DIRECTION('refdir',(1.,0.,0.));
#4617=DIRECTION('center_axis',(0.,1.,0.));
#4618=DIRECTION('ref_axis',(0.,0.,1.));
#4619=DIRECTION('',(0.,0.,1.));
#4620=DIRECTION('',(1.,0.,0.));
#4621=DIRECTION('',(1.,0.,0.));
#4622=DIRECTION('',(1.,0.,0.));
#4623=DIRECTION('',(1.,0.,0.));
#4624=DIRECTION('',(1.,0.,0.));
#4625=DIRECTION('',(1.,0.,0.));
#4626=DIRECTION('',(1.,0.,0.));
#4627=DIRECTION('',(1.,0.,0.));
#4628=DIRECTION('',(1.,0.,0.));
#4629=DIRECTION('',(1.,0.,0.));
#4630=DIRECTION('',(1.,0.,0.));
#4631=DIRECTION('',(1.,0.,0.));
#4632=DIRECTION('',(1.,0.,0.));
#4633=DIRECTION('',(0.,0.,1.));
#4634=DIRECTION('',(-1.,0.,0.));
#4635=DIRECTION('',(-1.,0.,0.));
#4636=DIRECTION('',(-1.,0.,0.));
#4637=DIRECTION('',(-1.,0.,0.));
#4638=DIRECTION('',(-1.,0.,0.));
#4639=DIRECTION('',(-1.,0.,0.));
#4640=DIRECTION('',(-1.,0.,0.));
#4641=DIRECTION('',(-1.,0.,0.));
#4642=DIRECTION('',(-1.,0.,0.));
#4643=DIRECTION('',(-1.,0.,0.));
#4644=DIRECTION('',(-1.,0.,0.));
#4645=DIRECTION('',(-1.,0.,0.));
#4646=DIRECTION('',(-1.,0.,0.));
#4647=DIRECTION('center_axis',(0.,-1.,0.));
#4648=DIRECTION('ref_axis',(0.,0.,-1.));
#4649=DIRECTION('',(1.,0.,0.));
#4650=DIRECTION('',(1.,0.,0.));
#4651=DIRECTION('',(1.,0.,0.));
#4652=DIRECTION('',(1.,0.,0.));
#4653=DIRECTION('',(1.,0.,0.));
#4654=DIRECTION('',(1.,0.,0.));
#4655=DIRECTION('',(1.,0.,0.));
#4656=DIRECTION('',(1.,0.,0.));
#4657=DIRECTION('',(1.,0.,0.));
#4658=DIRECTION('',(1.,0.,0.));
#4659=DIRECTION('',(1.,0.,0.));
#4660=DIRECTION('',(1.,0.,0.));
#4661=DIRECTION('',(1.,0.,0.));
#4662=DIRECTION('',(0.,0.,-1.));
#4663=DIRECTION('',(-1.,0.,0.));
#4664=DIRECTION('',(-1.,0.,0.));
#4665=DIRECTION('',(-1.,0.,0.));
#4666=DIRECTION('',(-1.,0.,0.));
#4667=DIRECTION('',(-1.,0.,0.));
#4668=DIRECTION('',(-1.,0.,0.));
#4669=DIRECTION('',(-1.,0.,0.));
#4670=DIRECTION('',(-1.,0.,0.));
#4671=DIRECTION('',(-1.,0.,0.));
#4672=DIRECTION('',(-1.,0.,0.));
#4673=DIRECTION('',(-1.,0.,0.));
#4674=DIRECTION('',(-1.,0.,0.));
#4675=DIRECTION('',(-1.,0.,0.));
#4676=DIRECTION('',(0.,0.,-1.));
#4677=DIRECTION('center_axis',(-1.,0.,0.));
#4678=DIRECTION('ref_axis',(0.,-1.,2.19773242311135E-14));
#4679=DIRECTION('center_axis',(-1.,0.,0.));
#4680=DIRECTION('ref_axis',(0.,-1.,2.19773242311135E-14));
#4681=DIRECTION('center_axis',(-1.,0.,0.));
#4682=DIRECTION('ref_axis',(0.,-1.,2.19773242311135E-14));
#4683=DIRECTION('center_axis',(-1.,0.,0.));
#4684=DIRECTION('ref_axis',(0.,-1.,2.19773242311135E-14));
#4685=DIRECTION('center_axis',(-1.,0.,0.));
#4686=DIRECTION('ref_axis',(0.,-1.,2.19773242311135E-14));
#4687=DIRECTION('center_axis',(-1.,0.,0.));
#4688=DIRECTION('ref_axis',(0.,-1.,2.19773242311135E-14));
#4689=DIRECTION('center_axis',(-1.,0.,0.));
#4690=DIRECTION('ref_axis',(0.,-1.,2.19773242311135E-14));
#4691=DIRECTION('center_axis',(-1.,0.,0.));
#4692=DIRECTION('ref_axis',(0.,-1.,2.19773242311135E-14));
#4693=DIRECTION('center_axis',(-1.,0.,0.));
#4694=DIRECTION('ref_axis',(0.,-1.,2.19773242311135E-14));
#4695=DIRECTION('center_axis',(-1.,0.,0.));
#4696=DIRECTION('ref_axis',(0.,-1.,2.19773242311135E-14));
#4697=DIRECTION('center_axis',(-1.,0.,0.));
#4698=DIRECTION('ref_axis',(0.,-1.,2.19773242311135E-14));
#4699=DIRECTION('center_axis',(-1.,0.,0.));
#4700=DIRECTION('ref_axis',(0.,-1.,2.19773242311135E-14));
#4701=DIRECTION('center_axis',(-1.,0.,0.));
#4702=DIRECTION('ref_axis',(0.,-1.,2.19773242311135E-14));
#4703=DIRECTION('center_axis',(-1.,0.,0.));
#4704=DIRECTION('ref_axis',(0.,-1.,2.19773242311135E-14));
#4705=DIRECTION('center_axis',(-1.,0.,0.));
#4706=DIRECTION('ref_axis',(0.,-1.,2.19773242311135E-14));
#4707=DIRECTION('center_axis',(1.,0.,0.));
#4708=DIRECTION('ref_axis',(0.,-1.,2.19773242311135E-14));
#4709=DIRECTION('center_axis',(1.,2.26944640896891E-13,2.4756931710509E-13));
#4710=DIRECTION('ref_axis',(-2.99635666187295E-14,0.794492776111595,-0.607273602840179));
#4711=DIRECTION('center_axis',(1.,-4.24721344664965E-14,7.81460509822211E-14));
#4712=DIRECTION('ref_axis',(-1.5231504897179E-14,0.783860772073074,0.620936623179052));
#4713=DIRECTION('center_axis',(-1.,0.,0.));
#4714=DIRECTION('ref_axis',(0.,-1.,0.));
#4715=DIRECTION('center_axis',(1.,0.,0.));
#4716=DIRECTION('ref_axis',(0.,-1.,0.));
#4717=DIRECTION('center_axis',(-1.,0.,0.));
#4718=DIRECTION('ref_axis',(0.,-1.,0.));
#4719=DIRECTION('center_axis',(-1.,0.,0.));
#4720=DIRECTION('ref_axis',(0.,-1.,0.));
#4721=DIRECTION('center_axis',(1.,0.,0.));
#4722=DIRECTION('ref_axis',(0.,-1.,0.));
#4723=DIRECTION('center_axis',(-1.,0.,0.));
#4724=DIRECTION('ref_axis',(0.,-1.,0.));
#4725=DIRECTION('center_axis',(-1.,0.,0.));
#4726=DIRECTION('ref_axis',(0.,-1.,0.));
#4727=DIRECTION('center_axis',(-1.,0.,0.));
#4728=DIRECTION('ref_axis',(0.,-1.,0.));
#4729=DIRECTION('center_axis',(-1.,0.,0.));
#4730=DIRECTION('ref_axis',(0.,-1.,0.));
#4731=DIRECTION('center_axis',(-1.,0.,0.));
#4732=DIRECTION('ref_axis',(0.,-1.,0.));
#4733=DIRECTION('center_axis',(-1.,0.,0.));
#4734=DIRECTION('ref_axis',(0.,-1.,0.));
#4735=DIRECTION('center_axis',(-1.,0.,0.));
#4736=DIRECTION('ref_axis',(0.,-1.,0.));
#4737=DIRECTION('center_axis',(-1.,0.,0.));
#4738=DIRECTION('ref_axis',(0.,-1.,0.));
#4739=DIRECTION('center_axis',(-1.,0.,0.));
#4740=DIRECTION('ref_axis',(0.,-1.,0.));
#4741=DIRECTION('center_axis',(-1.,0.,0.));
#4742=DIRECTION('ref_axis',(0.,-1.,0.));
#4743=DIRECTION('center_axis',(-1.,0.,0.));
#4744=DIRECTION('ref_axis',(0.,-1.,0.));
#4745=DIRECTION('center_axis',(-1.,0.,0.));
#4746=DIRECTION('ref_axis',(0.,-1.,0.));
#4747=DIRECTION('center_axis',(1.,-7.18663344203148E-15,1.44094323913819E-14));
#4748=DIRECTION('ref_axis',(-4.36221174028664E-15,0.74050159851997,0.672054597922944));
#4749=DIRECTION('center_axis',(1.,-2.70011984489144E-13,-2.93694733491497E-13));
#4750=DIRECTION('ref_axis',(4.40921431182727E-14,-0.656854870457007,0.754017028426354));
#4751=DIRECTION('center_axis',(1.,0.,0.));
#4752=DIRECTION('ref_axis',(0.,-1.,0.));
#4753=DIRECTION('center_axis',(1.,0.,0.));
#4754=DIRECTION('ref_axis',(0.,-1.,0.));
#4755=DIRECTION('',(-1.,0.,0.));
#4756=DIRECTION('center_axis',(-1.,0.,0.));
#4757=DIRECTION('ref_axis',(0.,-1.,0.));
#4758=DIRECTION('center_axis',(-1.,0.,0.));
#4759=DIRECTION('ref_axis',(0.,-1.,0.));
#4760=DIRECTION('center_axis',(-1.,0.,0.));
#4761=DIRECTION('ref_axis',(0.,-1.,0.));
#22153=CARTESIAN_POINT('',(0.,0.,0.));
#22154=CARTESIAN_POINT('Origin',(3.02384907614375,-2.84862442585767,-2.80808455720391));
#22155=CARTESIAN_POINT('',(11.0238443243108,-2.84858103864746,-1.7782820253861));
#22156=CARTESIAN_POINT('',(10.9314356691441,-2.84862442585767,-1.5071351773836));
#22157=CARTESIAN_POINT('Ctrl Pts',(11.0238395724777,-2.84862442585767,-1.77821291115482));
#22158=CARTESIAN_POINT('Ctrl Pts',(11.023058671384,-2.84862442585767,-1.77602158816867));
#22159=CARTESIAN_POINT('Ctrl Pts',(11.0222784621947,-2.84862442585824,-1.7738300165061));
#22160=CARTESIAN_POINT('Ctrl Pts',(11.0062774820837,-2.84862442585824,-1.72883879945583));
#22161=CARTESIAN_POINT('Ctrl Pts',(10.9913133628153,-2.84862442585851,-1.68592261376175));
#22162=CARTESIAN_POINT('Ctrl Pts',(10.9612482690896,-2.84862442585851,-1.59778423981652));
#22163=CARTESIAN_POINT('Ctrl Pts',(10.9461611622631,-2.84862442585767,-1.55250504487283));
#22164=CARTESIAN_POINT('Ctrl Pts',(10.9314356691441,-2.84862442585767,-1.5071351773836));
#22165=CARTESIAN_POINT('',(11.0238490787776,-2.84862442708806,2.51132611227744));
#22166=CARTESIAN_POINT('',(11.0238490761438,-2.84862442585767,6.75363122348402));
#22167=CARTESIAN_POINT('',(10.7378093816896,-2.84862442585767,1.50713517738359));
#22168=CARTESIAN_POINT('Ctrl Pts',(10.7378093816896,-2.84862442585767,1.5071351773836));
#22169=CARTESIAN_POINT('Ctrl Pts',(10.7745509100274,-2.84862442585767,1.67768015510688));
#22170=CARTESIAN_POINT('Ctrl Pts',(10.8181799183082,-2.84862442695797,1.84746530235002));
#22171=CARTESIAN_POINT('Ctrl Pts',(10.9144539328214,-2.84862442695797,2.18146463191032));
#22172=CARTESIAN_POINT('Ctrl Pts',(10.9675731917165,-2.84862442585767,2.34753476778138));
#22173=CARTESIAN_POINT('Ctrl Pts',(11.0238490840452,-2.84862442585767,2.51132611046758));
#22174=CARTESIAN_POINT('',(10.4912624831434,-2.84862442585767,1.50713517738358));
#22175=CARTESIAN_POINT('',(13.3346225254169,-2.84862442585767,1.50713517738359));
#22176=CARTESIAN_POINT('',(10.0266594217773,-2.84681894361813,2.71028906402779));
#22177=CARTESIAN_POINT('Ctrl Pts',(10.0267941012523,-2.84862442585767,2.70859765771964));
#22178=CARTESIAN_POINT('Ctrl Pts',(10.0337979544476,-2.84862442585767,2.69250499494907));
#22179=CARTESIAN_POINT('Ctrl Pts',(10.0407818720682,-2.84862442585767,2.67640214955592));
#22180=CARTESIAN_POINT('Ctrl Pts',(10.1253566086339,-2.84862442585767,2.48069385236447));
#22181=CARTESIAN_POINT('Ctrl Pts',(10.2012319741895,-2.84862442733188,2.29789169628234));
#22182=CARTESIAN_POINT('Ctrl Pts',(10.3504646709377,-2.84862442733188,1.91583275087761));
#22183=CARTESIAN_POINT('Ctrl Pts',(10.4249778185909,-2.84862442585767,1.7113610340671));
#22184=CARTESIAN_POINT('Ctrl Pts',(10.4912624831434,-2.84862442585767,1.5071351773836));
#22185=CARTESIAN_POINT('',(9.84333237813747,-2.84681996992431,2.71028970229123));
#22186=CARTESIAN_POINT('',(11.0238490761438,-2.84862442585767,2.71179421793157));
#22187=CARTESIAN_POINT('',(9.48780938168963,-2.84862442585767,1.50713517738359));
#22188=CARTESIAN_POINT('Ctrl Pts',(9.48780938168963,-2.84862442585767,1.5071351773836));
#22189=CARTESIAN_POINT('Ctrl Pts',(9.53185899985944,-2.84862442585767,1.71160247880986));
#22190=CARTESIAN_POINT('Ctrl Pts',(9.58587318685495,-2.84862442792121,1.91525078718682));
#22191=CARTESIAN_POINT('Ctrl Pts',(9.70094960223702,-2.84862442792121,2.2980896617317));
#22192=CARTESIAN_POINT('Ctrl Pts',(9.76180678295297,-2.84862442585767,2.48053952383311));
#22193=CARTESIAN_POINT('Ctrl Pts',(9.8318097489011,-2.84862442585767,2.67629614457399));
#22194=CARTESIAN_POINT('Ctrl Pts',(9.83762325462799,-2.84862442585767,2.69245362484614));
#22195=CARTESIAN_POINT('Ctrl Pts',(9.84346698885961,-2.84862442585767,2.70859905909217));
#22196=CARTESIAN_POINT('',(9.24126248314343,-2.84862442585767,1.50713517738358));
#22197=CARTESIAN_POINT('',(13.3346225254169,-2.84862442585767,1.50713517738359));
#22198=CARTESIAN_POINT('',(8.77665942204888,-2.84682623267641,2.71029357829656));
#22199=CARTESIAN_POINT('Ctrl Pts',(8.77679361475528,-2.84862442585767,2.70860756651644));
#22200=CARTESIAN_POINT('Ctrl Pts',(8.78379792777184,-2.84862442585767,2.69251369706502));
#22201=CARTESIAN_POINT('Ctrl Pts',(8.79078230243175,-2.84862442585767,2.67640964375849));
#22202=CARTESIAN_POINT('Ctrl Pts',(8.8753576224118,-2.84862442585767,2.48069807460854));
#22203=CARTESIAN_POINT('Ctrl Pts',(8.95123295617157,-2.8486244273253,2.29789414186475));
#22204=CARTESIAN_POINT('Ctrl Pts',(9.10046525102538,-2.8486244273253,1.91583271764201));
#22205=CARTESIAN_POINT('Ctrl Pts',(9.17497777181831,-2.84862442585767,1.71136117817557));
#22206=CARTESIAN_POINT('Ctrl Pts',(9.24126248314343,-2.84862442585767,1.50713517738359));
#22207=CARTESIAN_POINT('',(8.59333237745357,-2.84682736201,2.71029427388594));
#22208=CARTESIAN_POINT('',(11.0238490761438,-2.84862442585767,2.71179421793157));
#22209=CARTESIAN_POINT('',(8.23780938168963,-2.84862442585767,1.50713517738359));
#22210=CARTESIAN_POINT('Ctrl Pts',(8.23780938168964,-2.84862442585767,1.5071351773836));
#22211=CARTESIAN_POINT('Ctrl Pts',(8.28185902228173,-2.84862442585767,1.7116025828885));
#22212=CARTESIAN_POINT('Ctrl Pts',(8.33587259560373,-2.84862442791195,1.91525079323359));
#22213=CARTESIAN_POINT('Ctrl Pts',(8.45094825529517,-2.84862442791195,2.29809205765932));
#22214=CARTESIAN_POINT('Ctrl Pts',(8.51180523038482,-2.84862442585767,2.48054376287594));
#22215=CARTESIAN_POINT('Ctrl Pts',(8.58180849741605,-2.84862442585767,2.67630369365445));
#22216=CARTESIAN_POINT('Ctrl Pts',(8.58762237980882,-2.84862442585767,2.69246241698621));
#22217=CARTESIAN_POINT('Ctrl Pts',(8.59346649505355,-2.84862442585767,2.70860909277272));
#22218=CARTESIAN_POINT('',(7.99126248314343,-2.84862442585767,1.50713517738358));
#22219=CARTESIAN_POINT('',(13.3346225254169,-2.84862442585767,1.50713517738359));
#22220=CARTESIAN_POINT('',(7.526659415135,-2.84683427137387,2.71029850822801));
#22221=CARTESIAN_POINT('Ctrl Pts',(7.52679307496196,-2.84862442585767,2.70861838061488));
#22222=CARTESIAN_POINT('Ctrl Pts',(7.53379789201695,-2.84862442585767,2.6925231903734));
#22223=CARTESIAN_POINT('Ctrl Pts',(7.54078276765018,-2.84862442585767,2.67641781492382));
#22224=CARTESIAN_POINT('Ctrl Pts',(7.62535873067299,-2.84862442585767,2.48070267374547));
#22225=CARTESIAN_POINT('Ctrl Pts',(7.70123402906389,-2.84862442731812,2.29789681034083));
#22226=CARTESIAN_POINT('Ctrl Pts',(7.85046588841197,-2.84862442731812,1.91583267628874));
#22227=CARTESIAN_POINT('Ctrl Pts',(7.92497771912674,-2.84862442585767,1.7113613405205));
#22228=CARTESIAN_POINT('Ctrl Pts',(7.99126248314342,-2.84862442585767,1.5071351773836));
#22229=CARTESIAN_POINT('',(7.34333236934253,-2.846835520603,2.71029927000383));
#22230=CARTESIAN_POINT('',(11.0238490761438,-2.84862442585767,2.71179421793157));
#22231=CARTESIAN_POINT('',(6.98780938168963,-2.84862442585767,1.50713517738359));
#22232=CARTESIAN_POINT('Ctrl Pts',(6.98780938168963,-2.84862442585767,1.5071351773836));
#22233=CARTESIAN_POINT('Ctrl Pts',(7.0318590477534,-2.84862442585767,1.71160270112162));
#22234=CARTESIAN_POINT('Ctrl Pts',(7.08587194364161,-2.84862442790181,1.91525079631235));
#22235=CARTESIAN_POINT('Ctrl Pts',(7.20094677397292,-2.84862442790181,2.29809467489166));
#22236=CARTESIAN_POINT('Ctrl Pts',(7.26180352074679,-2.84862442585766,2.48054838492829));
#22237=CARTESIAN_POINT('Ctrl Pts',(7.33180711870137,-2.84862442585766,2.67631193139019));
#22238=CARTESIAN_POINT('Ctrl Pts',(7.33762141389105,-2.84862442585767,2.69247201579432));
#22239=CARTESIAN_POINT('Ctrl Pts',(7.34346594671238,-2.84862442585767,2.70862005097966));
#22240=CARTESIAN_POINT('',(6.74126248314343,-2.84862442585767,1.50713517738358));
#22241=CARTESIAN_POINT('',(13.3346225254169,-2.84862442585767,1.50713517738359));
#22242=CARTESIAN_POINT('',(6.2766593992019,-2.84684318562975,2.71030391984611));
#22243=CARTESIAN_POINT('Ctrl Pts',(6.27679247260682,-2.84862442585767,2.70863024324506));
#22244=CARTESIAN_POINT('Ctrl Pts',(6.28379784512061,-2.84862442585767,2.69253359968691));
#22245=CARTESIAN_POINT('Ctrl Pts',(6.29078327281752,-2.84862442585768,2.67642676942568));
#22246=CARTESIAN_POINT('Ctrl Pts',(6.37535994854178,-2.84862442585768,2.48070770856496));
#22247=CARTESIAN_POINT('Ctrl Pts',(6.45123520736229,-2.84862442731026,2.29789973691976));
#22248=CARTESIAN_POINT('Ctrl Pts',(6.60046659256744,-2.84862442731026,1.91583262505285));
#22249=CARTESIAN_POINT('Ctrl Pts',(6.67497765942542,-2.84862442585767,1.71136152446282));
#22250=CARTESIAN_POINT('Ctrl Pts',(6.74126248314343,-2.84862442585767,1.50713517738359));
#22251=CARTESIAN_POINT('',(6.09333235190302,-2.8468445755701,2.71030475869925));
#22252=CARTESIAN_POINT('',(11.0238490761438,-2.84862442585767,2.71179421793157));
#22253=CARTESIAN_POINT('',(5.73780938168963,-2.84862442585767,1.50713517738359));
#22254=CARTESIAN_POINT('Ctrl Pts',(5.73780938168963,-2.84862442585767,1.5071351773836));
#22255=CARTESIAN_POINT('Ctrl Pts',(5.78185907685439,-2.84862442585767,1.71160283620116));
#22256=CARTESIAN_POINT('Ctrl Pts',(5.83587122068751,-2.84862442789063,1.91525079561866));
#22257=CARTESIAN_POINT('Ctrl Pts',(5.9509451358443,-2.84862442789063,2.29809754881907));
#22258=CARTESIAN_POINT('Ctrl Pts',(6.01180162763585,-2.84862442585767,2.48055345043311));
#22259=CARTESIAN_POINT('Ctrl Pts',(6.08180559131495,-2.84862442585767,2.67632096708642));
#22260=CARTESIAN_POINT('Ctrl Pts',(6.08762034133423,-2.84862442585767,2.69248254974333));
#22261=CARTESIAN_POINT('Ctrl Pts',(6.09346533427394,-2.84862442585767,2.70863208133986));
#22262=CARTESIAN_POINT('',(5.49126248314343,-2.84862442585767,1.50713517738358));
#22263=CARTESIAN_POINT('',(13.3346225254169,-2.84862442585767,1.50713517738359));
#22264=CARTESIAN_POINT('',(5.02665937189225,-2.84685313164047,2.71030989474673));
#22265=CARTESIAN_POINT('Ctrl Pts',(5.02679179614449,-2.84862442585767,2.70864333135427));
#22266=CARTESIAN_POINT('Ctrl Pts',(5.03379778445795,-2.84862442585767,2.69254507916332));
#22267=CARTESIAN_POINT('Ctrl Pts',(5.04078382417434,-2.84862442585766,2.67643663859843));
#22268=CARTESIAN_POINT('Ctrl Pts',(5.12536129472081,-2.84862442585766,2.48071325160255));
#22269=CARTESIAN_POINT('Ctrl Pts',(5.20123650898541,-2.84862442730161,2.29790296509866));
#22270=CARTESIAN_POINT('Ctrl Pts',(5.35046737523669,-2.84862442730161,1.91583256170217));
#22271=CARTESIAN_POINT('Ctrl Pts',(5.42497759134768,-2.84862442585767,1.7113617342132));
#22272=CARTESIAN_POINT('Ctrl Pts',(5.49126248314342,-2.84862442585767,1.5071351773836));
#22273=CARTESIAN_POINT('',(4.84333232268694,-2.84685468828742,2.71031082423224));
#22274=CARTESIAN_POINT('',(11.0238490761438,-2.84862442585767,2.71179421793157));
#22275=CARTESIAN_POINT('',(4.48780938168963,-2.84862442585767,1.50713517738359));
#22276=CARTESIAN_POINT('Ctrl Pts',(4.48780938168963,-2.84862442585767,1.5071351773836));
#22277=CARTESIAN_POINT('Ctrl Pts',(4.53185911031318,-2.84862442585767,1.71160299150844));
#22278=CARTESIAN_POINT('Ctrl Pts',(4.58587041394647,-2.84862442787828,1.9152507901144));
#22279=CARTESIAN_POINT('Ctrl Pts',(4.70094331303715,-2.84862442787828,2.29810072324551));
#22280=CARTESIAN_POINT('Ctrl Pts',(4.76179951821517,-2.84862442585766,2.48055903410995));
#22281=CARTESIAN_POINT('Ctrl Pts',(4.83180388858748,-2.84862442585766,2.67633093595801));
#22282=CARTESIAN_POINT('Ctrl Pts',(4.83761914279346,-2.84862442585767,2.69249417782208));
#22283=CARTESIAN_POINT('Ctrl Pts',(4.84346464580177,-2.84862442585767,2.70864536656847));
#22284=CARTESIAN_POINT('',(4.24126248314343,-2.84862442585767,1.50713517738358));
#22285=CARTESIAN_POINT('',(13.3346225254169,-2.84862442585767,1.50713517738359));
#22286=CARTESIAN_POINT('',(3.77665933013941,-2.84686430560633,2.71031653510881));
#22287=CARTESIAN_POINT('Ctrl Pts',(3.77679103100252,-2.84862442585767,2.70865786644558));
#22288=CARTESIAN_POINT('Ctrl Pts',(3.78379770666065,-2.84862442585767,2.69255782170753));
#22289=CARTESIAN_POINT('Ctrl Pts',(3.7907844294769,-2.84862442585767,2.6764475867298));
#22290=CARTESIAN_POINT('Ctrl Pts',(3.87536279264918,-2.84862442585767,2.48071939353203));
#22291=CARTESIAN_POINT('Ctrl Pts',(3.95123795638205,-2.84862442729201,2.29790654931287));
#22292=CARTESIAN_POINT('Ctrl Pts',(4.10046825118152,-2.84862442729201,1.91583248336832));
#22293=CARTESIAN_POINT('Ctrl Pts',(4.17497751316149,-2.84862442585767,1.71136197510816));
#22294=CARTESIAN_POINT('Ctrl Pts',(4.24126248314342,-2.84862442585767,1.5071351773836));
#22295=CARTESIAN_POINT('',(3.5933397832319,-2.84842713334438,2.71177821818276));
#22296=CARTESIAN_POINT('',(11.0238490761438,-2.84862442585767,2.71179421793157));
#22297=CARTESIAN_POINT('',(3.23780938168963,-2.84862442585767,1.50713517738359));
#22298=CARTESIAN_POINT('Ctrl Pts',(3.23780938168963,-2.84862442585767,1.50713517738361));
#22299=CARTESIAN_POINT('Ctrl Pts',(3.28186054745108,-2.84862442585767,1.71160966234283));
#22300=CARTESIAN_POINT('Ctrl Pts',(3.33582269739854,-2.84862442724084,1.91524933773065));
#22301=CARTESIAN_POINT('Ctrl Pts',(3.45073483075678,-2.84862442724084,2.2979205346272));
#22302=CARTESIAN_POINT('Ctrl Pts',(3.51144589960124,-2.84862442585768,2.48014616288996));
#22303=CARTESIAN_POINT('Ctrl Pts',(3.58146712224872,-2.84862442585768,2.67616260726964));
#22304=CARTESIAN_POINT('Ctrl Pts',(3.58743530933706,-2.84862442585767,2.69276463740784));
#22305=CARTESIAN_POINT('Ctrl Pts',(3.59343543922426,-2.84862442585767,2.70935393890616));
#22306=CARTESIAN_POINT('',(3.02384907614375,-2.84862442585767,1.50713517738359));
#22307=CARTESIAN_POINT('',(13.3346225254169,-2.84862442585767,1.50713517738359));
#22308=CARTESIAN_POINT('',(3.02365448843556,-2.84819869582995,-2.12611758856074));
#22309=CARTESIAN_POINT('',(3.02384907614375,-2.84862442585767,-1.40404227860195));
#22310=CARTESIAN_POINT('',(3.18488877059788,-2.84862442585766,-1.50713517738361));
#22311=CARTESIAN_POINT('Ctrl Pts',(3.18488877059788,-2.84862442585767,-1.50713517738361));
#22312=CARTESIAN_POINT('Ctrl Pts',(3.16242044753531,-2.84862442585767,-1.61142750896447));
#22313=CARTESIAN_POINT('Ctrl Pts',(3.137405991007,-2.84862442595863,-1.71531300796113));
#22314=CARTESIAN_POINT('Ctrl Pts',(3.0834656597595,-2.84862442595863,-1.92105514468293));
#22315=CARTESIAN_POINT('Ctrl Pts',(3.0544704326137,-2.84862442585767,-2.02327555320667));
#22316=CARTESIAN_POINT('Ctrl Pts',(3.02384907614375,-2.84862442585767,-2.12477398354848));
#22317=CARTESIAN_POINT('',(3.43143566914408,-2.84862442585766,-1.5071351773836));
#22318=CARTESIAN_POINT('',(13.3346225254169,-2.84862442585767,-1.50713517738359));
#22319=CARTESIAN_POINT('',(3.89603880551603,-2.84686020278407,-2.71031410533045));
#22320=CARTESIAN_POINT('Ctrl Pts',(3.89590683973102,-2.84862442585767,-2.70865254916596));
#22321=CARTESIAN_POINT('Ctrl Pts',(3.88889722083,-2.84862442585767,-2.69254581918906));
#22322=CARTESIAN_POINT('Ctrl Pts',(3.88190757115915,-2.84862442585768,-2.67642888977708));
#22323=CARTESIAN_POINT('Ctrl Pts',(3.79732623229834,-2.84862442585768,-2.48069416593426));
#22324=CARTESIAN_POINT('Ctrl Pts',(3.7214509531498,-2.84862442738219,-2.29788126150319));
#22325=CARTESIAN_POINT('Ctrl Pts',(3.57222405172544,-2.84862442738219,-1.91581557178352));
#22326=CARTESIAN_POINT('Ctrl Pts',(3.49771788311829,-2.84862442585767,-1.71135348373173));
#22327=CARTESIAN_POINT('Ctrl Pts',(3.43143566914408,-2.84862442585767,-1.50713517738359));
#22328=CARTESIAN_POINT('',(4.07936584331022,-2.84685855096328,-2.71031312437899));
#22329=CARTESIAN_POINT('',(11.0238490761438,-2.84862442585767,-2.71179421793157));
#22330=CARTESIAN_POINT('',(4.43488877059788,-2.84862442585766,-1.50713517738361));
#22331=CARTESIAN_POINT('Ctrl Pts',(4.43488877059788,-2.84862442585767,-1.50713517738361));
#22332=CARTESIAN_POINT('Ctrl Pts',(4.39082934716643,-2.84862442585767,-1.71164799237998));
#22333=CARTESIAN_POINT('Ctrl Pts',(4.33680421314192,-2.84862442782486,-1.91534068114032));
#22334=CARTESIAN_POINT('Ctrl Pts',(4.22171428517076,-2.84862442782486,-2.29822947317743));
#22335=CARTESIAN_POINT('Ctrl Pts',(4.16085761026589,-2.84862442585767,-2.48068346557449));
#22336=CARTESIAN_POINT('Ctrl Pts',(4.09086679229697,-2.84862442585767,-2.67641287300669));
#22337=CARTESIAN_POINT('Ctrl Pts',(4.08506533437374,-2.84862442585767,-2.69253763418667));
#22338=CARTESIAN_POINT('Ctrl Pts',(4.07923377064371,-2.84862442585767,-2.70865040206242));
#22339=CARTESIAN_POINT('',(4.68143566914408,-2.84862442585766,-1.5071351773836));
#22340=CARTESIAN_POINT('',(13.3346225254169,-2.84862442585767,-1.50713517738359));
#22341=CARTESIAN_POINT('',(5.14603876927131,-2.8468494881385,-2.71030771333065));
#22342=CARTESIAN_POINT('Ctrl Pts',(5.14590610781719,-2.84862442585767,-2.70863855402169));
#22343=CARTESIAN_POINT('Ctrl Pts',(5.13889714963154,-2.84862442585767,-2.69253354823215));
#22344=CARTESIAN_POINT('Ctrl Pts',(5.13190815660042,-2.84862442585766,-2.67641834479668));
#22345=CARTESIAN_POINT('Ctrl Pts',(5.04732767386717,-2.84862442585766,-2.48068824836471));
#22346=CARTESIAN_POINT('Ctrl Pts',(4.97145234642707,-2.8486244273917,-2.29787781119133));
#22347=CARTESIAN_POINT('Ctrl Pts',(4.82222489298551,-2.8486244273917,-1.91581564514287));
#22348=CARTESIAN_POINT('Ctrl Pts',(4.74771780885373,-2.84862442585767,-1.71135325491949));
#22349=CARTESIAN_POINT('Ctrl Pts',(4.68143566914408,-2.84862442585767,-1.50713517738359));
#22350=CARTESIAN_POINT('',(5.3293658092159,-2.84684801847815,-2.71030683105326));
#22351=CARTESIAN_POINT('',(11.0238490761438,-2.84862442585767,-2.71179421793157));
#22352=CARTESIAN_POINT('',(5.68488877059788,-2.84862442585766,-1.50713517738361));
#22353=CARTESIAN_POINT('Ctrl Pts',(5.68488877059787,-2.84862442585767,-1.50713517738361));
#22354=CARTESIAN_POINT('Ctrl Pts',(5.64082938247698,-2.84862442585767,-1.71164782847729));
#22355=CARTESIAN_POINT('Ctrl Pts',(5.58680337295899,-2.84862442783755,-1.91534068797091));
#22356=CARTESIAN_POINT('Ctrl Pts',(5.47171238880716,-2.84862442783755,-2.29822617883969));
#22357=CARTESIAN_POINT('Ctrl Pts',(5.41085541472201,-2.84862442585768,-2.48067767630624));
#22358=CARTESIAN_POINT('Ctrl Pts',(5.34086501982091,-2.84862442585768,-2.67640253517119));
#22359=CARTESIAN_POINT('Ctrl Pts',(5.335064085706,-2.84862442585767,-2.69252557390748));
#22360=CARTESIAN_POINT('Ctrl Pts',(5.32923305188914,-2.84862442585767,-2.70863662146847));
#22361=CARTESIAN_POINT('',(5.93143566914408,-2.84862442585766,-1.5071351773836));
#22362=CARTESIAN_POINT('',(13.3346225254169,-2.84862442585767,-1.50713517738359));
#22363=CARTESIAN_POINT('',(6.3960387462905,-2.84683992679533,-2.71030194794593));
#22364=CARTESIAN_POINT('Ctrl Pts',(6.39590545902977,-2.84862442585767,-2.70862592165797));
#22365=CARTESIAN_POINT('Ctrl Pts',(6.38889709426525,-2.84862442585767,-2.69252246698333));
#22366=CARTESIAN_POINT('Ctrl Pts',(6.381908691017,-2.84862442585767,-2.67640881627049));
#22367=CARTESIAN_POINT('Ctrl Pts',(6.29732897257062,-2.84862442585767,-2.48068289513417));
#22368=CARTESIAN_POINT('Ctrl Pts',(6.22145360243729,-2.8486244274003,-2.29787469612044));
#22369=CARTESIAN_POINT('Ctrl Pts',(6.07222564657022,-2.8486244274003,-1.91581570455012));
#22370=CARTESIAN_POINT('Ctrl Pts',(5.99771774402429,-2.84862442585767,-1.71135305517723));
#22371=CARTESIAN_POINT('Ctrl Pts',(5.93143566914408,-2.84862442585767,-1.50713517738359));
#22372=CARTESIAN_POINT('',(6.57936578792838,-2.84683861010252,-2.71030114914197));
#22373=CARTESIAN_POINT('',(11.0238490761438,-2.84862442585767,-2.71179421793157));
#22374=CARTESIAN_POINT('',(6.93488877059788,-2.84862442585766,-1.50713517738361));
#22375=CARTESIAN_POINT('Ctrl Pts',(6.93488877059789,-2.84862442585767,-1.5071351773836));
#22376=CARTESIAN_POINT('Ctrl Pts',(6.89082941311706,-2.84862442585767,-1.71164768625373));
#22377=CARTESIAN_POINT('Ctrl Pts',(6.83680262185114,-2.84862442784899,-1.91534068961923));
#22378=CARTESIAN_POINT('Ctrl Pts',(6.72171068862222,-2.84862442784899,-2.29822320309697));
#22379=CARTESIAN_POINT('Ctrl Pts',(6.66085344903225,-2.84862442585767,-2.48067243596248));
#22380=CARTESIAN_POINT('Ctrl Pts',(6.59086343368136,-2.84862442585767,-2.67639318603298));
#22381=CARTESIAN_POINT('Ctrl Pts',(6.58506297100052,-2.84862442585767,-2.69251467300301));
#22382=CARTESIAN_POINT('Ctrl Pts',(6.5792324140922,-2.84862442585767,-2.70862417070381));
#22383=CARTESIAN_POINT('',(7.18143566914408,-2.84862442585767,-1.5071351773836));
#22384=CARTESIAN_POINT('',(13.3346225254169,-2.84862442585767,-1.50713517738359));
#22385=CARTESIAN_POINT('',(7.64603873378328,-2.84683133801731,-2.71029671495572));
#22386=CARTESIAN_POINT('Ctrl Pts',(7.64590487996825,-2.84862442585767,-2.70861444779753));
#22387=CARTESIAN_POINT('Ctrl Pts',(7.63889705165458,-2.84862442585767,-2.69251239752542));
#22388=CARTESIAN_POINT('Ctrl Pts',(7.63190918158326,-2.84862442585767,-2.67640015265958));
#22389=CARTESIAN_POINT('Ctrl Pts',(7.54733015001958,-2.84862442585767,-2.48067802259182));
#22390=CARTESIAN_POINT('Ctrl Pts',(7.47145474188106,-2.84862442740813,-2.29787186609686));
#22391=CARTESIAN_POINT('Ctrl Pts',(7.3222263260763,-2.84862442740813,-1.91581575263515));
#22392=CARTESIAN_POINT('Ctrl Pts',(7.2477176870411,-2.84862442585767,-1.7113528796096));
#22393=CARTESIAN_POINT('Ctrl Pts',(7.18143566914408,-2.84862442585767,-1.50713517738359));
#22394=CARTESIAN_POINT('',(7.82936577676323,-2.84683015106684,-2.71029598749509));
#22395=CARTESIAN_POINT('',(11.0238490761438,-2.84862442585767,-2.71179421793157));
#22396=CARTESIAN_POINT('',(8.18488877059788,-2.84862442585766,-1.50713517738361));
#22397=CARTESIAN_POINT('Ctrl Pts',(8.18488877059787,-2.84862442585767,-1.50713517738361));
#22398=CARTESIAN_POINT('Ctrl Pts',(8.14082943988044,-2.84862442585767,-1.71164756202476));
#22399=CARTESIAN_POINT('Ctrl Pts',(8.08680194594983,-2.84862442785935,-1.91534068721287));
#22400=CARTESIAN_POINT('Ctrl Pts',(7.97170915442048,-2.84862442785935,-2.29822049854839));
#22401=CARTESIAN_POINT('Ctrl Pts',(7.910851677616,-2.84862442585767,-2.48066766373789));
#22402=CARTESIAN_POINT('Ctrl Pts',(7.84086200497834,-2.84862442585767,-2.67638467936083));
#22403=CARTESIAN_POINT('Ctrl Pts',(7.83506196928568,-2.84862442585767,-2.69250475952157));
#22404=CARTESIAN_POINT('Ctrl Pts',(7.82923184430401,-2.84862442585767,-2.70861285213785));
#22405=CARTESIAN_POINT('',(8.43143566914408,-2.84862442585767,-1.5071351773836));
#22406=CARTESIAN_POINT('',(13.3346225254169,-2.84862442585767,-1.50713517738359));
#22407=CARTESIAN_POINT('',(8.89603872959521,-2.84682357725585,-2.71029193875473));
#22408=CARTESIAN_POINT('Ctrl Pts',(8.89590435996554,-2.84862442585767,-2.70860396846321));
#22409=CARTESIAN_POINT('Ctrl Pts',(8.88889701939368,-2.84862442585767,-2.69250319699323));
#22410=CARTESIAN_POINT('Ctrl Pts',(8.881909634102,-2.84862442585767,-2.67639223223817));
#22411=CARTESIAN_POINT('Ctrl Pts',(8.79733122354344,-2.84862442585767,-2.48067356350021));
#22412=CARTESIAN_POINT('Ctrl Pts',(8.72145578136366,-2.84862442741529,-2.29786928082383));
#22413=CARTESIAN_POINT('Ctrl Pts',(8.57222694237506,-2.84862442741529,-1.91581579145778));
#22414=CARTESIAN_POINT('Ctrl Pts',(8.49771763664538,-2.84862442585767,-1.71135272433826));
#22415=CARTESIAN_POINT('Ctrl Pts',(8.43143566914408,-2.84862442585767,-1.50713517738359));
#22416=CARTESIAN_POINT('',(9.07936577364419,-2.84682250133587,-2.71029127282857));
#22417=CARTESIAN_POINT('',(11.0238490761438,-2.84862442585767,-2.71179421793157));
#22418=CARTESIAN_POINT('',(9.43488877059788,-2.84862442585766,-1.5071351773836));
#22419=CARTESIAN_POINT('Ctrl Pts',(9.43488877059788,-2.84862442585767,-1.50713517738359));
#22420=CARTESIAN_POINT('Ctrl Pts',(9.39082946339622,-2.84862442585767,-1.71164745287044));
#22421=CARTESIAN_POINT('Ctrl Pts',(9.33680133416077,-2.8486244278688,-1.91534068162397));
#22422=CARTESIAN_POINT('Ctrl Pts',(9.2217077620153,-2.8486244278688,-2.29821802707406));
#22423=CARTESIAN_POINT('Ctrl Pts',(9.16085007199191,-2.84862442585767,-2.48066329456691));
#22424=CARTESIAN_POINT('Ctrl Pts',(9.09086071058218,-2.84862442585767,-2.67637689747843));
#22425=CARTESIAN_POINT('Ctrl Pts',(9.08506106379369,-2.84862442585767,-2.69249569513711));
#22426=CARTESIAN_POINT('Ctrl Pts',(9.07923133219744,-2.84862442585767,-2.70860250681946));
#22427=CARTESIAN_POINT('',(9.68143566914408,-2.84862442585767,-1.5071351773836));
#22428=CARTESIAN_POINT('',(13.3346225254169,-2.84862442585767,-1.50713517738359));
#22429=CARTESIAN_POINT('',(10.1460387320439,-2.84681652750098,-2.71028755790189));
#22430=CARTESIAN_POINT('Ctrl Pts',(10.1459038904249,-2.84862442585767,-2.70859435034995));
#22431=CARTESIAN_POINT('Ctrl Pts',(10.1388969955833,-2.84862442585767,-2.69249474921214));
#22432=CARTESIAN_POINT('Ctrl Pts',(10.1319100533288,-2.84862442585767,-2.67638495598403));
#22433=CARTESIAN_POINT('Ctrl Pts',(10.0473322072149,-2.84862442585767,-2.48066946312399));
#22434=CARTESIAN_POINT('Ctrl Pts',(9.97145673437474,-2.84862442742187,-2.29786690753779));
#22435=CARTESIAN_POINT('Ctrl Pts',(9.82222750426836,-2.84862442742187,-1.91581582264984));
#22436=CARTESIAN_POINT('Ctrl Pts',(9.74771759182774,-2.84862442585767,-1.71135258625323));
#22437=CARTESIAN_POINT('Ctrl Pts',(9.68143566914409,-2.84862442585767,-1.50713517738361));
#22438=CARTESIAN_POINT('',(10.3293573795468,-2.84839556406923,-2.71178786142128));
#22439=CARTESIAN_POINT('',(11.0238490761438,-2.84862442585767,-2.71179421793157));
#22440=CARTESIAN_POINT('',(10.6848887705979,-2.84862442585766,-1.5071351773836));
#22441=CARTESIAN_POINT('Ctrl Pts',(10.6848887705979,-2.84862442585767,-1.50713517738359));
#22442=CARTESIAN_POINT('Ctrl Pts',(10.6408288271577,-2.84862442585767,-1.71165040613047));
#22443=CARTESIAN_POINT('Ctrl Pts',(10.586823565171,-2.84862442755607,-1.9153402145107));
#22444=CARTESIAN_POINT('Ctrl Pts',(10.4718028413942,-2.84862442755607,-2.29814280868909));
#22445=CARTESIAN_POINT('Ctrl Pts',(10.4110099703332,-2.84862442585767,-2.48048848453579));
#22446=CARTESIAN_POINT('Ctrl Pts',(10.3410124389629,-2.84862442585767,-2.67631715615895));
#22447=CARTESIAN_POINT('Ctrl Pts',(10.3351441403831,-2.84862442585767,-2.69263311564845));
#22448=CARTESIAN_POINT('Ctrl Pts',(10.3292450042586,-2.84862442585767,-2.70893678933792));
#22449=CARTESIAN_POINT('',(13.3346225254169,-2.84862442585767,-1.50713517738359));
#22450=CARTESIAN_POINT('Origin',(3.02384907614375,2.84862442585767,2.80808455720391));
#22451=CARTESIAN_POINT('',(10.6516571958764,2.84853760141617,-2.71188542038896));
#22452=CARTESIAN_POINT('',(11.0238490761438,2.84862442585767,-1.77841863815956));
#22453=CARTESIAN_POINT('Ctrl Pts',(10.6517444165533,2.84862442585767,-2.70958663119422));
#22454=CARTESIAN_POINT('Ctrl Pts',(10.7181155081048,2.84862442585767,-2.5572180519126));
#22455=CARTESIAN_POINT('Ctrl Pts',(10.7831857927431,2.84862442636543,-2.40277143381646));
#22456=CARTESIAN_POINT('Ctrl Pts',(10.9075012055968,2.84862442636543,-2.09344139364087));
#22457=CARTESIAN_POINT('Ctrl Pts',(10.9677673094432,2.84862442585767,-1.93595017012862));
#22458=CARTESIAN_POINT('Ctrl Pts',(11.0238490761437,2.84862442585767,-1.77841863815954));
#22459=CARTESIAN_POINT('',(10.4683323761737,2.84681652750097,-2.71028755790189));
#22460=CARTESIAN_POINT('',(11.0238490761438,2.84862442585767,-2.71179421793157));
#22461=CARTESIAN_POINT('',(10.1128093816896,2.84862442585767,-1.50713517738358));
#22462=CARTESIAN_POINT('Ctrl Pts',(10.1128093816896,2.84862442585767,-1.50713517738361));
#22463=CARTESIAN_POINT('Ctrl Pts',(10.1568589896422,2.84862442585767,-1.71160243138402));
#22464=CARTESIAN_POINT('Ctrl Pts',(10.2108734623886,2.84862442792555,-1.91525078325235));
#22465=CARTESIAN_POINT('Ctrl Pts',(10.3259502311565,2.84862442792555,-2.29808853750365));
#22466=CARTESIAN_POINT('Ctrl Pts',(10.3868075072088,2.84862442585767,-2.48053753211887));
#22467=CARTESIAN_POINT('Ctrl Pts',(10.4568103325124,2.84862442585767,-2.6762925996824));
#22468=CARTESIAN_POINT('Ctrl Pts',(10.4626236619148,2.84862442585767,-2.69244949767383));
#22469=CARTESIAN_POINT('Ctrl Pts',(10.4684672177927,2.84862442585767,-2.70859435034994));
#22470=CARTESIAN_POINT('',(9.86626248314343,2.84862442585767,-1.50713517738359));
#22471=CARTESIAN_POINT('',(13.3346225254169,2.84862442585767,-1.50713517738359));
#22472=CARTESIAN_POINT('',(9.40165942271325,2.8468225013359,-2.71029127282857));
#22473=CARTESIAN_POINT('Ctrl Pts',(9.40179386416001,2.84862442585767,-2.70860250681946));
#22474=CARTESIAN_POINT('Ctrl Pts',(9.40879794213361,2.84862442585767,-2.69250925396209));
#22475=CARTESIAN_POINT('Ctrl Pts',(9.41578208317429,2.84862442585767,-2.67640581787988));
#22476=CARTESIAN_POINT('Ctrl Pts',(9.50035710454219,2.84862442585767,-2.48069591960582));
#22477=CARTESIAN_POINT('Ctrl Pts',(9.57623245461227,2.84862442732866,-2.29789289314525));
#22478=CARTESIAN_POINT('Ctrl Pts',(9.72546495433774,2.84862442732866,-1.91583273517924));
#22479=CARTESIAN_POINT('Ctrl Pts',(9.79997779588513,2.84862442585767,-1.71136110402466));
#22480=CARTESIAN_POINT('Ctrl Pts',(9.86626248314343,2.84862442585767,-1.50713517738359));
#22481=CARTESIAN_POINT('',(9.21833237862236,2.84682357725585,-2.71029193875473));
#22482=CARTESIAN_POINT('',(11.0238490761438,2.84862442585767,-2.71179421793157));
#22483=CARTESIAN_POINT('',(8.86280938168963,2.84862442585767,-1.50713517738358));
#22484=CARTESIAN_POINT('Ctrl Pts',(8.86280938168963,2.84862442585767,-1.5071351773836));
#22485=CARTESIAN_POINT('Ctrl Pts',(8.90685901072075,2.84862442585767,-1.71160252922533));
#22486=CARTESIAN_POINT('Ctrl Pts',(8.96087289825601,2.84862442791668,-1.91525079053687));
#22487=CARTESIAN_POINT('Ctrl Pts',(9.07594894433648,2.84862442791668,-2.29809083397137));
#22488=CARTESIAN_POINT('Ctrl Pts',(9.13680602485858,2.84862442585767,-2.48054159879405));
#22489=CARTESIAN_POINT('Ctrl Pts',(9.20680913788998,2.84862442585767,-2.67629983902876));
#22490=CARTESIAN_POINT('Ctrl Pts',(9.21262282775703,2.84862442585767,-2.69245792713028));
#22491=CARTESIAN_POINT('Ctrl Pts',(9.21846674825203,2.84862442585767,-2.70860396846321));
#22492=CARTESIAN_POINT('',(8.61626248314343,2.84862442585767,-1.50713517738359));
#22493=CARTESIAN_POINT('',(13.3346225254169,2.84862442585767,-1.50713517738359));
#22494=CARTESIAN_POINT('',(8.15165941959421,2.84683015106688,-2.71029598749509));
#22495=CARTESIAN_POINT('Ctrl Pts',(8.15179335205343,2.84862442585767,-2.70861285213785));
#22496=CARTESIAN_POINT('Ctrl Pts',(8.15879791114812,2.84862442585767,-2.69251833761412));
#22497=CARTESIAN_POINT('Ctrl Pts',(8.16578253039036,2.84862442585767,-2.67641363857816));
#22498=CARTESIAN_POINT('Ctrl Pts',(8.25035816386072,2.84862442585767,-2.48070032366843));
#22499=CARTESIAN_POINT('Ctrl Pts',(8.32623348041883,2.84862442732179,-2.29789544620645));
#22500=CARTESIAN_POINT('Ctrl Pts',(8.47546556201146,2.84862442732179,-1.91583269807888));
#22501=CARTESIAN_POINT('Ctrl Pts',(8.54997774627531,2.84862442585767,-1.71136125687463));
#22502=CARTESIAN_POINT('Ctrl Pts',(8.61626248314343,2.84862442585767,-1.50713517738358));
#22503=CARTESIAN_POINT('',(7.9683323744343,2.84683133801736,-2.71029671495571));
#22504=CARTESIAN_POINT('',(11.0238490761438,2.84862442585767,-2.71179421793157));
#22505=CARTESIAN_POINT('',(7.61280938168963,2.84862442585767,-1.50713517738358));
#22506=CARTESIAN_POINT('Ctrl Pts',(7.61280938168963,2.84862442585767,-1.5071351773836));
#22507=CARTESIAN_POINT('Ctrl Pts',(7.65685903460308,2.84862442585767,-1.71160264008112));
#22508=CARTESIAN_POINT('Ctrl Pts',(7.71087227780285,2.84862442790699,-1.91525079518883));
#22509=CARTESIAN_POINT('Ctrl Pts',(7.82594753272231,2.84862442790699,-2.29809333657086));
#22510=CARTESIAN_POINT('Ctrl Pts',(7.88680439671883,2.84862442585767,-2.48054602253814));
#22511=CARTESIAN_POINT('Ctrl Pts',(7.9568078251961,2.84862442585767,-2.67630772013523));
#22512=CARTESIAN_POINT('Ctrl Pts',(7.96262190913101,2.84862442585767,-2.69246710814726));
#22513=CARTESIAN_POINT('Ctrl Pts',(7.96846622824932,2.84862442585767,-2.70861444779752));
#22514=CARTESIAN_POINT('',(7.36626248314343,2.84862442585767,-1.50713517738359));
#22515=CARTESIAN_POINT('',(13.3346225254169,2.84862442585767,-1.50713517738359));
#22516=CARTESIAN_POINT('',(6.90165940842906,2.84683861010255,-2.71030114914197));
#22517=CARTESIAN_POINT('Ctrl Pts',(6.90179278226525,2.84862442585767,-2.70862417070381));
#22518=CARTESIAN_POINT('Ctrl Pts',(6.90879787011014,2.84862442585767,-2.69252827167807));
#22519=CARTESIAN_POINT('Ctrl Pts',(6.91578301488098,2.84862442585767,-2.67642218671447));
#22520=CARTESIAN_POINT('Ctrl Pts',(7.00035932483387,2.84862442585767,-2.48070513252597));
#22521=CARTESIAN_POINT('Ctrl Pts',(7.07623460400956,2.84862442731428,-2.29789823886797));
#22522=CARTESIAN_POINT('Ctrl Pts',(7.2254662314708,2.84862442731428,-1.91583265203173));
#22523=CARTESIAN_POINT('Ctrl Pts',(7.29997769023056,2.84862442585767,-1.71136142955089));
#22524=CARTESIAN_POINT('Ctrl Pts',(7.36626248314343,2.84862442585767,-1.50713517738359));
#22525=CARTESIAN_POINT('',(6.71833236192707,2.84683992679534,-2.71030194794594));
#22526=CARTESIAN_POINT('',(11.0238490761438,2.84862442585767,-2.71179421793157));
#22527=CARTESIAN_POINT('',(6.36280938168963,2.84862442585767,-1.50713517738358));
#22528=CARTESIAN_POINT('Ctrl Pts',(6.36280938168963,2.84862442585767,-1.50713517738361));
#22529=CARTESIAN_POINT('Ctrl Pts',(6.40685906180869,2.84862442585767,-1.71160276636274));
#22530=CARTESIAN_POINT('Ctrl Pts',(6.46087159177102,2.84862442789636,-1.91525079649567));
#22531=CARTESIAN_POINT('Ctrl Pts',(6.57594597610578,2.84862442789636,-2.29809607725535));
#22532=CARTESIAN_POINT('Ctrl Pts',(6.63680259900565,2.84862442585767,-2.48055085796017));
#22533=CARTESIAN_POINT('Ctrl Pts',(6.70680637511918,2.84862442585767,-2.67631634173415));
#22534=CARTESIAN_POINT('Ctrl Pts',(6.71262089204982,2.84862442585767,-2.69247715675436));
#22535=CARTESIAN_POINT('Ctrl Pts',(6.7184656491878,2.84862442585767,-2.70862592165798));
#22536=CARTESIAN_POINT('',(6.11626248314343,2.84862442585767,-1.50713517738359));
#22537=CARTESIAN_POINT('',(13.3346225254169,2.84862442585767,-1.50713517738359));
#22538=CARTESIAN_POINT('',(5.65165938714153,2.84684801847819,-2.71030683105326));
#22539=CARTESIAN_POINT('Ctrl Pts',(5.6517921444683,2.84862442585767,-2.70863662146848));
#22540=CARTESIAN_POINT('Ctrl Pts',(5.65879781670129,2.84862442585767,-2.69253919463776));
#22541=CARTESIAN_POINT('Ctrl Pts',(5.66578354227913,2.84862442585766,-2.67643158029353));
#22542=CARTESIAN_POINT('Ctrl Pts',(5.75036060425611,2.84862442585766,-2.48071041137392));
#22543=CARTESIAN_POINT('Ctrl Pts',(5.82623584147821,2.84862442730604,-2.29790131019802));
#22544=CARTESIAN_POINT('Ctrl Pts',(5.97546697324722,2.84862442730604,-1.91583259505172));
#22545=CARTESIAN_POINT('Ctrl Pts',(6.04997762653236,2.84862442585767,-1.71136162580774));
#22546=CARTESIAN_POINT('Ctrl Pts',(6.11626248314343,2.84862442585767,-1.50713517738359));
#22547=CARTESIAN_POINT('',(5.46833233894627,2.84684948813853,-2.71030771333066));
#22548=CARTESIAN_POINT('',(11.0238490761438,2.84862442585767,-2.71179421793157));
#22549=CARTESIAN_POINT('',(5.11280938168963,2.84862442585767,-1.50713517738358));
#22550=CARTESIAN_POINT('Ctrl Pts',(5.11280938168963,2.84862442585767,-1.50713517738362));
#22551=CARTESIAN_POINT('Ctrl Pts',(5.15685909298675,2.84862442585767,-1.7116029110835));
#22552=CARTESIAN_POINT('Ctrl Pts',(5.2108708287094,2.84862442788461,-1.91525079354619));
#22553=CARTESIAN_POINT('Ctrl Pts',(5.3259442495258,2.84862442788461,-2.2980990953389));
#22554=CARTESIAN_POINT('Ctrl Pts',(5.38680060232149,2.84862442585766,-2.48055617216051));
#22555=CARTESIAN_POINT('Ctrl Pts',(5.45680476378349,2.84862442585766,-2.67632582520572));
#22556=CARTESIAN_POINT('Ctrl Pts',(5.46261975920138,2.84862442585767,-2.69248821564317));
#22557=CARTESIAN_POINT('Ctrl Pts',(5.46846500040038,2.84862442585767,-2.70863855402171));
#22558=CARTESIAN_POINT('',(4.86626248314343,2.84862442585767,-1.50713517738359));
#22559=CARTESIAN_POINT('',(13.3346225254169,2.84862442585767,-1.50713517738359));
#22560=CARTESIAN_POINT('',(4.40165935304722,2.84685855096331,-2.71031312437897));
#22561=CARTESIAN_POINT('Ctrl Pts',(4.40179142571374,2.84862442585767,-2.7086504020624));
#22562=CARTESIAN_POINT('Ctrl Pts',(4.40879774794817,2.84862442585767,-2.69255127864938));
#22563=CARTESIAN_POINT('Ctrl Pts',(4.41578411952675,2.84862442585767,-2.67644196595571));
#22564=CARTESIAN_POINT('Ctrl Pts',(4.50036202302706,2.84862442585767,-2.48071624117288));
#22565=CARTESIAN_POINT('Ctrl Pts',(4.5762372128446,2.84862442729694,-2.29790470877537));
#22566=CARTESIAN_POINT('Ctrl Pts',(4.72546780048414,2.84862442729694,-1.91583252461549));
#22567=CARTESIAN_POINT('Ctrl Pts',(4.79997755364427,2.84862442585767,-1.71136185037904));
#22568=CARTESIAN_POINT('Ctrl Pts',(4.86626248314343,2.84862442585767,-1.50713517738359));
#22569=CARTESIAN_POINT('',(4.21833230270155,2.8468602027841,-2.71031410533046));
#22570=CARTESIAN_POINT('',(11.0238490761438,2.84862442585767,-2.71179421793157));
#22571=CARTESIAN_POINT('',(3.86280938168963,2.84862442585767,-1.50713517738358));
#22572=CARTESIAN_POINT('Ctrl Pts',(3.86280938168963,2.84862442585767,-1.50713517738361));
#22573=CARTESIAN_POINT('Ctrl Pts',(3.90685912895696,2.84862442585767,-1.71160307804822));
#22574=CARTESIAN_POINT('Ctrl Pts',(3.9608699742735,2.84862442787157,-1.91525078515163));
#22575=CARTESIAN_POINT('Ctrl Pts',(4.07594232175518,2.84862442787157,-2.29810243978791));
#22576=CARTESIAN_POINT('Ctrl Pts',(4.13679836986563,2.84862442585768,-2.48056204862024));
#22577=CARTESIAN_POINT('Ctrl Pts',(4.20680296129537,2.84862442585768,-2.67633632166697));
#22578=CARTESIAN_POINT('Ctrl Pts',(4.21261848888836,2.84862442585767,-2.69250046252893));
#22579=CARTESIAN_POINT('Ctrl Pts',(4.21846426848655,2.84862442585767,-2.70865254916597));
#22580=CARTESIAN_POINT('',(3.61626248314343,2.84862442585767,-1.50713517738359));
#22581=CARTESIAN_POINT('',(13.3346225254169,2.84862442585767,-1.50713517738359));
#22582=CARTESIAN_POINT('',(3.15165930263079,2.84687042859227,-2.71032014408668));
#22583=CARTESIAN_POINT('Ctrl Pts',(3.15179060954266,2.84862442585767,-2.70866576166606));
#22584=CARTESIAN_POINT('Ctrl Pts',(3.15879766001169,2.84862442585767,-2.69256474069428));
#22585=CARTESIAN_POINT('Ctrl Pts',(3.1657847553136,2.84862442585768,-2.6764535284648));
#22586=CARTESIAN_POINT('Ctrl Pts',(3.25036360752406,2.84862442585768,-2.48072272386991));
#22587=CARTESIAN_POINT('Ctrl Pts',(3.32623874336682,2.84862442728679,-2.29790849584301));
#22588=CARTESIAN_POINT('Ctrl Pts',(3.4754687298166,2.84862442728679,-1.91583243746613));
#22589=CARTESIAN_POINT('Ctrl Pts',(3.54997746960448,2.84862442585767,-1.71136210930917));
#22590=CARTESIAN_POINT('Ctrl Pts',(3.61626248314343,2.84862442585767,-1.50713517738359));
#22591=CARTESIAN_POINT('',(3.02384907614375,2.84862442585767,-2.71179421793157));
#22592=CARTESIAN_POINT('',(11.0238490761438,2.84862442585767,-2.71179421793157));
#22593=CARTESIAN_POINT('',(3.02384907614375,2.84862442585767,2.11350930841789));
#22594=CARTESIAN_POINT('',(3.02384907614375,2.84862442585767,1.40404227860195));
#22595=CARTESIAN_POINT('',(3.27104142627809,2.84862444224244,2.71179420072006));
#22596=CARTESIAN_POINT('Ctrl Pts',(3.27100497985698,2.84862442585767,2.71079938718163));
#22597=CARTESIAN_POINT('Ctrl Pts',(3.228076353399,2.84862442585767,2.61225572759565));
#22598=CARTESIAN_POINT('Ctrl Pts',(3.18578823704266,2.84862442598707,2.51303020389064));
#22599=CARTESIAN_POINT('Ctrl Pts',(3.10334913028736,2.84862442598707,2.31421002248986));
#22600=CARTESIAN_POINT('Ctrl Pts',(3.06291723376633,2.84862442585767,2.21392684695503));
#22601=CARTESIAN_POINT('Ctrl Pts',(3.02384907614376,2.84862442585767,2.11350930841789));
#22602=CARTESIAN_POINT('',(3.45436586621803,2.84686430560626,2.71031653510883));
#22603=CARTESIAN_POINT('',(11.0238490761438,2.84862442585767,2.71179421793157));
#22604=CARTESIAN_POINT('',(3.80988877059788,2.84862442585767,1.5071351773836));
#22605=CARTESIAN_POINT('Ctrl Pts',(3.80988877059788,2.84862442585767,1.5071351773836));
#22606=CARTESIAN_POINT('Ctrl Pts',(3.7658293274531,2.84862442585767,1.71164808388438));
#22607=CARTESIAN_POINT('Ctrl Pts',(3.7118046719511,2.84862442781797,1.9153406753387));
#22608=CARTESIAN_POINT('Ctrl Pts',(3.59671531847852,2.84862442781797,2.29823125790659));
#22609=CARTESIAN_POINT('Ctrl Pts',(3.53585880786088,2.84862442585766,2.48068659685609));
#22610=CARTESIAN_POINT('Ctrl Pts',(3.46586775948282,2.84862442585766,2.67641846844891));
#22611=CARTESIAN_POINT('Ctrl Pts',(3.46006601698536,2.84862442585767,2.69254416467973));
#22612=CARTESIAN_POINT('Ctrl Pts',(3.45423416535493,2.84862442585767,2.7086578664456));
#22613=CARTESIAN_POINT('',(4.05643566914408,2.84862442585766,1.50713517738361));
#22614=CARTESIAN_POINT('',(13.3346225254169,2.84862442585767,1.50713517738359));
#22615=CARTESIAN_POINT('',(4.52103878553064,2.84685468828742,2.71031082423224));
#22616=CARTESIAN_POINT('Ctrl Pts',(4.52090646241579,2.84862442585767,2.70864536656847));
#22617=CARTESIAN_POINT('Ctrl Pts',(4.51389718302579,2.84862442585767,2.69253952221217));
#22618=CARTESIAN_POINT('Ctrl Pts',(4.50690787077022,2.84862442585768,2.67642347934393));
#22619=CARTESIAN_POINT('Ctrl Pts',(4.42232697249459,2.84862442585768,2.48069113060106));
#22620=CARTESIAN_POINT('Ctrl Pts',(4.34645166843461,2.84862442738707,2.29787949083546));
#22621=CARTESIAN_POINT('Ctrl Pts',(4.19722448429369,2.84862442738707,1.91581561039782));
#22622=CARTESIAN_POINT('Ctrl Pts',(4.12271784469148,2.84862442585767,1.7113533653371));
#22623=CARTESIAN_POINT('Ctrl Pts',(4.05643566914409,2.84862442585767,1.50713517738361));
#22624=CARTESIAN_POINT('',(4.70436582446518,2.84685313164041,2.71030989474673));
#22625=CARTESIAN_POINT('',(11.0238490761438,2.84862442585767,2.71179421793157));
#22626=CARTESIAN_POINT('',(5.05988877059788,2.84862442585767,1.5071351773836));
#22627=CARTESIAN_POINT('Ctrl Pts',(5.05988877059787,2.84862442585767,1.50713517738362));
#22628=CARTESIAN_POINT('Ctrl Pts',(5.01582936546295,2.84862442585767,1.71164790745213));
#22629=CARTESIAN_POINT('Ctrl Pts',(4.96180378091768,2.84862442783138,1.91534068528627));
#22630=CARTESIAN_POINT('Ctrl Pts',(4.84671331029461,2.84862442783138,2.29822778278234));
#22631=CARTESIAN_POINT('Ctrl Pts',(4.78585648120188,2.84862442585767,2.48068049652974));
#22632=CARTESIAN_POINT('Ctrl Pts',(4.71586588068668,2.84862442585767,2.6764075700122));
#22633=CARTESIAN_POINT('Ctrl Pts',(4.71006469178374,2.84862442585767,2.69253144678897));
#22634=CARTESIAN_POINT('Ctrl Pts',(4.70423340021296,2.84862442585767,2.70864333135427));
#22635=CARTESIAN_POINT('',(5.30643566914408,2.84862442585766,1.50713517738361));
#22636=CARTESIAN_POINT('',(13.3346225254169,2.84862442585767,1.50713517738359));
#22637=CARTESIAN_POINT('',(5.77103875631455,2.8468445755701,2.71030475869924));
#22638=CARTESIAN_POINT('Ctrl Pts',(5.77090577394363,2.84862442585767,2.70863208133986));
#22639=CARTESIAN_POINT('Ctrl Pts',(5.7638971201788,2.84862442585767,2.69252787095137));
#22640=CARTESIAN_POINT('Ctrl Pts',(5.75690842970124,2.84862442585768,2.67641346374591));
#22641=CARTESIAN_POINT('Ctrl Pts',(5.67232833961162,2.84862442585768,2.48068550687512));
#22642=CARTESIAN_POINT('Ctrl Pts',(5.59645299018697,2.84862442739611,2.29787621515313));
#22643=CARTESIAN_POINT('Ctrl Pts',(5.44722527981436,2.84862442739611,1.91581567641076));
#22644=CARTESIAN_POINT('Ctrl Pts',(5.3727177753678,2.84862442585767,1.71135315174791));
#22645=CARTESIAN_POINT('Ctrl Pts',(5.30643566914408,2.84862442585767,1.5071351773836));
#22646=CARTESIAN_POINT('',(5.95436579715553,2.84684318562971,2.71030391984611));
#22647=CARTESIAN_POINT('',(11.0238490761438,2.84862442585767,2.71179421793157));
#22648=CARTESIAN_POINT('',(6.30988877059788,2.84862442585767,1.5071351773836));
#22649=CARTESIAN_POINT('Ctrl Pts',(6.30988877059789,2.84862442585767,1.5071351773836));
#22650=CARTESIAN_POINT('Ctrl Pts',(6.2658293983268,2.84862442585767,1.71164775490643));
#22651=CARTESIAN_POINT('Ctrl Pts',(6.21180298721187,2.84862442784341,1.91534068936543));
#22652=CARTESIAN_POINT('Ctrl Pts',(6.09671151624063,2.84862442784341,2.29822465435504));
#22653=CARTESIAN_POINT('Ctrl Pts',(6.03585440555947,2.84862442585767,2.48067499299047));
#22654=CARTESIAN_POINT('Ctrl Pts',(5.96586420541966,2.84862442585767,2.67639774691987));
#22655=CARTESIAN_POINT('Ctrl Pts',(5.96006351303068,2.84862442585767,2.69251999018277));
#22656=CARTESIAN_POINT('Ctrl Pts',(5.95423272375062,2.84862442585767,2.70863024324505));
#22657=CARTESIAN_POINT('',(6.55643566914408,2.84862442585766,1.50713517738361));
#22658=CARTESIAN_POINT('',(13.3346225254169,2.84862442585767,1.50713517738359));
#22659=CARTESIAN_POINT('',(7.02103873887505,2.84683552060301,2.71029927000383));
#22660=CARTESIAN_POINT('Ctrl Pts',(7.02090516150519,2.84862442585767,2.70862005097967));
#22661=CARTESIAN_POINT('Ctrl Pts',(7.01389707152942,2.84862442585767,2.69251731541987));
#22662=CARTESIAN_POINT('Ctrl Pts',(7.0069089413909,2.84862442585767,2.67640438456248));
#22663=CARTESIAN_POINT('Ctrl Pts',(6.92232957528187,2.84862442585767,2.48068040331129));
#22664=CARTESIAN_POINT('Ctrl Pts',(6.84645418560907,2.84862442740432,2.29787324819636));
#22665=CARTESIAN_POINT('Ctrl Pts',(6.6972259948484,2.84862442740432,1.91581572986742));
#22666=CARTESIAN_POINT('Ctrl Pts',(6.62271771463721,2.84862442585767,1.71135296463439));
#22667=CARTESIAN_POINT('Ctrl Pts',(6.55643566914408,2.84862442585767,1.5071351773836));
#22668=CARTESIAN_POINT('',(7.20436578122244,2.84683427137383,2.71029850822801));
#22669=CARTESIAN_POINT('',(11.0238490761438,2.84862442585767,2.71179421793157));
#22670=CARTESIAN_POINT('',(7.55988877059788,2.84862442585767,1.5071351773836));
#22671=CARTESIAN_POINT('Ctrl Pts',(7.55988877059788,2.84862442585767,1.5071351773836));
#22672=CARTESIAN_POINT('Ctrl Pts',(7.51582942694069,2.84862442585767,1.71164762208787));
#22673=CARTESIAN_POINT('Ctrl Pts',(7.46180227524923,2.84862442785429,1.91534068886327));
#22674=CARTESIAN_POINT('Ctrl Pts',(7.34670990240678,2.84862442785429,2.29822181949426));
#22675=CARTESIAN_POINT('Ctrl Pts',(7.28585254096374,2.84862442585767,2.48066999572136));
#22676=CARTESIAN_POINT('Ctrl Pts',(7.2158627012126,2.84862442585767,2.67638883532302));
#22677=CARTESIAN_POINT('Ctrl Pts',(7.21006245715211,2.84862442585767,2.69250960216246));
#22678=CARTESIAN_POINT('Ctrl Pts',(7.20423212139549,2.84862442585767,2.70861838061489));
#22679=CARTESIAN_POINT('',(7.80643566914408,2.84862442585766,1.50713517738361));
#22680=CARTESIAN_POINT('',(13.3346225254169,2.84862442585767,1.50713517738359));
#22681=CARTESIAN_POINT('',(8.271038730764,2.84682736201001,2.71029427388594));
#22682=CARTESIAN_POINT('Ctrl Pts',(8.27090461316402,2.84862442585767,2.70860909277273));
#22683=CARTESIAN_POINT('Ctrl Pts',(8.26389703435909,2.84862442585767,2.69250769644918));
#22684=CARTESIAN_POINT('Ctrl Pts',(8.25690941227972,2.84862442585767,2.67639610620256));
#22685=CARTESIAN_POINT('Ctrl Pts',(8.17233069882605,2.84862442585767,2.48067574504101));
#22686=CARTESIAN_POINT('Ctrl Pts',(8.0964552732107,2.84862442741179,2.29787054506796));
#22687=CARTESIAN_POINT('Ctrl Pts',(7.94722664153419,2.84862442741179,1.91581577309339));
#22688=CARTESIAN_POINT('Ctrl Pts',(7.87271766108794,2.84862442585767,1.71135279964682));
#22689=CARTESIAN_POINT('Ctrl Pts',(7.80643566914409,2.84862442585767,1.50713517738362));
#22690=CARTESIAN_POINT('',(8.45436577430856,2.84682623267637,2.71029357829656));
#22691=CARTESIAN_POINT('',(11.0238490761438,2.84862442585767,2.71179421793157));
#22692=CARTESIAN_POINT('',(8.80988877059788,2.84862442585767,1.50713517738359));
#22693=CARTESIAN_POINT('Ctrl Pts',(8.80988877059788,2.84862442585767,1.50713517738359));
#22694=CARTESIAN_POINT('Ctrl Pts',(8.76582945201024,2.84862442585767,1.7116475057213));
#22695=CARTESIAN_POINT('Ctrl Pts',(8.71180163264592,2.84862442786418,1.91534068476964));
#22696=CARTESIAN_POINT('Ctrl Pts',(8.59670844181264,2.84862442786418,2.29821923576154));
#22697=CARTESIAN_POINT('Ctrl Pts',(8.53585085563285,2.84862442585767,2.48066543233191));
#22698=CARTESIAN_POINT('Ctrl Pts',(8.46586134225275,2.84862442585767,2.67638070425965));
#22699=CARTESIAN_POINT('Ctrl Pts',(8.46006150542514,2.84862442585767,2.69250012875935));
#22700=CARTESIAN_POINT('Ctrl Pts',(8.45423158160217,2.84862442585767,2.70860756651644));
#22701=CARTESIAN_POINT('',(9.05643566914408,2.84862442585766,1.50713517738361));
#22702=CARTESIAN_POINT('',(13.3346225254169,2.84862442585767,1.50713517738359));
#22703=CARTESIAN_POINT('',(9.52103873008012,2.84681996992432,2.71028970229123));
#22704=CARTESIAN_POINT('Ctrl Pts',(9.52090411935796,2.84862442585767,2.70859905909218));
#22705=CARTESIAN_POINT('Ctrl Pts',(9.51389700653417,2.84862442585767,2.69249888540408));
#22706=CARTESIAN_POINT('Ctrl Pts',(9.50690984761346,2.84862442585768,2.67638851904301));
#22707=CARTESIAN_POINT('Ctrl Pts',(9.42233172583661,2.84862442585768,2.48067147148852));
#22708=CARTESIAN_POINT('Ctrl Pts',(9.3464562679359,2.84862442741865,2.29786806948615));
#22709=CARTESIAN_POINT('Ctrl Pts',(9.19722722963917,2.84862442741865,1.9158158079193));
#22710=CARTESIAN_POINT('Ctrl Pts',(9.12271761359435,2.84862442585767,1.71135265331708));
#22711=CARTESIAN_POINT('Ctrl Pts',(9.05643566914409,2.84862442585767,1.50713517738362));
#22712=CARTESIAN_POINT('',(9.70436577458009,2.8468189436181,2.71028906402778));
#22713=CARTESIAN_POINT('',(11.0238490761438,2.84862442585767,2.71179421793157));
#22714=CARTESIAN_POINT('',(10.0598887705979,2.84862442585767,1.50713517738359));
#22715=CARTESIAN_POINT('Ctrl Pts',(10.0598887705979,2.84862442585767,1.50713517738359));
#22716=CARTESIAN_POINT('Ctrl Pts',(10.0158294740978,2.84862442585767,1.71164740319615));
#22717=CARTESIAN_POINT('Ctrl Pts',(9.96180104943227,2.84862442787322,1.91534067785543));
#22718=CARTESIAN_POINT('Ctrl Pts',(9.84670711270893,2.84862442787322,2.29821686881042));
#22719=CARTESIAN_POINT('Ctrl Pts',(9.78584932396424,2.84862442585767,2.48066124415883));
#22720=CARTESIAN_POINT('Ctrl Pts',(9.71586010775059,2.84862442585767,2.67637324766241));
#22721=CARTESIAN_POINT('Ctrl Pts',(9.71006064278651,2.84862442585767,2.69249144531452));
#22722=CARTESIAN_POINT('Ctrl Pts',(9.70423109510515,2.84862442585767,2.70859765771964));
#22723=CARTESIAN_POINT('',(10.3064356691441,2.84862442585766,1.50713517738361));
#22724=CARTESIAN_POINT('',(13.3346225254169,2.84862442585767,1.50713517738359));
#22725=CARTESIAN_POINT('',(10.771038735331,2.84681323863445,2.71028549959174));
#22726=CARTESIAN_POINT('Ctrl Pts',(10.7709036723368,2.84862442585767,2.70858982922371));
#22727=CARTESIAN_POINT('Ctrl Pts',(10.7638969863635,2.84862442585767,2.69249077707409));
#22728=CARTESIAN_POINT('Ctrl Pts',(10.7569102517173,2.84862442585767,2.67638153338721));
#22729=CARTESIAN_POINT('Ctrl Pts',(10.6723326690498,2.84862442585767,2.48066753305333));
#22730=CARTESIAN_POINT('Ctrl Pts',(10.5964571819956,2.84862442742496,2.29786579177956));
#22731=CARTESIAN_POINT('Ctrl Pts',(10.4472277671172,2.84862442742496,1.91581583580293));
#22732=CARTESIAN_POINT('Ctrl Pts',(10.3727175712488,2.84862442585767,1.71135252284851));
#22733=CARTESIAN_POINT('Ctrl Pts',(10.3064356691441,2.84862442585767,1.5071351773836));
#22734=CARTESIAN_POINT('',(10.9543681768003,2.84860418144656,2.71177492056083));
#22735=CARTESIAN_POINT('',(11.0238490761438,2.84862442585767,2.71179421793157));
#22736=CARTESIAN_POINT('',(11.0238490761438,2.84862442585767,2.5145657703754));
#22737=CARTESIAN_POINT('Ctrl Pts',(11.0238490761438,2.84862442585767,2.51456577037539));
#22738=CARTESIAN_POINT('Ctrl Pts',(11.0125388019847,2.84862442585767,2.54755700411209));
#22739=CARTESIAN_POINT('Ctrl Pts',(11.0010794330984,2.84862442585774,2.58050639119045));
#22740=CARTESIAN_POINT('Ctrl Pts',(10.9781080325486,2.84862442585774,2.6456791051022));
#22741=CARTESIAN_POINT('Ctrl Pts',(10.9665953160741,2.84862442585767,2.67792052124666));
#22742=CARTESIAN_POINT('Ctrl Pts',(10.9547630945647,2.84862442585767,2.71065726237697));
#22743=CARTESIAN_POINT('Ctrl Pts',(10.9545649113151,2.84862442585767,2.71120547217373));
#22744=CARTESIAN_POINT('Ctrl Pts',(10.9543666920789,2.84862442585767,2.71175366890678));
#22745=CARTESIAN_POINT('',(11.0238490761438,2.84862442585767,-6.75363122348402));
#22746=CARTESIAN_POINT('Origin',(13.3346225254169,0.,0.));
#22747=CARTESIAN_POINT('',(3.02386560100257,-0.0279675576018124,3.22262864416951));
#22748=CARTESIAN_POINT('Ctrl Pts',(3.23780938168963,-2.84862442585767,1.50713517738358));
#22749=CARTESIAN_POINT('Ctrl Pts',(3.2313463182794,-2.79966227599299,1.5996781543773));
#22750=CARTESIAN_POINT('Ctrl Pts',(3.22488325486918,-2.74617683440501,1.68985168048399));
#22751=CARTESIAN_POINT('Ctrl Pts',(3.21842019145895,-2.68842250870076,1.77721748168622));
#22752=CARTESIAN_POINT('Ctrl Pts',(3.21195831309532,-2.63067877264464,1.86456726377506));
#22753=CARTESIAN_POINT('Ctrl Pts',(3.20549643473169,-2.56866791940005,1.94911003510213));
#22754=CARTESIAN_POINT('Ctrl Pts',(3.19903455636806,-2.50268804578698,2.03043594037708));
#22755=CARTESIAN_POINT('Ctrl Pts',(3.19257306896931,-2.43671216417302,2.11175692516759));
#22756=CARTESIAN_POINT('Ctrl Pts',(3.18611158157055,-2.36676797758294,2.18986114188401));
#22757=CARTESIAN_POINT('Ctrl Pts',(3.17965009417179,-2.29319407993019,2.26437154068698));
#22758=CARTESIAN_POINT('Ctrl Pts',(3.17318610757495,-2.2195917250922,2.33891075889858));
#22759=CARTESIAN_POINT('Ctrl Pts',(3.16672212097811,-2.14235711490485,2.409853112714));
#22760=CARTESIAN_POINT('Ctrl Pts',(3.16025813438127,-2.06186607637872,2.47685805923121));
#22761=CARTESIAN_POINT('Ctrl Pts',(3.15379347444796,-1.98136665331285,2.54386998547744));
#22762=CARTESIAN_POINT('Ctrl Pts',(3.14732881451464,-1.89761041744266,2.60694345163933));
#22763=CARTESIAN_POINT('Ctrl Pts',(3.14086415458132,-1.81100596096446,2.66577849264548));
#22764=CARTESIAN_POINT('Ctrl Pts',(3.13439513068962,-1.72434304228595,2.72465325015229));
#22765=CARTESIAN_POINT('Ctrl Pts',(3.12792610679791,-1.63482837237314,2.77928365617125));
#22766=CARTESIAN_POINT('Ctrl Pts',(3.12145708290621,-1.54289948435689,2.82941314474773));
#22767=CARTESIAN_POINT('Ctrl Pts',(3.11566378858085,-1.46057313741543,2.87430629811445));
#22768=CARTESIAN_POINT('Ctrl Pts',(3.1098704942555,-1.37631113062514,2.91559022856466));
#22769=CARTESIAN_POINT('Ctrl Pts',(3.10407719993014,-1.29044359936636,2.9531124054723));
#22770=CARTESIAN_POINT('Ctrl Pts',(3.09739290001951,-1.19136968748049,2.99640547322698));
#22771=CARTESIAN_POINT('Ctrl Pts',(3.09070860010888,-1.0900490626428,3.03473683538019));
#22772=CARTESIAN_POINT('Ctrl Pts',(3.08402430019824,-0.987005187934864,
3.06788825114111));
#22773=CARTESIAN_POINT('Ctrl Pts',(3.07764680269255,-0.8886909197672,3.09951805144215));
#22774=CARTESIAN_POINT('Ctrl Pts',(3.07126930518686,-0.788808504705706,
3.12643274001858));
#22775=CARTESIAN_POINT('Ctrl Pts',(3.06489180768116,-0.687831587946816,
3.14849253915625));
#22776=CARTESIAN_POINT('Ctrl Pts',(3.05851704894084,-0.586898034918329,
3.17054286488937));
#22777=CARTESIAN_POINT('Ctrl Pts',(3.05214229020051,-0.484871300248373,
3.18774237030377));
#22778=CARTESIAN_POINT('Ctrl Pts',(3.04576753146018,-0.382237297735694,
3.20000190792439));
#22779=CARTESIAN_POINT('Ctrl Pts',(3.03939415566387,-0.279625560705552,
3.2122587859535));
#22780=CARTESIAN_POINT('Ctrl Pts',(3.03302077986756,-0.176407208550043,
3.2195777843509));
#22781=CARTESIAN_POINT('Ctrl Pts',(3.02664740407124,-0.0730749405909518,
3.22192141672599));
#22782=CARTESIAN_POINT('Ctrl Pts',(3.02572013638169,-0.0580410438885451,
3.22226239372893));
#22783=CARTESIAN_POINT('Ctrl Pts',(3.02479286869213,-0.0430047421599852,
3.22249814408038));
#22784=CARTESIAN_POINT('Ctrl Pts',(3.02386560100257,-0.0279675576018124,
3.22262864416951));
#22785=CARTESIAN_POINT('Origin',(3.02384907614375,0.,0.));
#22786=CARTESIAN_POINT('Origin',(13.3346225254169,0.,0.));
#22787=CARTESIAN_POINT('Ctrl Pts',(3.61626248314343,2.84862442585767,-1.50713517738359));
#22788=CARTESIAN_POINT('Ctrl Pts',(3.60981814030002,2.79980409716038,-1.59941009929665));
#22789=CARTESIAN_POINT('Ctrl Pts',(3.6033737974566,2.74648418316931,-1.68933387103504));
#22790=CARTESIAN_POINT('Ctrl Pts',(3.59692945461318,2.68891651929892,-1.77646995886263));
#22791=CARTESIAN_POINT('Ctrl Pts',(3.59048653183097,2.63136154091221,-1.86358684557373));
#22792=CARTESIAN_POINT('Ctrl Pts',(3.58404360904876,2.56956088675986,-1.94791695677699));
#22793=CARTESIAN_POINT('Ctrl Pts',(3.57760068626655,2.50381017084846,-2.02905204242173));
#22794=CARTESIAN_POINT('Ctrl Pts',(3.57115830034015,2.438064933608,-2.11018036749468));
#22795=CARTESIAN_POINT('Ctrl Pts',(3.56471591441375,2.36837052961789,-2.1881139039722));
#22796=CARTESIAN_POINT('Ctrl Pts',(3.55827352848734,2.29506314790585,-2.26247711803335));
#22797=CARTESIAN_POINT('Ctrl Pts',(3.5518307966975,2.22175183064207,-2.33684432432924));
#22798=CARTESIAN_POINT('Ctrl Pts',(3.54538806490766,2.14482741599023,-2.40764055767011));
#22799=CARTESIAN_POINT('Ctrl Pts',(3.53894533311782,2.06466301231591,-2.47452706755748));
#22800=CARTESIAN_POINT('Ctrl Pts',(3.53249922680016,1.9844566207056,-2.54144861078092));
#22801=CARTESIAN_POINT('Ctrl Pts',(3.52605312048251,1.90100714009866,-2.60445609580204));
#22802=CARTESIAN_POINT('Ctrl Pts',(3.51960701416485,1.81472094286566,-2.66325091983928));
#22803=CARTESIAN_POINT('Ctrl Pts',(3.51315938360299,1.72841434242652,-2.72205964648149));
#22804=CARTESIAN_POINT('Ctrl Pts',(3.50671175304113,1.63927000535803,-2.77665351913181));
#22805=CARTESIAN_POINT('Ctrl Pts',(3.50026412247928,1.54772264342607,-2.82677770288472));
#22806=CARTESIAN_POINT('Ctrl Pts',(3.49381173810022,1.45610778391972,-2.87693884303648));
#22807=CARTESIAN_POINT('Ctrl Pts',(3.48735935372116,1.36208669566401,-2.92262353462528));
#22808=CARTESIAN_POINT('Ctrl Pts',(3.4809069693421,1.26611816796091,-2.96362317902586));
#22809=CARTESIAN_POINT('Ctrl Pts',(3.47809506143749,1.22429569648526,-2.9814905622138));
#22810=CARTESIAN_POINT('Ctrl Pts',(3.47528315353287,1.18210364055045,-2.99846879411564));
#22811=CARTESIAN_POINT('Ctrl Pts',(3.47247124562825,1.1395810861412,-3.0145434995384));
#22812=CARTESIAN_POINT('Ctrl Pts',(3.46617126457528,1.04431079415822,-3.05055831333412));
#22813=CARTESIAN_POINT('Ctrl Pts',(3.45987128352231,0.947252186086576,-3.08208279945663));
#22814=CARTESIAN_POINT('Ctrl Pts',(3.45357130246934,0.848856252778096,-3.10894847571));
#22815=CARTESIAN_POINT('Ctrl Pts',(3.44727552762368,0.750526013904431,-3.13579621498815));
#22816=CARTESIAN_POINT('Ctrl Pts',(3.44097975277802,0.650860620899843,-3.15799122523729));
#22817=CARTESIAN_POINT('Ctrl Pts',(3.43468397793237,0.550327087937376,-3.17541456486903));
#22818=CARTESIAN_POINT('Ctrl Pts',(3.42839100102228,0.449838233565586,-3.19283016131065));
#22819=CARTESIAN_POINT('Ctrl Pts',(3.42209802411218,0.348482410725096,-3.20547823762093));
#22820=CARTESIAN_POINT('Ctrl Pts',(3.41580504720209,0.246737031113831,-3.21329089874806));
#22821=CARTESIAN_POINT('Ctrl Pts',(3.40951346280697,0.14501416580161,-3.22110183108329));
#22822=CARTESIAN_POINT('Ctrl Pts',(3.40322187841185,0.0429023241629521,
-3.22407944781139));
#22823=CARTESIAN_POINT('Ctrl Pts',(3.39693029401672,-0.0591164460693605,
-3.22220775374651));
#22824=CARTESIAN_POINT('Ctrl Pts',(3.39063656516385,-0.161169988932681,
-3.22033542172327));
#22825=CARTESIAN_POINT('Ctrl Pts',(3.38434283631098,-0.263129986453162,
-3.21361047975511));
#22826=CARTESIAN_POINT('Ctrl Pts',(3.3780491074581,-0.36451508727217,-3.20206906759535));
#22827=CARTESIAN_POINT('Ctrl Pts',(3.37175438206171,-0.465916241319268,
-3.1905258279785));
#22828=CARTESIAN_POINT('Ctrl Pts',(3.36545965666533,-0.566741910482421,
-3.17416465359994));
#22829=CARTESIAN_POINT('Ctrl Pts',(3.35916493126894,-0.666517837287942,
-3.15307334755743));
#22830=CARTESIAN_POINT('Ctrl Pts',(3.3528648162117,-0.766379194095918,-3.13196398274679));
#22831=CARTESIAN_POINT('Ctrl Pts',(3.34656470115446,-0.865188613006443,
-3.10611648897175));
#22832=CARTESIAN_POINT('Ctrl Pts',(3.34026458609723,-0.962483988941134,
-3.07566937975003));
#22833=CARTESIAN_POINT('Ctrl Pts',(3.33640306010251,-1.02211918923905,-3.05700745014149));
#22834=CARTESIAN_POINT('Ctrl Pts',(3.33254153410778,-1.0811858773422,-3.03661850873259));
#22835=CARTESIAN_POINT('Ctrl Pts',(3.32868000811306,-1.13958108614105,-3.01454349953846));
#22836=CARTESIAN_POINT('Ctrl Pts',(3.32222787133228,-1.23715232482427,-2.97765886404663));
#22837=CARTESIAN_POINT('Ctrl Pts',(3.31577573455149,-1.33298225140899,-2.93601378761227));
#22838=CARTESIAN_POINT('Ctrl Pts',(3.30932359777071,-1.42660369135491,-2.8897957488917));
#22839=CARTESIAN_POINT('Ctrl Pts',(3.30287533190599,-1.52016896374772,-2.84360543837256));
#22840=CARTESIAN_POINT('Ctrl Pts',(3.29642706604126,-1.61152805019238,-2.79284779845975));
#22841=CARTESIAN_POINT('Ctrl Pts',(3.28997880017654,-1.70023542039651,-2.73775767330293));
#22842=CARTESIAN_POINT('Ctrl Pts',(3.28353351658572,-1.78890176411679,-2.68269302690989));
#22843=CARTESIAN_POINT('Ctrl Pts',(3.2770882329949,-1.87491851400246,-2.6233000873556));
#22844=CARTESIAN_POINT('Ctrl Pts',(3.27064294940408,-1.95786663758549,-2.55985854920339));
#22845=CARTESIAN_POINT('Ctrl Pts',(3.26419976213879,-2.04078778232953,-2.49643764538225));
#22846=CARTESIAN_POINT('Ctrl Pts',(3.25775657487349,-2.12064198953114,-2.42897099735954));
#22847=CARTESIAN_POINT('Ctrl Pts',(3.25131338760819,-2.19704128404677,-2.35778013366262));
#22848=CARTESIAN_POINT('Ctrl Pts',(3.24487046796784,-2.27343740523273,-2.2865922269574));
#22849=CARTESIAN_POINT('Ctrl Pts',(3.23842754832749,-2.34637861930785,-2.21168066725837));
#22850=CARTESIAN_POINT('Ctrl Pts',(3.23198462868714,-2.41551206945869,-2.13340549469607));
#22851=CARTESIAN_POINT('Ctrl Pts',(3.22554227911908,-2.48463940265226,-2.05513724795456));
#22852=CARTESIAN_POINT('Ctrl Pts',(3.21909992955102,-2.54995939553337,-1.97350626776285));
#22853=CARTESIAN_POINT('Ctrl Pts',(3.21265757998296,-2.6111583393268,-1.88890700921568));
#22854=CARTESIAN_POINT('Ctrl Pts',(3.20621358079725,-2.67237295362312,-1.80428608831874));
#22855=CARTESIAN_POINT('Ctrl Pts',(3.19976958161155,-2.72946418966193,-1.71669567822796));
#22856=CARTESIAN_POINT('Ctrl Pts',(3.19332558242584,-2.78216069558516,-1.62656061259366));
#22857=CARTESIAN_POINT('Ctrl Pts',(3.19051331181652,-2.80515834511165,-1.58722414021874));
#22858=CARTESIAN_POINT('Ctrl Pts',(3.1877010412072,-2.82731954204425,-1.54740337185725));
#22859=CARTESIAN_POINT('Ctrl Pts',(3.18488877059788,-2.84862442585766,-1.50713517738361));
#22860=CARTESIAN_POINT('Ctrl Pts',(3.86280938168963,2.84862442585768,-1.50713517738357));
#22861=CARTESIAN_POINT('Ctrl Pts',(3.85636606854818,2.79981189786092,-1.5993953552535));
#22862=CARTESIAN_POINT('Ctrl Pts',(3.84992275540674,2.74650107987591,-1.6893054006252));
#22863=CARTESIAN_POINT('Ctrl Pts',(3.84347944226529,2.68894366242018,-1.77642887356357));
#22864=CARTESIAN_POINT('Ctrl Pts',(3.83703756419086,2.63139906426248,-1.86353294219552));
#22865=CARTESIAN_POINT('Ctrl Pts',(3.83059568611644,2.56960996034231,-1.94785135922787));
#22866=CARTESIAN_POINT('Ctrl Pts',(3.82415380804201,2.50387182458097,-2.02897596056966));
#22867=CARTESIAN_POINT('Ctrl Pts',(3.81771247715649,2.43813927277788,-2.11009367098914));
#22868=CARTESIAN_POINT('Ctrl Pts',(3.81127114627096,2.36845859682568,-2.18801781258259));
#22869=CARTESIAN_POINT('Ctrl Pts',(3.80482981538543,2.29516584988645,-2.2623729321257));
#22870=CARTESIAN_POINT('Ctrl Pts',(3.79838814430917,2.22186923208361,-2.33673197864027));
#22871=CARTESIAN_POINT('Ctrl Pts',(3.79194647323291,2.14496043015097,-2.40752135873283));
#22872=CARTESIAN_POINT('Ctrl Pts',(3.78550480215665,2.06481241972296,-2.47440239933965));
#22873=CARTESIAN_POINT('Ctrl Pts',(3.77905975356884,1.98462238590886,-2.54131850716494));
#22874=CARTESIAN_POINT('Ctrl Pts',(3.77261470498103,1.90119004104676,-2.60432193774656));
#22875=CARTESIAN_POINT('Ctrl Pts',(3.76616965639323,1.81492162709215,-2.66311416390908));
#22876=CARTESIAN_POINT('Ctrl Pts',(3.75972307966444,1.72863275862937,-2.72192032989055));
#22877=CARTESIAN_POINT('Ctrl Pts',(3.75327650293565,1.63950679792908,-2.77651309360132));
#22878=CARTESIAN_POINT('Ctrl Pts',(3.74682992620685,1.54797832620639,-2.82663769593757));
#22879=CARTESIAN_POINT('Ctrl Pts',(3.74037857905811,1.45638212407943,-2.87679939011548));
#22880=CARTESIAN_POINT('Ctrl Pts',(3.73392723190936,1.3623801950629,-2.92248614132501));
#22881=CARTESIAN_POINT('Ctrl Pts',(3.72747588476061,1.26643119723935,-2.96348942720552));
#22882=CARTESIAN_POINT('Ctrl Pts',(3.72465663789856,1.22450136385816,-2.98140791498601));
#22883=CARTESIAN_POINT('Ctrl Pts',(3.7218373910365,1.18219996526355,-2.99843261799755));
#22884=CARTESIAN_POINT('Ctrl Pts',(3.71901814417445,1.13956640274635,-3.0145490502282));
#22885=CARTESIAN_POINT('Ctrl Pts',(3.71271660161073,1.04427243879401,-3.05057228219266));
#22886=CARTESIAN_POINT('Ctrl Pts',(3.706415059047,0.947189762030143,-3.08210278953502));
#22887=CARTESIAN_POINT('Ctrl Pts',(3.70011351648328,0.848769608982329,-3.10897213132701));
#22888=CARTESIAN_POINT('Ctrl Pts',(3.6938161682386,0.750414964580609,-3.13582358883261));
#22889=CARTESIAN_POINT('Ctrl Pts',(3.68751881999391,0.650725009496901,-3.15801994590081));
#22890=CARTESIAN_POINT('Ctrl Pts',(3.68122147174923,0.550166988852229,-3.17544230728213));
#22891=CARTESIAN_POINT('Ctrl Pts',(3.67492691326741,0.449653516011018,-3.19285695045336));
#22892=CARTESIAN_POINT('Ctrl Pts',(3.6686323547856,0.348273146329405,-3.20550173722294));
#22893=CARTESIAN_POINT('Ctrl Pts',(3.66233779630378,0.246503510729632,-3.2133088214017));
#22894=CARTESIAN_POINT('Ctrl Pts',(3.65604462587464,0.144756316992322,-3.22111418399122));
#22895=CARTESIAN_POINT('Ctrl Pts',(3.64975145544551,0.0426204367755807,
-3.22408393729004));
#22896=CARTESIAN_POINT('Ctrl Pts',(3.64345828501638,-0.0594218713400216,
-3.22220213576157));
#22897=CARTESIAN_POINT('Ctrl Pts',(3.63716297451389,-0.161498880251751,
-3.22031969430236));
#22898=CARTESIAN_POINT('Ctrl Pts',(3.63086766401141,-0.263481843224689,
-3.21358240497111));
#22899=CARTESIAN_POINT('Ctrl Pts',(3.62457235350892,-0.364889203980296,
-3.20202645699854));
#22900=CARTESIAN_POINT('Ctrl Pts',(3.61827604930386,-0.466312571691608,
-3.19046868494194));
#22901=CARTESIAN_POINT('Ctrl Pts',(3.61197974509879,-0.567159749635694,
-3.17409079367219));
#22902=CARTESIAN_POINT('Ctrl Pts',(3.60568344089372,-0.666956276636632,
-3.15298063545512));
#22903=CARTESIAN_POINT('Ctrl Pts',(3.59938176457317,-0.766837951757845,
-3.1318524656865));
#22904=CARTESIAN_POINT('Ctrl Pts',(3.59308008825263,-0.86566678543172,-3.10598405634246));
#22905=CARTESIAN_POINT('Ctrl Pts',(3.58677841193208,-0.962980468876425,
-3.07551396990203));
#22906=CARTESIAN_POINT('Ctrl Pts',(3.58292791017447,-1.02244187090388,-3.05689588870818));
#22907=CARTESIAN_POINT('Ctrl Pts',(3.57907740841687,-1.08133787029128,-3.03656072698695));
#22908=CARTESIAN_POINT('Ctrl Pts',(3.57522690665926,-1.13956640274621,-3.01454905022826));
#22909=CARTESIAN_POINT('Ctrl Pts',(3.56877580865339,-1.23712199244632,-2.97767087356899));
#22910=CARTESIAN_POINT('Ctrl Pts',(3.56232471064752,-1.33293715724246,-2.93603367737495));
#22911=CARTESIAN_POINT('Ctrl Pts',(3.55587361264165,-1.4265448349937,-2.88982480372994));
#22912=CARTESIAN_POINT('Ctrl Pts',(3.54942639732379,-1.52009617359032,-2.84364374157368));
#22913=CARTESIAN_POINT('Ctrl Pts',(3.54297918200593,-1.61144233285859,-2.79289665086444));
#22914=CARTESIAN_POINT('Ctrl Pts',(3.53653196668807,-1.70013788545573,-2.73781824322546));
#22915=CARTESIAN_POINT('Ctrl Pts',(3.53008774073388,-1.7887923128152,-2.68276537364941));
#22916=CARTESIAN_POINT('Ctrl Pts',(3.52364351477968,-1.8747982608721,-2.62338538836474));
#22917=CARTESIAN_POINT('Ctrl Pts',(3.51719928882549,-1.95773679325689,-2.55995785333044));
#22918=CARTESIAN_POINT('Ctrl Pts',(3.51075716161945,-2.04064831431511,-2.49655097530337));
#22919=CARTESIAN_POINT('Ctrl Pts',(3.50431503441341,-2.12049411009414,-2.42909940481136));
#22920=CARTESIAN_POINT('Ctrl Pts',(3.49787290720737,-2.19688629710065,-2.35792454504197));
#22921=CARTESIAN_POINT('Ctrl Pts',(3.49143104021728,-2.27327539840822,-2.28675256022876));
#22922=CARTESIAN_POINT('Ctrl Pts',(3.48498917322719,-2.3462108883281,-2.21185784036661));
#22923=CARTESIAN_POINT('Ctrl Pts',(3.47854730623709,-2.4153399985513,-2.13360030321947));
#22924=CARTESIAN_POINT('Ctrl Pts',(3.47210600263395,-2.48446306294354,-2.05534961024896));
#22925=CARTESIAN_POINT('Ctrl Pts',(3.46566469903081,-2.54978016307586,-1.97373697256748));
#22926=CARTESIAN_POINT('Ctrl Pts',(3.45922339542768,-2.61097767827721,-1.88915672352459));
#22927=CARTESIAN_POINT('Ctrl Pts',(3.45278042233379,-2.67219105497052,-1.80455455253053));
#22928=CARTESIAN_POINT('Ctrl Pts',(3.44633744923991,-2.72928249243958,-1.71698354132592));
#22929=CARTESIAN_POINT('Ctrl Pts',(3.43989447614602,-2.78198072685917,-1.6268684021408));
#22930=CARTESIAN_POINT('Ctrl Pts',(3.43707487381204,-2.80504276089236,-1.58743181703159));
#22931=CARTESIAN_POINT('Ctrl Pts',(3.43425527147806,-2.82726399918805,-1.54750835297587));
#22932=CARTESIAN_POINT('Ctrl Pts',(3.43143566914408,-2.84862442585766,-1.50713517738361));
#22933=CARTESIAN_POINT('Origin',(13.3346225254169,0.,0.));
#22934=CARTESIAN_POINT('Ctrl Pts',(4.48780938168963,-2.84862442585767,1.50713517738358));
#22935=CARTESIAN_POINT('Ctrl Pts',(4.48136661099587,-2.79981600727515,1.59938758808176));
#22936=CARTESIAN_POINT('Ctrl Pts',(4.4749238403021,-2.74650998087232,1.68929040254968));
#22937=CARTESIAN_POINT('Ctrl Pts',(4.46848106960834,-2.68895796079644,1.77640723021763));
#22938=CARTESIAN_POINT('Ctrl Pts',(4.46203974188704,-2.63141883051341,1.86350454653112));
#22939=CARTESIAN_POINT('Ctrl Pts',(4.45559841416573,-2.56963581058662,1.94781680342466));
#22940=CARTESIAN_POINT('Ctrl Pts',(4.44915708644443,-2.50390430110695,2.02893588203228));
#22941=CARTESIAN_POINT('Ctrl Pts',(4.44271631136336,-2.43817843112874,2.11004800094636));
#22942=CARTESIAN_POINT('Ctrl Pts',(4.43627553628229,-2.36850498597941,2.18796719366113));
#22943=CARTESIAN_POINT('Ctrl Pts',(4.42983476120122,-2.2952199472197,2.26231804934337));
#22944=CARTESIAN_POINT('Ctrl Pts',(4.42339364893318,-2.22193107184706,2.33667279743611));
#22945=CARTESIAN_POINT('Ctrl Pts',(4.41695253666512,-2.14503049317434,2.40745856738946));
#22946=CARTESIAN_POINT('Ctrl Pts',(4.41051142439708,-2.06489111689294,2.47433672685765));
#22947=CARTESIAN_POINT('Ctrl Pts',(4.404066933082,-1.98470969900286,2.54124997101879));
#22948=CARTESIAN_POINT('Ctrl Pts',(4.39762244176692,-1.90128637962944,2.60425126539633));
#22949=CARTESIAN_POINT('Ctrl Pts',(4.39117795045184,-1.81502733201031,2.663042122565));
#22950=CARTESIAN_POINT('Ctrl Pts',(4.38473192897104,-1.72874780323421,2.72184693890444));
#22951=CARTESIAN_POINT('Ctrl Pts',(4.37828590749023,-1.63963152143695,2.77643911766918));
#22952=CARTESIAN_POINT('Ctrl Pts',(4.37183988600943,-1.54811299905293,2.82656393960288));
#22953=CARTESIAN_POINT('Ctrl Pts',(4.3653890854091,-1.45652662427993,2.87672592438435));
#22954=CARTESIAN_POINT('Ctrl Pts',(4.35893828480877,-1.36253478677607,2.922413759257));
#22955=CARTESIAN_POINT('Ctrl Pts',(4.35248748420844,-1.26659607549749,2.96341896194824));
#22956=CARTESIAN_POINT('Ctrl Pts',(4.34966437086378,-1.2246096814262,2.98136438331384));
#22957=CARTESIAN_POINT('Ctrl Pts',(4.34684125751911,-1.18225067630238,2.99841357392487));
#22958=CARTESIAN_POINT('Ctrl Pts',(4.34401814417444,-1.13955862823483,3.01455198915453));
#22959=CARTESIAN_POINT('Ctrl Pts',(4.33771576978968,-1.04425205094761,3.05057970832007));
#22960=CARTESIAN_POINT('Ctrl Pts',(4.33141339540492,-0.94715654926464,3.08211342543778));
#22961=CARTESIAN_POINT('Ctrl Pts',(4.32511102102016,-0.848723490673857,
3.10898472155757));
#22962=CARTESIAN_POINT('Ctrl Pts',(4.31881283459272,-0.750355841312021,
3.1358381615751));
#22963=CARTESIAN_POINT('Ctrl Pts',(4.31251464816528,-0.650652797700703,
3.15803523728402));
#22964=CARTESIAN_POINT('Ctrl Pts',(4.30621646173785,-0.550081728076085,
3.17545707811282));
#22965=CARTESIAN_POINT('Ctrl Pts',(4.29992106070215,-0.44955513630709,3.19287121408053));
#22966=CARTESIAN_POINT('Ctrl Pts',(4.29362565966646,-0.348161685766163,
3.20551424845805));
#22967=CARTESIAN_POINT('Ctrl Pts',(4.28733025863076,-0.246379124247223,
3.21331836107709));
#22968=CARTESIAN_POINT('Ctrl Pts',(4.2810362432644,-0.14461896590384,3.22112075594702));
#22969=CARTESIAN_POINT('Ctrl Pts',(4.27474222789805,-0.0424702754849352,
3.22408631900469));
#22970=CARTESIAN_POINT('Ctrl Pts',(4.26844821253169,0.0595845760164542,
3.22219913115266));
#22971=CARTESIAN_POINT('Ctrl Pts',(4.26215205943878,0.161674089868234,3.220311302328));
#22972=CARTESIAN_POINT('Ctrl Pts',(4.25585590634587,0.263669291018626,3.21356743282028));
#22973=CARTESIAN_POINT('Ctrl Pts',(4.24955975325296,0.365088513931847,3.20200373820754));
#22974=CARTESIAN_POINT('Ctrl Pts',(4.24326260798755,0.466523718883887,3.19043822134245));
#22975=CARTESIAN_POINT('Ctrl Pts',(4.23696546272215,0.567382358389521,3.17405142095642));
#22976=CARTESIAN_POINT('Ctrl Pts',(4.23066831745674,0.667189862659268,3.15293121549848));
#22977=CARTESIAN_POINT('Ctrl Pts',(4.22436580945623,0.767082364365909,3.13179302378445));
#22978=CARTESIAN_POINT('Ctrl Pts',(4.21806330145572,0.86592154302919,3.10591346756781));
#22979=CARTESIAN_POINT('Ctrl Pts',(4.21176079345521,0.963244981248796,3.07543113540183));
#22980=CARTESIAN_POINT('Ctrl Pts',(4.20791616452323,1.02261380812033,3.05683643371323));
#22981=CARTESIAN_POINT('Ctrl Pts',(4.20407153559125,1.08141888564317,3.03652993000679));
#22982=CARTESIAN_POINT('Ctrl Pts',(4.20022690665927,1.13955862823483,3.01455198915453));
#22983=CARTESIAN_POINT('Ctrl Pts',(4.19377635600178,1.2371059758296,2.9776772157179));
#22984=CARTESIAN_POINT('Ctrl Pts',(4.18732580534429,1.33291336564918,2.93604417137762));
#22985=CARTESIAN_POINT('Ctrl Pts',(4.18087525468681,1.42651379475993,2.88984012634949));
#22986=CARTESIAN_POINT('Ctrl Pts',(4.17442859288135,1.52005779485586,2.84366393641526));
#22987=CARTESIAN_POINT('Ctrl Pts',(4.16798193107589,1.61139714563366,2.79292240306838));
#22988=CARTESIAN_POINT('Ctrl Pts',(4.16153526927044,1.70008647398485,2.73785016819288));
#22989=CARTESIAN_POINT('Ctrl Pts',(4.15509160053378,1.78873462548057,2.68280350236269));
#22990=CARTESIAN_POINT('Ctrl Pts',(4.14864793179712,1.87473488450725,2.62343034099842));
#22991=CARTESIAN_POINT('Ctrl Pts',(4.14220426306046,1.95766836532562,2.56001018238274));
#22992=CARTESIAN_POINT('Ctrl Pts',(4.13576269432608,2.04057481798564,2.49661069250149));
#22993=CARTESIAN_POINT('Ctrl Pts',(4.12932112559171,2.12041618366918,2.42916706414711));
#22994=CARTESIAN_POINT('Ctrl Pts',(4.12287955685733,2.1968046271748,2.35800063454686));
#22995=CARTESIAN_POINT('Ctrl Pts',(4.11643824441589,2.27319003138686,2.28683703647009));
#22996=CARTESIAN_POINT('Ctrl Pts',(4.10999693197444,2.34612250647129,2.21195118690088));
#22997=CARTESIAN_POINT('Ctrl Pts',(4.103555619533,2.4152493307578,2.13370293920546));
#22998=CARTESIAN_POINT('Ctrl Pts',(4.09711486695258,2.48437014673239,2.05546149263079));
#22999=CARTESIAN_POINT('Ctrl Pts',(4.09067411437216,2.54968572303579,1.9738585168972));
#23000=CARTESIAN_POINT('Ctrl Pts',(4.08423336179173,2.61088248542984,1.88928828127835));
#23001=CARTESIAN_POINT('Ctrl Pts',(4.07779092924952,2.67209520996826,1.80469598693846));
#23002=CARTESIAN_POINT('Ctrl Pts',(4.07134849670731,2.72918675307052,1.71713519437524));
#23003=CARTESIAN_POINT('Ctrl Pts',(4.06490606416509,2.78188589731074,1.62703055190849));
#23004=CARTESIAN_POINT('Ctrl Pts',(4.06208259915809,2.8049818612477,1.58754122806902));
#23005=CARTESIAN_POINT('Ctrl Pts',(4.05925913415108,2.82723473678362,1.54756366161791));
#23006=CARTESIAN_POINT('Ctrl Pts',(4.05643566914408,2.84862442585767,1.5071351773836));
#23007=CARTESIAN_POINT('Ctrl Pts',(4.24126248314343,-2.84862442585767,1.50713517738358));
#23008=CARTESIAN_POINT('Ctrl Pts',(4.23481876049118,-2.79980879553496,1.59940121893556));
#23009=CARTESIAN_POINT('Ctrl Pts',(4.22837503783893,-2.74649436014097,1.68931672321789));
#23010=CARTESIAN_POINT('Ctrl Pts',(4.22193131518668,-2.6889328678291,1.77644521300501));
#23011=CARTESIAN_POINT('Ctrl Pts',(4.21548902163385,-2.63138414159976,1.8635543792922));
#23012=CARTESIAN_POINT('Ctrl Pts',(4.20904672808102,-2.56959044436887,1.94787744697516));
#23013=CARTESIAN_POINT('Ctrl Pts',(4.20260443452819,-2.50384730577855,2.0290062177937));
#23014=CARTESIAN_POINT('Ctrl Pts',(4.19616268405277,-2.43810970925386,2.11012814955677));
#23015=CARTESIAN_POINT('Ctrl Pts',(4.18972093357736,-2.36842357401578,2.1880560273807));
#23016=CARTESIAN_POINT('Ctrl Pts',(4.18327918310194,-2.29512500726732,2.26241436600729));
#23017=CARTESIAN_POINT('Ctrl Pts',(4.17683709017549,-2.22182254388083,2.33677665761064));
#23018=CARTESIAN_POINT('Ctrl Pts',(4.17039499724904,-2.14490753324225,2.40756876318795));
#23019=CARTESIAN_POINT('Ctrl Pts',(4.16395290432258,-2.06475300377837,2.47445197890123));
#23020=CARTESIAN_POINT('Ctrl Pts',(4.15750743506085,-1.98455646489775,2.54137024846487));
#23021=CARTESIAN_POINT('Ctrl Pts',(4.15106196579911,-1.90111730565429,2.60437529159052));
#23022=CARTESIAN_POINT('Ctrl Pts',(4.14461649653737,-1.81484181987328,2.663168551057));
#23023=CARTESIAN_POINT('Ctrl Pts',(4.13816950067629,-1.72854589987803,2.72197573561528));
#23024=CARTESIAN_POINT('Ctrl Pts',(4.13172250481521,-1.63941263144259,2.77656894057831));
#23025=CARTESIAN_POINT('Ctrl Pts',(4.12527550895413,-1.54787664770338,2.82669337672032));
#23026=CARTESIAN_POINT('Ctrl Pts',(4.11882374926244,-1.45627302596195,2.87685485093835));
#23027=CARTESIAN_POINT('Ctrl Pts',(4.11237198957076,-1.36226347780444,2.92254078344268));
#23028=CARTESIAN_POINT('Ctrl Pts',(4.10592022987908,-1.2663067134988,2.96354262156762));
#23029=CARTESIAN_POINT('Ctrl Pts',(4.10310390179547,-1.22441957835406,2.98144078171453));
#23030=CARTESIAN_POINT('Ctrl Pts',(4.10028757371185,-1.18216166644338,2.99844700132402));
#23031=CARTESIAN_POINT('Ctrl Pts',(4.09747124562824,-1.1395722534486,3.0145468385265));
#23032=CARTESIAN_POINT('Ctrl Pts',(4.09117032668804,-1.04428774432049,3.05056670771484));
#23033=CARTESIAN_POINT('Ctrl Pts',(4.08486940774784,-0.94721468089237,3.08209480971671));
#23034=CARTESIAN_POINT('Ctrl Pts',(4.07856848880764,-0.848804201550354,
3.10896268712419));
#23035=CARTESIAN_POINT('Ctrl Pts',(4.07227176894274,-0.750459305183979,
3.13581265916873));
#23036=CARTESIAN_POINT('Ctrl Pts',(4.06597504907784,-0.6507791607072,3.15800847802623));
#23037=CARTESIAN_POINT('Ctrl Pts',(4.05967832921294,-0.550230920981323,
3.1754312299428));
#23038=CARTESIAN_POINT('Ctrl Pts',(4.05338440237998,-0.449727281372719,
3.19284625366064));
#23039=CARTESIAN_POINT('Ctrl Pts',(4.04709047554701,-0.348356716342556,
3.20549235420444));
#23040=CARTESIAN_POINT('Ctrl Pts',(4.04079654871405,-0.246596769234935,
3.21330166587311));
#23041=CARTESIAN_POINT('Ctrl Pts',(4.03450401171771,-0.14485929294807,3.22110925307505));
#23042=CARTESIAN_POINT('Ctrl Pts',(4.02821147472137,-0.0427330144242478,
3.22408214721155));
#23043=CARTESIAN_POINT('Ctrl Pts',(4.02191893772504,0.0592998919896358,
3.22220438292018));
#23044=CARTESIAN_POINT('Ctrl Pts',(4.01562425890107,0.161367527940822,3.2203259794832));
#23045=CARTESIAN_POINT('Ctrl Pts',(4.0093295800771,0.263341317904613,3.21359362212927));
#23046=CARTESIAN_POINT('Ctrl Pts',(4.00303490125313,0.364739787469471,3.20204348033201));
#23047=CARTESIAN_POINT('Ctrl Pts',(3.99673922758709,0.466154282548244,3.19049151309341));
#23048=CARTESIAN_POINT('Ctrl Pts',(3.99044355392106,0.566992869424478,3.17412029923523));
#23049=CARTESIAN_POINT('Ctrl Pts',(3.98414788025502,0.666781168304401,3.15301767138952));
#23050=CARTESIAN_POINT('Ctrl Pts',(3.97784682745646,0.766654728033676,3.13189701309342));
#23051=CARTESIAN_POINT('Ctrl Pts',(3.9715457746579,0.8654758072472,3.10603695831234));
#23052=CARTESIAN_POINT('Ctrl Pts',(3.96524472185934,0.962782178547027,3.07557604997377));
#23053=CARTESIAN_POINT('Ctrl Pts',(3.96138981727725,1.02231298848977,3.05694045067268));
#23054=CARTESIAN_POINT('Ctrl Pts',(3.95753491269516,1.08127715485643,3.03658380806987));
#23055=CARTESIAN_POINT('Ctrl Pts',(3.95368000811307,1.13957225344858,3.0145468385265));
#23056=CARTESIAN_POINT('Ctrl Pts',(3.947228496954,1.23713406621913,2.97766609299998));
#23057=CARTESIAN_POINT('Ctrl Pts',(3.94077698579493,1.33295510131961,2.93602576269598));
#23058=CARTESIAN_POINT('Ctrl Pts',(3.93432547463586,1.42656825190966,2.88981324399059));
#23059=CARTESIAN_POINT('Ctrl Pts',(3.92787784149396,1.52012513143452,2.8436285037291));
#23060=CARTESIAN_POINT('Ctrl Pts',(3.92143020835205,1.6114764313792,2.79287721761468));
#23061=CARTESIAN_POINT('Ctrl Pts',(3.91498257521015,1.70017668345824,2.73779414995447));
#23062=CARTESIAN_POINT('Ctrl Pts',(3.90853792862088,1.7888358494573,2.68273659684773));
#23063=CARTESIAN_POINT('Ctrl Pts',(3.9020932820316,1.87484609299292,2.62335145979373));
#23064=CARTESIAN_POINT('Ctrl Pts',(3.89564863544233,1.95778843947618,2.55991835587649));
#23065=CARTESIAN_POINT('Ctrl Pts',(3.889206086644,2.04070378747302,2.4965059000102));
#23066=CARTESIAN_POINT('Ctrl Pts',(3.88276353784567,2.12055292816708,2.4290483334246));
#23067=CARTESIAN_POINT('Ctrl Pts',(3.87632098904734,2.19694794161334,2.35786710913506));
#23068=CARTESIAN_POINT('Ctrl Pts',(3.869878703417,2.2733398344434,2.28668879248663));
#23069=CARTESIAN_POINT('Ctrl Pts',(3.86343641778667,2.34627760067319,2.21178737573021));
#23070=CARTESIAN_POINT('Ctrl Pts',(3.85699413215633,2.41540843679194,2.13352282527615));
#23071=CARTESIAN_POINT('Ctrl Pts',(3.85055241257265,2.48453319878091,2.05526515147893));
#23072=CARTESIAN_POINT('Ctrl Pts',(3.84411069298898,2.54985144934752,1.97364521927884));
#23073=CARTESIAN_POINT('Ctrl Pts',(3.8376689734053,2.61104953277672,1.88905741042628));
#23074=CARTESIAN_POINT('Ctrl Pts',(3.83122559223455,2.67226340173385,1.80444778286399));
#23075=CARTESIAN_POINT('Ctrl Pts',(3.82478221106381,2.72935475925089,1.71686905696282));
#23076=CARTESIAN_POINT('Ctrl Pts',(3.81833882989306,2.78205230648587,1.62674599322594));
#23077=CARTESIAN_POINT('Ctrl Pts',(3.81552214346133,2.80508873136103,1.58734922247993));
#23078=CARTESIAN_POINT('Ctrl Pts',(3.8127054570296,2.82728608915286,1.54746660090595));
#23079=CARTESIAN_POINT('Ctrl Pts',(3.80988877059788,2.84862442585767,1.5071351773836));
#23080=CARTESIAN_POINT('Origin',(13.3346225254169,0.,0.));
#23081=CARTESIAN_POINT('Ctrl Pts',(4.86626248314343,2.84862442585767,-1.50713517738359));
#23082=CARTESIAN_POINT('Ctrl Pts',(4.85981933345969,2.79981313616544,-1.59939301474379));
#23083=CARTESIAN_POINT('Ctrl Pts',(4.85337618377595,2.74650376206013,-1.68930088118904));
#23084=CARTESIAN_POINT('Ctrl Pts',(4.84693303409221,2.68894797104939,-1.77642235166342));
#23085=CARTESIAN_POINT('Ctrl Pts',(4.84049132185755,2.63140502057819,-1.86352438557603));
#23086=CARTESIAN_POINT('Ctrl Pts',(4.83404960962288,2.56961775001987,-1.9478409463242));
#23087=CARTESIAN_POINT('Ctrl Pts',(4.82760789738821,2.50388161105083,-2.02896388344926));
#23088=CARTESIAN_POINT('Ctrl Pts',(4.82116673398445,2.43815107277048,-2.11007990893753));
#23089=CARTESIAN_POINT('Ctrl Pts',(4.81472557058069,2.36847257578656,-2.18800255924028));
#23090=CARTESIAN_POINT('Ctrl Pts',(4.80828440717693,2.29518215168749,-2.26235639391215));
#23091=CARTESIAN_POINT('Ctrl Pts',(4.80184290448635,2.22188786703192,-2.33671414515543));
#23092=CARTESIAN_POINT('Ctrl Pts',(4.79540140179577,2.14498154315761,-2.4075024373787));
#23093=CARTESIAN_POINT('Ctrl Pts',(4.78895989910519,2.0648361346245,-2.47438260979359));
#23094=CARTESIAN_POINT('Ctrl Pts',(4.78251501843759,1.98464869717969,-2.54129785472121));
#23095=CARTESIAN_POINT('Ctrl Pts',(4.77607013776999,1.90121907212231,-2.60430064161492));
#23096=CARTESIAN_POINT('Ctrl Pts',(4.76962525710239,1.8149534807021,-2.66309245528339));
#23097=CARTESIAN_POINT('Ctrl Pts',(4.76317884768156,1.72866742671495,-2.72189821462132));
#23098=CARTESIAN_POINT('Ctrl Pts',(4.75673243826072,1.63954438272681,-2.77649080212196));
#23099=CARTESIAN_POINT('Ctrl Pts',(4.75028602883989,1.54801890922746,-2.82661547069534));
#23100=CARTESIAN_POINT('Ctrl Pts',(4.74383484637411,1.45642566851539,-2.8767772525329));
#23101=CARTESIAN_POINT('Ctrl Pts',(4.73738366390833,1.36242678053088,-2.92246433038377));
#23102=CARTESIAN_POINT('Ctrl Pts',(4.73093248144255,1.26648088252647,-2.96346819397391));
#23103=CARTESIAN_POINT('Ctrl Pts',(4.72811206950445,1.22453400572065,-2.9813947968861));
#23104=CARTESIAN_POINT('Ctrl Pts',(4.72529165756634,1.18221524872853,-2.99842687834116));
#23105=CARTESIAN_POINT('Ctrl Pts',(4.72247124562824,1.13956406305674,-3.01454993468173));
#23106=CARTESIAN_POINT('Ctrl Pts',(4.71616945312009,1.04426630931427,-3.05057451473779));
#23107=CARTESIAN_POINT('Ctrl Pts',(4.70986766061195,0.947179779202421,-3.08210598637527));
#23108=CARTESIAN_POINT('Ctrl Pts',(4.70356586810381,0.84875574859297,-3.10897591527023));
#23109=CARTESIAN_POINT('Ctrl Pts',(4.69726826800526,0.750397196789678,-3.13582796833899));
#23110=CARTESIAN_POINT('Ctrl Pts',(4.69097066790671,0.650703309207103,-3.15802454125043));
#23111=CARTESIAN_POINT('Ctrl Pts',(4.68467306780816,0.550141367953137,-3.17544674617079));
#23112=CARTESIAN_POINT('Ctrl Pts',(4.67837825616033,0.449623953505189,-3.19286123688904));
#23113=CARTESIAN_POINT('Ctrl Pts',(4.67208344451251,0.348239653662265,-3.2055054971021));
#23114=CARTESIAN_POINT('Ctrl Pts',(4.66578863286469,0.246466134457317,-3.21331168844008));
#23115=CARTESIAN_POINT('Ctrl Pts',(4.65949520855386,0.14471504549758,-3.22111615934247));
#23116=CARTESIAN_POINT('Ctrl Pts',(4.65320178424304,0.04257531645346,-3.22408465366294));
#23117=CARTESIAN_POINT('Ctrl Pts',(4.64690835993221,-0.0594707603238784,
-3.22220123380997));
#23118=CARTESIAN_POINT('Ctrl Pts',(4.64061279625238,-0.161551526358372,
-3.22031717371254));
#23119=CARTESIAN_POINT('Ctrl Pts',(4.63431723257254,-0.263538166304509,
-3.21357790737857));
#23120=CARTESIAN_POINT('Ctrl Pts',(4.62802166889271,-0.364949091061416,
-3.20201963195628));
#23121=CARTESIAN_POINT('Ctrl Pts',(4.62172511196881,-0.46637601530677,-3.19045953299778));
#23122=CARTESIAN_POINT('Ctrl Pts',(4.61542855504492,-0.567226636915087,
-3.174078965025));
#23123=CARTESIAN_POINT('Ctrl Pts',(4.60913199812103,-0.667026462081897,
-3.15296578817191));
#23124=CARTESIAN_POINT('Ctrl Pts',(4.60283007189777,-0.766911390130261,
-3.13183460735753));
#23125=CARTESIAN_POINT('Ctrl Pts',(4.59652814567451,-0.865743332042191,
-3.1059628489963));
#23126=CARTESIAN_POINT('Ctrl Pts',(4.59022621945125,-0.963059946406137,
-3.07548908340254));
#23127=CARTESIAN_POINT('Ctrl Pts',(4.58637748233852,-1.0224935310148,-3.05687802569571));
#23128=CARTESIAN_POINT('Ctrl Pts',(4.58252874522579,-1.08136220999437,-3.03655147441081));
#23129=CARTESIAN_POINT('Ctrl Pts',(4.57868000811306,-1.13956406305672,-3.01454993468173));
#23130=CARTESIAN_POINT('Ctrl Pts',(4.57222907503224,-1.23711716899467,-2.97767278347336));
#23131=CARTESIAN_POINT('Ctrl Pts',(4.56577814195141,-1.33292999080922,-2.93603683833042));
#23132=CARTESIAN_POINT('Ctrl Pts',(4.55932720887058,-1.42653548420085,-2.88982941967443));
#23133=CARTESIAN_POINT('Ctrl Pts',(4.55288016033801,-1.52008461131938,-2.84364982566724));
#23134=CARTESIAN_POINT('Ctrl Pts',(4.54643311180544,-1.61142871884073,-2.79290440957343));
#23135=CARTESIAN_POINT('Ctrl Pts',(4.53998606327287,-1.7001223957646,-2.73782786199565));
#23136=CARTESIAN_POINT('Ctrl Pts',(4.5335420052227,-1.78877493186577,-2.68277686183632));
#23137=CARTESIAN_POINT('Ctrl Pts',(4.52709794717254,-1.87477916552009,-2.62339893285564));
#23138=CARTESIAN_POINT('Ctrl Pts',(4.52065388912237,-1.9577161756141,-2.55997362061387));
#23139=CARTESIAN_POINT('Ctrl Pts',(4.51421193019997,-2.04062616928784,-2.49656896892991));
#23140=CARTESIAN_POINT('Ctrl Pts',(4.50776997127757,-2.1204706300486,-2.42911979172178));
#23141=CARTESIAN_POINT('Ctrl Pts',(4.50132801235517,-2.19686168895409,-2.35794747229573));
#23142=CARTESIAN_POINT('Ctrl Pts',(4.49488631246818,-2.27324967612483,-2.28677801475546));
#23143=CARTESIAN_POINT('Ctrl Pts',(4.48844461258119,-2.34618425752059,-2.21188596787905));
#23144=CARTESIAN_POINT('Ctrl Pts',(4.48200291269419,-2.41531267888492,-2.13363123002026));
#23145=CARTESIAN_POINT('Ctrl Pts',(4.47556177513205,-2.48443506571956,-2.05538332336822));
#23146=CARTESIAN_POINT('Ctrl Pts',(4.4691206375699,-2.54975170666112,-1.97377359722138));
#23147=CARTESIAN_POINT('Ctrl Pts',(4.46267950000776,-2.61094899502869,-1.88919636561653));
#23148=CARTESIAN_POINT('Ctrl Pts',(4.45623668979986,-2.67216217521413,-1.80459717084963));
#23149=CARTESIAN_POINT('Ctrl Pts',(4.44979387959195,-2.72925364454466,-1.71702923891643));
#23150=CARTESIAN_POINT('Ctrl Pts',(4.44335106938405,-2.78195215317476,-1.62691726278454));
#23151=CARTESIAN_POINT('Ctrl Pts',(4.44053030312199,-2.80502441052948,-1.58746478570115));
#23152=CARTESIAN_POINT('Ctrl Pts',(4.43770953685994,-2.82725518163247,-1.5475250189688));
#23153=CARTESIAN_POINT('Ctrl Pts',(4.43488877059788,-2.84862442585766,-1.50713517738361));
#23154=CARTESIAN_POINT('Ctrl Pts',(5.11280938168962,2.84862442585767,-1.50713517738359));
#23155=CARTESIAN_POINT('Ctrl Pts',(5.10636711383503,2.79981981662761,-1.59938038805443));
#23156=CARTESIAN_POINT('Ctrl Pts',(5.09992484598043,2.74651823180318,-1.6892764997169));
#23157=CARTESIAN_POINT('Ctrl Pts',(5.09348257812584,2.68897121470972,-1.77638716752923));
#23158=CARTESIAN_POINT('Ctrl Pts',(5.08704176057363,2.63143715277091,-1.86347822473044));
#23159=CARTESIAN_POINT('Ctrl Pts',(5.08060094302142,2.56965977216091,-1.94778477152975));
#23160=CARTESIAN_POINT('Ctrl Pts',(5.07416012546921,2.50393440450652,-2.02889873094459));
#23161=CARTESIAN_POINT('Ctrl Pts',(5.06771986561689,2.43821472790447,-2.11000566683405));
#23162=CARTESIAN_POINT('Ctrl Pts',(5.06127960576456,2.36854798484811,-2.18792027227159));
#23163=CARTESIAN_POINT('Ctrl Pts',(5.05483934591224,2.29527009050459,-2.26226717567467));
#23164=CARTESIAN_POINT('Ctrl Pts',(5.04839875166834,2.2219883914217,-2.33661793932228));
#23165=CARTESIAN_POINT('Ctrl Pts',(5.04195815742445,2.1450954345748,-2.40740036286648));
#23166=CARTESIAN_POINT('Ctrl Pts',(5.03551756318055,2.06496406080377,-2.47427585165616));
#23167=CARTESIAN_POINT('Ctrl Pts',(5.02907358849095,1.98479062883933,-2.54118644108257));
#23168=CARTESIAN_POINT('Ctrl Pts',(5.02262961380134,1.90137567487522,-2.60418575505825));
#23169=CARTESIAN_POINT('Ctrl Pts',(5.01618563911174,1.8151253084368,-2.66297534295236));
#23170=CARTESIAN_POINT('Ctrl Pts',(5.00974013239813,1.72885443638833,-2.7217789077884));
#23171=CARTESIAN_POINT('Ctrl Pts',(5.00329462568452,1.63974712559499,-2.77637054387109));
#23172=CARTESIAN_POINT('Ctrl Pts',(4.99684911897091,1.54823782472648,-2.8264955688248));
#23173=CARTESIAN_POINT('Ctrl Pts',(4.99039882510423,1.4566605588321,-2.87665782221961));
#23174=CARTESIAN_POINT('Ctrl Pts',(4.98394853123755,1.36267807492272,-2.92234666080682));
#23175=CARTESIAN_POINT('Ctrl Pts',(4.97749823737087,1.26674889787392,-2.96335363941518));
#23176=CARTESIAN_POINT('Ctrl Pts',(4.97467153963873,1.22471007099033,-2.98132403515682));
#23177=CARTESIAN_POINT('Ctrl Pts',(4.97184484190659,1.18229766210062,-2.99839592961301));
#23178=CARTESIAN_POINT('Ctrl Pts',(4.96901814417446,1.13955139439377,-3.01455472367566));
#23179=CARTESIAN_POINT('Ctrl Pts',(4.96271499237138,1.04423302649469,-3.05058663850462));
#23180=CARTESIAN_POINT('Ctrl Pts',(4.95641184056829,0.947125536289407,-3.08212335702997));
#23181=CARTESIAN_POINT('Ctrl Pts',(4.95010868876521,0.848680413718823,-3.10899648083912));
#23182=CARTESIAN_POINT('Ctrl Pts',(4.94380971895555,0.750300607178534,-3.1358517749608));
#23183=CARTESIAN_POINT('Ctrl Pts',(4.93751074914588,0.65058532817276,-3.15804952315385));
#23184=CARTESIAN_POINT('Ctrl Pts',(4.93121177933621,0.550002060058652,-3.17547087790634));
#23185=CARTESIAN_POINT('Ctrl Pts',(4.92491559082192,0.449463204251157,-3.19288454030041));
#23186=CARTESIAN_POINT('Ctrl Pts',(4.91861940230763,0.348057525191484,-3.20552593692252));
#23187=CARTESIAN_POINT('Ctrl Pts',(4.91232321379334,0.246262879960412,-3.21332727191825));
#23188=CARTESIAN_POINT('Ctrl Pts',(4.90602840871693,0.144490601684816,-3.22112689275592));
#23189=CARTESIAN_POINT('Ctrl Pts',(4.89973360364052,0.0423299356387917,
-3.22408853877205));
#23190=CARTESIAN_POINT('Ctrl Pts',(4.89343879856411,-0.0597366420634672,
-3.22219631557343));
#23191=CARTESIAN_POINT('Ctrl Pts',(4.88714185796157,-0.161837846071059,
-3.22030345043403));
#23192=CARTESIAN_POINT('Ctrl Pts',(4.88084491735904,-0.263844488001992,
-3.21355342937545));
#23193=CARTESIAN_POINT('Ctrl Pts',(4.87454797675651,-0.365274800146589,
-3.2019824925939));
#23194=CARTESIAN_POINT('Ctrl Pts',(4.86825004542209,-0.46672107087347,-3.19040973529399));
#23195=CARTESIAN_POINT('Ctrl Pts',(4.86195211408767,-0.567590424925492,
-3.17401460588662));
#23196=CARTESIAN_POINT('Ctrl Pts',(4.85565418275325,-0.667408190937708,
-3.15288500728607));
#23197=CARTESIAN_POINT('Ctrl Pts',(4.84935089747216,-0.767310813225424,
-3.13173744616129));
#23198=CARTESIAN_POINT('Ctrl Pts',(4.84304761219107,-0.866159662195225,
-3.10584746878142));
#23199=CARTESIAN_POINT('Ctrl Pts',(4.83674432690997,-0.963492218863993,
-3.07535368806395));
#23200=CARTESIAN_POINT('Ctrl Pts',(4.8329051868264,-1.02277453008417,-3.05678085014986));
#23201=CARTESIAN_POINT('Ctrl Pts',(4.82906604674283,-1.08149463511915,-3.03650113601502));
#23202=CARTESIAN_POINT('Ctrl Pts',(4.82522690665926,-1.13955139439361,-3.01455472367572));
#23203=CARTESIAN_POINT('Ctrl Pts',(4.81877686346817,-1.23709110294912,-2.97768310544958));
#23204=CARTESIAN_POINT('Ctrl Pts',(4.81232682027708,-1.33289128658037,-2.93605391017899));
#23205=CARTESIAN_POINT('Ctrl Pts',(4.80587677708598,-1.42648499723591,-2.88985434151289));
#23206=CARTESIAN_POINT('Ctrl Pts',(4.79943062843622,-1.52002219593272,-2.84368266818397));
#23207=CARTESIAN_POINT('Ctrl Pts',(4.79298447978646,-1.61135523643265,-2.79294628646449));
#23208=CARTESIAN_POINT('Ctrl Pts',(4.7865383311367,-1.70003879590331,-2.73787977364303));
#23209=CARTESIAN_POINT('Ctrl Pts',(4.78009517897046,-1.78868113094077,-2.68283885841591));
#23210=CARTESIAN_POINT('Ctrl Pts',(4.77365202680422,-1.87467611728968,-2.6234720224791));
#23211=CARTESIAN_POINT('Ctrl Pts',(4.76720887463797,-1.95760491614971,-2.56005870142981));
#23212=CARTESIAN_POINT('Ctrl Pts',(4.76076782362139,-2.0405066714427,-2.49666605983594));
#23213=CARTESIAN_POINT('Ctrl Pts',(4.75432677260481,-2.12034393124181,-2.42922979327325));
#23214=CARTESIAN_POINT('Ctrl Pts',(4.74788572158823,-2.19672890512053,-2.35807117787143));
#23215=CARTESIAN_POINT('Ctrl Pts',(4.74144492321345,-2.27311088289856,-2.28691535357323));
#23216=CARTESIAN_POINT('Ctrl Pts',(4.73500412483867,-2.34604056377377,-2.21203772602462));
#23217=CARTESIAN_POINT('Ctrl Pts',(4.72856332646389,-2.4151652693211,-2.13379808894027));
#23218=CARTESIAN_POINT('Ctrl Pts',(4.72212308467781,-2.48428400138074,-2.05556521302048));
#23219=CARTESIAN_POINT('Ctrl Pts',(4.71568284289172,-2.54959816524026,-1.97397119318511));
#23220=CARTESIAN_POINT('Ctrl Pts',(4.70924260110564,-2.61079422971956,-1.88941023935064));
#23221=CARTESIAN_POINT('Ctrl Pts',(4.70280066964823,-2.6720063496885,-1.80482709997974));
#23222=CARTESIAN_POINT('Ctrl Pts',(4.69635873819083,-2.72909799048163,-1.71727577947338));
#23223=CARTESIAN_POINT('Ctrl Pts',(4.68991680673342,-2.7817979777028,-1.62718086694399));
#23224=CARTESIAN_POINT('Ctrl Pts',(4.68708976087031,-2.8049254018061,-1.58764265523871));
#23225=CARTESIAN_POINT('Ctrl Pts',(4.6842627150072,-2.82720760933608,-1.54761493499459));
#23226=CARTESIAN_POINT('Ctrl Pts',(4.68143566914408,-2.84862442585766,-1.50713517738361));
#23227=CARTESIAN_POINT('Origin',(13.3346225254169,0.,0.));
#23228=CARTESIAN_POINT('Ctrl Pts',(5.73780938168963,-2.84862442585767,1.50713517738358));
#23229=CARTESIAN_POINT('Ctrl Pts',(5.73136758080448,-2.79982335424228,1.59937370163659));
#23230=CARTESIAN_POINT('Ctrl Pts',(5.72492577991932,-2.74652589403969,1.68926358874148));
#23231=CARTESIAN_POINT('Ctrl Pts',(5.71848397903417,-2.68898352277793,1.77636853629218));
#23232=CARTESIAN_POINT('Ctrl Pts',(5.71204363526109,-2.63145416739255,1.8634537810186));
#23233=CARTESIAN_POINT('Ctrl Pts',(5.70560329148801,-2.5696820234343,1.9477550252753));
#23234=CARTESIAN_POINT('Ctrl Pts',(5.69916294771493,-2.5039623589255,2.02886423093913));
#23235=CARTESIAN_POINT('Ctrl Pts',(5.69272316634707,-2.43824843340877,2.10996635371399));
#23236=CARTESIAN_POINT('Ctrl Pts',(5.6862833849792,-2.36858791370451,2.18787669933437));
#23237=CARTESIAN_POINT('Ctrl Pts',(5.67984360361133,-2.29531665330212,2.26221993262679));
#23238=CARTESIAN_POINT('Ctrl Pts',(5.6734034904585,-2.22204161787986,2.33656699616836));
#23239=CARTESIAN_POINT('Ctrl Pts',(5.66696337730567,-2.14515573827782,2.40734631214546));
#23240=CARTESIAN_POINT('Ctrl Pts',(5.66052326415283,-2.06503179509463,2.47421932086633));
#23241=CARTESIAN_POINT('Ctrl Pts',(5.65407976927837,-1.98486577860227,2.54112744479321));
#23242=CARTESIAN_POINT('Ctrl Pts',(5.64763627440391,-1.90145859236094,2.60412491949775));
#23243=CARTESIAN_POINT('Ctrl Pts',(5.64119277952944,-1.81521628671604,2.66291332846956));
#23244=CARTESIAN_POINT('Ctrl Pts',(5.63474775092228,-1.72895345298092,2.72171573073335));
#23245=CARTESIAN_POINT('Ctrl Pts',(5.62830272231512,-1.6398544721981,2.77630686247375));
#23246=CARTESIAN_POINT('Ctrl Pts',(5.62185769370796,-1.54835373381425,2.82643207551207));
#23247=CARTESIAN_POINT('Ctrl Pts',(5.61540787051526,-1.45678492620307,2.8765945776978));
#23248=CARTESIAN_POINT('Ctrl Pts',(5.60895804732255,-1.36281112768951,2.92228434769856));
#23249=CARTESIAN_POINT('Ctrl Pts',(5.60250822412985,-1.26689080363705,2.96329297474277));
#23250=CARTESIAN_POINT('Ctrl Pts',(5.59967819747804,-1.22480328194728,2.98128656991919));
#23251=CARTESIAN_POINT('Ctrl Pts',(5.59684817082624,-1.18234127527403,2.99837955251588));
#23252=CARTESIAN_POINT('Ctrl Pts',(5.59401814417444,-1.13954465120738,3.01455727270269));
#23253=CARTESIAN_POINT('Ctrl Pts',(5.58771426446053,-1.04421524146304,3.05059311782018));
#23254=CARTESIAN_POINT('Ctrl Pts',(5.58141038474663,-0.947096523955763,
3.08213264808556));
#23255=CARTESIAN_POINT('Ctrl Pts',(5.57510650503273,-0.848640103333476,
3.10900748431298));
#23256=CARTESIAN_POINT('Ctrl Pts',(5.56880680171199,-0.75024891122765,3.13586451565083));
#23257=CARTESIAN_POINT('Ctrl Pts',(5.56250709839125,-0.650522173317262,
3.15806289431417));
#23258=CARTESIAN_POINT('Ctrl Pts',(5.5562073950705,-0.549927480801481,3.17548379437832));
#23259=CARTESIAN_POINT('Ctrl Pts',(5.54991046919983,-0.449377139062347,
3.19289701381412));
#23260=CARTESIAN_POINT('Ctrl Pts',(5.54361354332915,-0.347960007274539,
3.20553687704002));
#23261=CARTESIAN_POINT('Ctrl Pts',(5.53731661745847,-0.246154044899148,
3.21333561096251));
#23262=CARTESIAN_POINT('Ctrl Pts',(5.53102107293278,-0.144370415509591,
3.22113263409115));
#23263=CARTESIAN_POINT('Ctrl Pts',(5.52472552840709,-0.0421985334635265,
3.2240906117739));
#23264=CARTESIAN_POINT('Ctrl Pts',(5.5184299838814,0.0598790266433576,3.2221936727435));
#23265=CARTESIAN_POINT('Ctrl Pts',(5.51213230589621,0.161991179205344,3.22029609087076));
#23266=CARTESIAN_POINT('Ctrl Pts',(5.50583462791101,0.264008536143621,3.21354030846408));
#23267=CARTESIAN_POINT('Ctrl Pts',(5.49953694992581,0.365449234025181,3.20196258876496));
#23268=CARTESIAN_POINT('Ctrl Pts',(5.49323828256693,0.466905868376912,3.19038305019049));
#23269=CARTESIAN_POINT('Ctrl Pts',(5.48693961520804,0.567785257085751,3.1739801198557));
#23270=CARTESIAN_POINT('Ctrl Pts',(5.48064094784916,0.667612633620952,3.15284172357727));
#23271=CARTESIAN_POINT('Ctrl Pts',(5.4743369347914,0.767524733965719,3.1316853870752));
#23272=CARTESIAN_POINT('Ctrl Pts',(5.46803292173365,0.866382639234982,3.10578564917918));
#23273=CARTESIAN_POINT('Ctrl Pts',(5.46172890867589,0.963723735270517,3.07528114561519));
#23274=CARTESIAN_POINT('Ctrl Pts',(5.45789490800369,1.02292504469274,3.05672879077419));
#23275=CARTESIAN_POINT('Ctrl Pts',(5.45406090733147,1.08156559106839,3.03647416526322));
#23276=CARTESIAN_POINT('Ctrl Pts',(5.45022690665927,1.13954465120736,3.01455727270269));
#23277=CARTESIAN_POINT('Ctrl Pts',(5.44377733481477,1.23707726682557,2.97768858506739));
#23278=CARTESIAN_POINT('Ctrl Pts',(5.43732776297028,1.3328707593346,2.93606296465374));
#23279=CARTESIAN_POINT('Ctrl Pts',(5.43087819112579,1.42645823164935,2.88986755334216));
#23280=CARTESIAN_POINT('Ctrl Pts',(5.4244325190837,1.51998911530078,2.84370007457874));
#23281=CARTESIAN_POINT('Ctrl Pts',(5.41798684704161,1.61131629666718,2.79296847706825));
#23282=CARTESIAN_POINT('Ctrl Pts',(5.41154117499952,1.6999944996087,2.73790727815976));
#23283=CARTESIAN_POINT('Ctrl Pts',(5.40509850259378,1.78863143418289,2.68287170320063));
#23284=CARTESIAN_POINT('Ctrl Pts',(5.39865583018805,1.87462152487066,2.62351074129486));
#23285=CARTESIAN_POINT('Ctrl Pts',(5.39221315778232,1.95754597646872,2.56010376987167));
#23286=CARTESIAN_POINT('Ctrl Pts',(5.38577258757756,2.04044337037202,2.4967174877198));
#23287=CARTESIAN_POINT('Ctrl Pts',(5.37933201737281,2.12027681787577,2.42928805744418));
#23288=CARTESIAN_POINT('Ctrl Pts',(5.37289144716806,2.19665857014442,2.3581366984785));
#23289=CARTESIAN_POINT('Ctrl Pts',(5.36645112620017,2.27303736659577,2.28698809292462));
#23290=CARTESIAN_POINT('Ctrl Pts',(5.36001080523229,2.34596445307008,2.21211810038558));
#23291=CARTESIAN_POINT('Ctrl Pts',(5.35357048426441,2.41508719131533,2.13388645922051));
#23292=CARTESIAN_POINT('Ctrl Pts',(5.34713071684206,2.48420398846185,2.05566154206429));
#23293=CARTESIAN_POINT('Ctrl Pts',(5.3406909494197,2.5495168407891,1.97407583878954));
#23294=CARTESIAN_POINT('Ctrl Pts',(5.33425118199735,2.61071225711959,1.88952350422681));
#23295=CARTESIAN_POINT('Ctrl Pts',(5.32780971588266,2.6719238156766,1.80494886631164));
#23296=CARTESIAN_POINT('Ctrl Pts',(5.32136824976798,2.72901554704453,1.71740634179815));
#23297=CARTESIAN_POINT('Ctrl Pts',(5.31492678365329,2.78171631680616,1.62732046484839));
#23298=CARTESIAN_POINT('Ctrl Pts',(5.31209641215022,2.80487296379731,1.58773685229682));
#23299=CARTESIAN_POINT('Ctrl Pts',(5.30926604064715,2.82718241532643,1.54766255399543));
#23300=CARTESIAN_POINT('Ctrl Pts',(5.30643566914408,2.84862442585767,1.5071351773836));
#23301=CARTESIAN_POINT('Ctrl Pts',(5.49126248314343,-2.84862442585767,1.50713517738358));
#23302=CARTESIAN_POINT('Ctrl Pts',(5.48481986387308,-2.79981715441166,1.59938541988801));
#23303=CARTESIAN_POINT('Ctrl Pts',(5.47837724460274,-2.74651246554549,1.68928621588219));
#23304=CARTESIAN_POINT('Ctrl Pts',(5.47193462533239,-2.68896195208233,1.77640118857019));
#23305=CARTESIAN_POINT('Ctrl Pts',(5.46549345124158,-2.63142434809293,1.86349662001718));
#23306=CARTESIAN_POINT('Ctrl Pts',(5.45905227715078,-2.56964302641709,1.94780715736535));
#23307=CARTESIAN_POINT('Ctrl Pts',(5.45261110305997,-2.50391336653128,2.02892469436546));
#23308=CARTESIAN_POINT('Ctrl Pts',(5.44617048313234,-2.43818936166382,2.11003525245893));
#23309=CARTESIAN_POINT('Ctrl Pts',(5.43972986320472,-2.36851793483692,2.18795306374967));
#23310=CARTESIAN_POINT('Ctrl Pts',(5.43328924327709,-2.29523504761997,2.26230272922899));
#23311=CARTESIAN_POINT('Ctrl Pts',(5.42684828700312,-2.22194833337513,2.33665627744621));
#23312=CARTESIAN_POINT('Ctrl Pts',(5.42040733072914,-2.14505005001677,2.40744103965874));
#23313=CARTESIAN_POINT('Ctrl Pts',(5.41396637445516,-2.06491308370881,2.4743183948773));
#23314=CARTESIAN_POINT('Ctrl Pts',(5.40752203871037,-1.98473407076575,2.54123083961673));
#23315=CARTESIAN_POINT('Ctrl Pts',(5.40107770296558,-1.90131327063422,2.60423153763966));
#23316=CARTESIAN_POINT('Ctrl Pts',(5.3946333672208,-1.81505683736707,2.66302201260655));
#23317=CARTESIAN_POINT('Ctrl Pts',(5.38818750074876,-1.72877991555328,2.72182645211317));
#23318=CARTESIAN_POINT('Ctrl Pts',(5.38174163427671,-1.6396663353765,2.77641846750094));
#23319=CARTESIAN_POINT('Ctrl Pts',(5.37529576780467,-1.54815059006993,2.82654335062566));
#23320=CARTESIAN_POINT('Ctrl Pts',(5.36884511979071,-1.45656695840953,2.87670541637441));
#23321=CARTESIAN_POINT('Ctrl Pts',(5.36239447177675,-1.36257793772757,2.9223935535854));
#23322=CARTESIAN_POINT('Ctrl Pts',(5.3559438237628,-1.26664209768339,2.96339929116483));
#23323=CARTESIAN_POINT('Ctrl Pts',(5.35311963105128,-1.22463991439267,2.98135223247424));
#23324=CARTESIAN_POINT('Ctrl Pts',(5.35029543833976,-1.18226482780987,2.99840825960803));
#23325=CARTESIAN_POINT('Ctrl Pts',(5.34747124562824,-1.13955645269919,3.01455281154795));
#23326=CARTESIAN_POINT('Ctrl Pts',(5.34116863780042,-1.04424633516078,3.05058179038433));
#23327=CARTESIAN_POINT('Ctrl Pts',(5.3348660299726,-0.947147233815046,3.08211640860091));
#23328=CARTESIAN_POINT('Ctrl Pts',(5.32856342214479,-0.84871055291417,3.10898825341495));
#23329=CARTESIAN_POINT('Ctrl Pts',(5.32226500048531,-0.750339253285435,
3.13584225005102));
#23330=CARTESIAN_POINT('Ctrl Pts',(5.31596657882584,-0.650632535932309,
3.15803952760407));
#23331=CARTESIAN_POINT('Ctrl Pts',(5.30966815716637,-0.550057803653538,
3.17546122242736));
#23332=CARTESIAN_POINT('Ctrl Pts',(5.30337251966971,-0.44952752956525,3.19287521614113));
#23333=CARTESIAN_POINT('Ctrl Pts',(5.29707688217306,-0.348130407377017,
3.20551775872895));
#23334=CARTESIAN_POINT('Ctrl Pts',(5.2907812446764,-0.246344217693348,3.21332103732401));
#23335=CARTESIAN_POINT('Ctrl Pts',(5.28448699217943,-0.144580420315566,
3.22112259924806));
#23336=CARTESIAN_POINT('Ctrl Pts',(5.27819273968245,-0.0424281341942792,
3.22408698618299));
#23337=CARTESIAN_POINT('Ctrl Pts',(5.27189848718548,0.0596302381179428,
3.22219828645011));
#23338=CARTESIAN_POINT('Ctrl Pts',(5.26560209762197,0.161723261968531,3.22030894545331));
#23339=CARTESIAN_POINT('Ctrl Pts',(5.25930570805847,0.26372189824142,3.21356322893573));
#23340=CARTESIAN_POINT('Ctrl Pts',(5.25300931849496,0.365144450726462,3.20199735986832));
#23341=CARTESIAN_POINT('Ctrl Pts',(5.24671193719046,0.466582978224168,3.19042966906698));
#23342=CARTESIAN_POINT('Ctrl Pts',(5.24041455588597,0.567444834820857,3.17404036790822));
#23343=CARTESIAN_POINT('Ctrl Pts',(5.23411717458147,0.667255420232703,3.15291734218804));
#23344=CARTESIAN_POINT('Ctrl Pts',(5.22781443317866,0.76715096072735,3.13177633732875));
#23345=CARTESIAN_POINT('Ctrl Pts',(5.22151169177585,0.865993042988278,3.10589365218794));
#23346=CARTESIAN_POINT('Ctrl Pts',(5.21520895037304,0.963319219118907,3.07540788263543));
#23347=CARTESIAN_POINT('Ctrl Pts',(5.21136596961972,1.02266206658176,3.05681974484695));
#23348=CARTESIAN_POINT('Ctrl Pts',(5.20752298886639,1.08144162827987,3.03652128491847));
#23349=CARTESIAN_POINT('Ctrl Pts',(5.20368000811307,1.13955645269916,3.01455281154796));
#23350=CARTESIAN_POINT('Ctrl Pts',(5.19722961026351,1.23710149976634,2.97767898821057));
#23351=CARTESIAN_POINT('Ctrl Pts',(5.19077921241396,1.33290671942348,2.93604710292728));
#23352=CARTESIAN_POINT('Ctrl Pts',(5.18432881456441,1.42650512526415,2.88984440586256));
#23353=CARTESIAN_POINT('Ctrl Pts',(5.17788230728269,1.52004707707577,2.84366957602888));
#23354=CARTESIAN_POINT('Ctrl Pts',(5.17143580000098,1.61138452748375,2.79292959402038));
#23355=CARTESIAN_POINT('Ctrl Pts',(5.16498929271926,1.70007211851932,2.73785908226359));
#23356=CARTESIAN_POINT('Ctrl Pts',(5.15854577953673,1.78871851834361,2.68281414816721));
#23357=CARTESIAN_POINT('Ctrl Pts',(5.15210226635419,1.87471718947248,2.62344289164424));
#23358=CARTESIAN_POINT('Ctrl Pts',(5.14565875317165,1.95764926030105,2.56002479209533));
#23359=CARTESIAN_POINT('Ctrl Pts',(5.13921734033849,2.04055429831095,2.49662736452492));
#23360=CARTESIAN_POINT('Ctrl Pts',(5.13277592750534,2.1203944274837,2.42918595312001));
#23361=CARTESIAN_POINT('Ctrl Pts',(5.12633451467218,2.19678182610023,2.35802187670423));
#23362=CARTESIAN_POINT('Ctrl Pts',(5.11989335703403,2.27316619841126,2.28686061965709));
#23363=CARTESIAN_POINT('Ctrl Pts',(5.11345219939589,2.34609783200353,2.21197724610014));
#23364=CARTESIAN_POINT('Ctrl Pts',(5.10701104175774,2.41522401822815,2.13373159143175));
#23365=CARTESIAN_POINT('Ctrl Pts',(5.10057044299562,2.48434420662283,2.05549272585669));
#23366=CARTESIAN_POINT('Ctrl Pts',(5.0941298442335,2.54965935757275,1.97389244712996));
#23367=CARTESIAN_POINT('Ctrl Pts',(5.08768924547138,2.61085590980442,1.88932500664637));
#23368=CARTESIAN_POINT('Ctrl Pts',(5.08124696382397,2.67206845228505,1.80473546925737));
#23369=CARTESIAN_POINT('Ctrl Pts',(5.07480468217656,2.72916002482629,1.71717752912428));
#23370=CARTESIAN_POINT('Ctrl Pts',(5.06836240052915,2.78185942295809,1.62707581673359));
#23371=CARTESIAN_POINT('Ctrl Pts',(5.06553785721873,2.804964859914,1.58757177097474));
#23372=CARTESIAN_POINT('Ctrl Pts',(5.0627133139083,2.82722656789367,1.54757910157298));
#23373=CARTESIAN_POINT('Ctrl Pts',(5.05988877059788,2.84862442585765,1.50713517738362));
#23374=CARTESIAN_POINT('Origin',(13.3346225254169,0.,0.));
#23375=CARTESIAN_POINT('Ctrl Pts',(6.11626248314343,2.84862442585767,-1.50713517738359));
#23376=CARTESIAN_POINT('Ctrl Pts',(6.10982035582423,2.79982088127992,-1.59937837576342));
#23377=CARTESIAN_POINT('Ctrl Pts',(6.10337822850504,2.74652053778117,-1.68927261412125));
#23378=CARTESIAN_POINT('Ctrl Pts',(6.09693610118584,2.68897491888786,-1.77638156038956));
#23379=CARTESIAN_POINT('Ctrl Pts',(6.09049542621811,2.63144227342083,-1.86347086829939));
#23380=CARTESIAN_POINT('Ctrl Pts',(6.08405475125038,2.56966646883176,-1.94777581926405));
#23381=CARTESIAN_POINT('Ctrl Pts',(6.07761407628265,2.50394281760817,-2.02888834799959));
#23382=CARTESIAN_POINT('Ctrl Pts',(6.07117396043016,2.43822487185728,-2.10999383535336));
#23383=CARTESIAN_POINT('Ctrl Pts',(6.06473384457767,2.3685600017985,-2.18790715876599));
#23384=CARTESIAN_POINT('Ctrl Pts',(6.05829372872518,2.29528410403912,-2.26225295761666));
#23385=CARTESIAN_POINT('Ctrl Pts',(6.05185327926446,2.22200441047183,-2.33660260769782));
#23386=CARTESIAN_POINT('Ctrl Pts',(6.04541282980374,2.14511358362727,-2.40738409599932));
#23387=CARTESIAN_POINT('Ctrl Pts',(6.03897238034302,2.06498444621732,-2.47425883839596));
#23388=CARTESIAN_POINT('Ctrl Pts',(6.03252855005019,1.9848132460348,-2.54116868583893));
#23389=CARTESIAN_POINT('Ctrl Pts',(6.02608471975735,1.9014006298802,-2.6041674462957));
#23390=CARTESIAN_POINT('Ctrl Pts',(6.01964088946452,1.81515268946992,-2.66295667940921));
#23391=CARTESIAN_POINT('Ctrl Pts',(6.01319552663167,1.72888423666039,-2.72175989440119));
#23392=CARTESIAN_POINT('Ctrl Pts',(6.00675016379883,1.6397794329097,-2.77635137873808));
#23393=CARTESIAN_POINT('Ctrl Pts',(6.00030480096598,1.54827270906505,-2.82647646034146));
#23394=CARTESIAN_POINT('Ctrl Pts',(5.99385464874034,1.45669798879331,-2.87663878867724));
#23395=CARTESIAN_POINT('Ctrl Pts',(5.9874044965147,1.36271811887205,-2.92232790764606));
#23396=CARTESIAN_POINT('Ctrl Pts',(5.98095434428906,1.2667916062669,-2.96333538243509));
#23397=CARTESIAN_POINT('Ctrl Pts',(5.97812664473545,1.22473812483214,-2.98131275941767));
#23398=CARTESIAN_POINT('Ctrl Pts',(5.97529894518185,1.18231078976918,-2.99839099999396));
#23399=CARTESIAN_POINT('Ctrl Pts',(5.97247124562824,1.13954936768589,-3.01455548980388));
#23400=CARTESIAN_POINT('Ctrl Pts',(5.96616787538459,1.04422768643007,-3.05058858389328));
#23401=CARTESIAN_POINT('Ctrl Pts',(5.95986450514094,0.947116827229342,-3.08212614604685));
#23402=CARTESIAN_POINT('Ctrl Pts',(5.95356113489729,0.848668314441946,-3.1089997836221));
#23403=CARTESIAN_POINT('Ctrl Pts',(5.9472619449681,0.750285091448085,-3.1358555989449));
#23404=CARTESIAN_POINT('Ctrl Pts',(5.94096275503892,0.650566373990987,-3.15805353625163));
#23405=CARTESIAN_POINT('Ctrl Pts',(5.93466356510973,0.549979677785018,-3.17547475450892));
#23406=CARTESIAN_POINT('Ctrl Pts',(5.92836715532296,0.449437375436762,-3.1928882839255));
#23407=CARTESIAN_POINT('Ctrl Pts',(5.9220707455362,0.348028259806088,-3.2055292203786));
#23408=CARTESIAN_POINT('Ctrl Pts',(5.91577433574944,0.246230218691873,-3.21332977484462));
#23409=CARTESIAN_POINT('Ctrl Pts',(5.90947930877286,0.144454534344897,-3.22112861616195));
#23410=CARTESIAN_POINT('Ctrl Pts',(5.90318428179628,0.0422905027743748,
-3.22408916141321));
#23411=CARTESIAN_POINT('Ctrl Pts',(5.8968892548197,-0.0597793703575645,
-3.22219552314562));
#23412=CARTESIAN_POINT('Ctrl Pts',(5.89059209293653,-0.161883859646896,
-3.22030124266619));
#23413=CARTESIAN_POINT('Ctrl Pts',(5.88429493105337,-0.263893716779201,
-3.2135494928278));
#23414=CARTESIAN_POINT('Ctrl Pts',(5.8779977691702,-0.365327145324713,-3.20197652074291));
#23415=CARTESIAN_POINT('Ctrl Pts',(5.87169961696178,-0.466776525832027,
-3.19040172863073));
#23416=CARTESIAN_POINT('Ctrl Pts',(5.86540146475336,-0.567648890954547,
-3.17400425846124));
#23417=CARTESIAN_POINT('Ctrl Pts',(5.85910331254494,-0.667469540774835,
-3.15287202002204));
#23418=CARTESIAN_POINT('Ctrl Pts',(5.85279980886301,-0.767375007148562,
-3.13172182574269));
#23419=CARTESIAN_POINT('Ctrl Pts',(5.84649630518108,-0.866226573654231,
-3.10582891961319));
#23420=CARTESIAN_POINT('Ctrl Pts',(5.84019280149915,-0.963561692753684,
-3.07533192139607));
#23421=CARTESIAN_POINT('Ctrl Pts',(5.83635520370379,-1.02281969549554,-3.05676522912006));
#23422=CARTESIAN_POINT('Ctrl Pts',(5.83251760590843,-1.08151592530543,-3.03649304338117));
#23423=CARTESIAN_POINT('Ctrl Pts',(5.82868000811307,-1.13954936768585,-3.01455548980389));
#23424=CARTESIAN_POINT('Ctrl Pts',(5.82223010676624,-1.23708694148339,-2.97768475349715));
#23425=CARTESIAN_POINT('Ctrl Pts',(5.81578020541942,-1.33288511130044,-2.93605663404916));
#23426=CARTESIAN_POINT('Ctrl Pts',(5.8093303040726,-1.42647694442399,-2.88985831651429));
#23427=CARTESIAN_POINT('Ctrl Pts',(5.80288429885277,-1.52001224247094,-2.84368790553208));
#23428=CARTESIAN_POINT('Ctrl Pts',(5.79643829363293,-1.61134351954702,-2.79295296362187));
#23429=CARTESIAN_POINT('Ctrl Pts',(5.78999228841309,-1.70002546687168,-2.73788805002829));
#23430=CARTESIAN_POINT('Ctrl Pts',(5.78354928062754,-1.78866617651503,-2.68284874197707));
#23431=CARTESIAN_POINT('Ctrl Pts',(5.77710627284198,-1.87465968941073,-2.62348367385894));
#23432=CARTESIAN_POINT('Ctrl Pts',(5.77066326505643,-1.95758717987831,-2.56007226376055));
#23433=CARTESIAN_POINT('Ctrl Pts',(5.76422235873842,-2.04048762250796,-2.49668153608646));
#23434=CARTESIAN_POINT('Ctrl Pts',(5.75778145242042,-2.12032373491512,-2.42924732695385));
#23435=CARTESIAN_POINT('Ctrl Pts',(5.75134054610242,-2.19670773918908,-2.35809089542511));
#23436=CARTESIAN_POINT('Ctrl Pts',(5.74489989140302,-2.27308875946739,-2.28693724367316));
#23437=CARTESIAN_POINT('Ctrl Pts',(5.73845923670362,-2.34601765950018,-2.21206191394668));
#23438=CARTESIAN_POINT('Ctrl Pts',(5.73201858200422,-2.41514177295116,-2.13382468329672));
#23439=CARTESIAN_POINT('Ctrl Pts',(5.72557848297815,-2.48425992265654,-2.0555942026348));
#23440=CARTESIAN_POINT('Ctrl Pts',(5.71913838395208,-2.54957369178943,-1.97400268573327));
#23441=CARTESIAN_POINT('Ctrl Pts',(5.712698284926,-2.61076956120682,-1.88944432592653));
#23442=CARTESIAN_POINT('Ctrl Pts',(5.7062564935142,-2.67198151221173,-1.80486374513205));
#23443=CARTESIAN_POINT('Ctrl Pts',(5.6998147021024,-2.72907318027611,-1.7173150718364));
#23444=CARTESIAN_POINT('Ctrl Pts',(5.69337291069059,-2.7817734030335,-1.62722287861111));
#23445=CARTESIAN_POINT('Ctrl Pts',(5.69054486399302,-2.80490962111365,-1.58767100348194));
#23446=CARTESIAN_POINT('Ctrl Pts',(5.68771681729545,-2.82720002732681,-1.54762926569109));
#23447=CARTESIAN_POINT('Ctrl Pts',(5.68488877059788,-2.84862442585766,-1.50713517738361));
#23448=CARTESIAN_POINT('Ctrl Pts',(6.36280938168963,2.84862442585767,-1.50713517738359));
#23449=CARTESIAN_POINT('Ctrl Pts',(6.35636801520394,2.79982664511693,-1.59936748158012));
#23450=CARTESIAN_POINT('Ctrl Pts',(6.34992664871825,2.74653302174499,-1.68925157837877));
#23451=CARTESIAN_POINT('Ctrl Pts',(6.34348528223255,2.68899497203504,-1.77635120482135));
#23452=CARTESIAN_POINT('Ctrl Pts',(6.33704537919698,2.63146999471675,-1.86343104261215));
#23453=CARTESIAN_POINT('Ctrl Pts',(6.3306054761614,2.56970272181874,-1.94772735437613));
#23454=CARTESIAN_POINT('Ctrl Pts',(6.32416557312583,2.50398836217138,-2.02883213810564));
#23455=CARTESIAN_POINT('Ctrl Pts',(6.31772623687936,2.43827978617998,-2.10992978363631));
#23456=CARTESIAN_POINT('Ctrl Pts',(6.3112869006329,2.36862505518029,-2.18783616676831));
#23457=CARTESIAN_POINT('Ctrl Pts',(6.30484756438643,2.2953599652657,-2.26217598615922));
#23458=CARTESIAN_POINT('Ctrl Pts',(6.29840789879005,2.2220911280935,-2.33651960777647));
#23459=CARTESIAN_POINT('Ctrl Pts',(6.29196823319366,2.14521183132221,-2.40729603306182));
#23460=CARTESIAN_POINT('Ctrl Pts',(6.28552856759727,2.06509479949499,-2.47416673480158));
#23461=CARTESIAN_POINT('Ctrl Pts',(6.27908551911379,1.9849356805641,-2.54107256507885));
#23462=CARTESIAN_POINT('Ctrl Pts',(6.2726424706303,1.90153571941476,-2.60406832868935));
#23463=CARTESIAN_POINT('Ctrl Pts',(6.26619942214681,1.81530091132731,-2.66285564081763));
#23464=CARTESIAN_POINT('Ctrl Pts',(6.25975483835675,1.72904555444717,-2.72165696130652));
#23465=CARTESIAN_POINT('Ctrl Pts',(6.25331025456669,1.63995432172068,-2.77624762357214));
#23466=CARTESIAN_POINT('Ctrl Pts',(6.24686567077663,1.54846154749456,-2.82637301119841));
#23467=CARTESIAN_POINT('Ctrl Pts',(6.24041628551254,1.45690060747319,-2.87653574425374));
#23468=CARTESIAN_POINT('Ctrl Pts',(6.23396690024845,1.36293488768221,-2.92222638010325));
#23469=CARTESIAN_POINT('Ctrl Pts',(6.22751751498436,1.26702279812037,-2.96323653992442));
#23470=CARTESIAN_POINT('Ctrl Pts',(6.22468439138106,1.22488997558715,-2.98125172230338));
#23471=CARTESIAN_POINT('Ctrl Pts',(6.22185126777775,1.18238182695123,-2.99836432568748));
#23472=CARTESIAN_POINT('Ctrl Pts',(6.21901814417444,1.13953835446524,-3.01455965295143));
#23473=CARTESIAN_POINT('Ctrl Pts',(6.21271358172062,1.04419858612223,-3.05059918616363));
#23474=CARTESIAN_POINT('Ctrl Pts',(6.2064090192668,0.947069335931392,-3.08214135506957));
#23475=CARTESIAN_POINT('Ctrl Pts',(6.20010445681298,0.84860231617677,-3.10901779851442));
#23476=CARTESIAN_POINT('Ctrl Pts',(6.19380406548531,0.750200442633861,-3.13587646038652));
#23477=CARTESIAN_POINT('Ctrl Pts',(6.18750367415763,0.650462954403152,-3.15807543117493));
#23478=CARTESIAN_POINT('Ctrl Pts',(6.18120328282995,0.549857543880931,-3.17549590519925));
#23479=CARTESIAN_POINT('Ctrl Pts',(6.17490566533694,0.449296426286045,-3.19290870961828));
#23480=CARTESIAN_POINT('Ctrl Pts',(6.16860804784393,0.347868549735401,-3.20554713469663));
#23481=CARTESIAN_POINT('Ctrl Pts',(6.16231043035092,0.246051969765162,-3.21334342868525));
#23482=CARTESIAN_POINT('Ctrl Pts',(6.15601419223677,0.144257690869664,-3.22113801503711));
#23483=CARTESIAN_POINT('Ctrl Pts',(6.14971795412262,0.0420752860446296,
-3.22409255138702));
#23484=CARTESIAN_POINT('Ctrl Pts',(6.14342171600848,-0.0600125776946586,
-3.22219118815418));
#23485=CARTESIAN_POINT('Ctrl Pts',(6.13712334637876,-0.162135002050547,
-3.22028918123772));
#23486=CARTESIAN_POINT('Ctrl Pts',(6.13082497674903,-0.264162411682084,
-3.21352799363139));
#23487=CARTESIAN_POINT('Ctrl Pts',(6.12452660711931,-0.365612853322439,
-3.20194391018728));
#23488=CARTESIAN_POINT('Ctrl Pts',(6.11822724939808,-0.467079210560954,
-3.19035800942613));
#23489=CARTESIAN_POINT('Ctrl Pts',(6.11192789167685,-0.567968013507524,
-3.17394776016987));
#23490=CARTESIAN_POINT('Ctrl Pts',(6.10562853395562,-0.667804406318028,
-3.15280110971216));
#23491=CARTESIAN_POINT('Ctrl Pts',(6.09932383828838,-0.767725398431793,
-3.13163654001835));
#23492=CARTESIAN_POINT('Ctrl Pts',(6.09301914262114,-0.86659179974346,-3.10572764459076));
#23493=CARTESIAN_POINT('Ctrl Pts',(6.08671444695391,-0.963940906770531,
-3.07521308054489));
#23494=CARTESIAN_POINT('Ctrl Pts',(6.08288526685569,-1.02306624491239,-3.05667994785821));
#23495=CARTESIAN_POINT('Ctrl Pts',(6.07905608675748,-1.08163217204868,-3.03644885848091));
#23496=CARTESIAN_POINT('Ctrl Pts',(6.07522690665927,-1.13953835446521,-3.01455965295144));
#23497=CARTESIAN_POINT('Ctrl Pts',(6.06877777336206,-1.23706437297518,-2.97769369193402));
#23498=CARTESIAN_POINT('Ctrl Pts',(6.06232864006486,-1.33285164201609,-2.93607139738089));
#23499=CARTESIAN_POINT('Ctrl Pts',(6.05587950676766,-1.42643331191441,-2.88987985375878));
#23500=CARTESIAN_POINT('Ctrl Pts',(6.04943427814655,-1.5199583220893,-2.84371627715297));
#23501=CARTESIAN_POINT('Ctrl Pts',(6.04298904952543,-1.61128005392832,-2.79298913024698));
#23502=CARTESIAN_POINT('Ctrl Pts',(6.03654382090432,-1.69995327473113,-2.73793287467588));
#23503=CARTESIAN_POINT('Ctrl Pts',(6.03010159483563,-1.78858518652693,-2.68290226742595));
#23504=CARTESIAN_POINT('Ctrl Pts',(6.02365936876695,-1.87457072385523,-2.62354676971529));
#23505=CARTESIAN_POINT('Ctrl Pts',(6.01721714269827,-1.9574911320762,-2.56014570490491));
#23506=CARTESIAN_POINT('Ctrl Pts',(6.01077701979519,-2.04038446963108,-2.49676533836522));
#23507=CARTESIAN_POINT('Ctrl Pts',(6.00433689689211,-2.12021437140274,-2.42934226726545));
#23508=CARTESIAN_POINT('Ctrl Pts',(5.99789677398903,-2.19659312725626,-2.35819765833794));
#23509=CARTESIAN_POINT('Ctrl Pts',(5.99145689714146,-2.27296896493357,-2.28705576760744));
#23510=CARTESIAN_POINT('Ctrl Pts',(5.98501702029389,-2.34589363843928,-2.21219287712536));
#23511=CARTESIAN_POINT('Ctrl Pts',(5.97857714344631,-2.41501454690557,-2.13396867379409));
#23512=CARTESIAN_POINT('Ctrl Pts',(5.97213781730877,-2.48412954445493,-2.0557511598536));
#23513=CARTESIAN_POINT('Ctrl Pts',(5.96569849117122,-2.54944117691125,-1.97417319267129));
#23514=CARTESIAN_POINT('Ctrl Pts',(5.95925916503367,-2.61063599032593,-1.88962887586821));
#23515=CARTESIAN_POINT('Ctrl Pts',(5.9528181318071,-2.67184702671059,-1.80506214605598));
#23516=CARTESIAN_POINT('Ctrl Pts',(5.94637709858052,-2.72893884225502,-1.71752780370473));
#23517=CARTESIAN_POINT('Ctrl Pts',(5.93993606535394,-2.78164033975134,-1.62745033188975));
#23518=CARTESIAN_POINT('Ctrl Pts',(5.93710259995065,-2.80482417759292,-1.58782448444805));
#23519=CARTESIAN_POINT('Ctrl Pts',(5.93426913454737,-2.82715897690467,-1.54770685477331));
#23520=CARTESIAN_POINT('Ctrl Pts',(5.93143566914408,-2.84862442585766,-1.50713517738361));
#23521=CARTESIAN_POINT('Origin',(13.3346225254169,0.,0.));
#23522=CARTESIAN_POINT('Ctrl Pts',(6.98780938168963,-2.84862442585767,1.50713517738359));
#23523=CARTESIAN_POINT('Ctrl Pts',(6.9813684199558,-2.79982971139062,1.59936168604016));
#23524=CARTESIAN_POINT('Ctrl Pts',(6.97492745822197,-2.74653966288739,1.68924038781867));
#23525=CARTESIAN_POINT('Ctrl Pts',(6.96848649648814,-2.68900563955951,1.77633505649051));
#23526=CARTESIAN_POINT('Ctrl Pts',(6.96204700411376,-2.63148474131515,1.86340985648754));
#23527=CARTESIAN_POINT('Ctrl Pts',(6.95560751173937,-2.56972200671623,1.94770157259629));
#23528=CARTESIAN_POINT('Ctrl Pts',(6.94916801936499,-2.50401258941778,2.0288022364285));
#23529=CARTESIAN_POINT('Ctrl Pts',(6.94272909787128,-2.43830899745991,2.1098957104391));
#23530=CARTESIAN_POINT('Ctrl Pts',(6.93629017637757,-2.3686596595625,2.18779840172598));
#23531=CARTESIAN_POINT('Ctrl Pts',(6.92985125488386,-2.29540031832038,2.26213504043298));
#23532=CARTESIAN_POINT('Ctrl Pts',(6.92341200631891,-2.22213725579923,2.33647545514137));
#23533=CARTESIAN_POINT('Ctrl Pts',(6.91697275775396,-2.14526409186646,2.40724918715468));
#23534=CARTESIAN_POINT('Ctrl Pts',(6.91053350918901,-2.06515349881969,2.47411773948064));
#23535=CARTESIAN_POINT('Ctrl Pts',(6.90409087667113,-1.98500080606625,2.54102143255805));
#23536=CARTESIAN_POINT('Ctrl Pts',(6.89764824415326,-1.90160757612952,2.60401560177531));
#23537=CARTESIAN_POINT('Ctrl Pts',(6.89120561163538,-1.81537975297001,2.66280189180618));
#23538=CARTESIAN_POINT('Ctrl Pts',(6.88476144235891,-1.72913136192184,2.72160220410762));
#23539=CARTESIAN_POINT('Ctrl Pts',(6.87831727308244,-1.64004734757743,2.77619242868343));
#23540=CARTESIAN_POINT('Ctrl Pts',(6.87187310380597,-1.54856199293611,2.82631797866655));
#23541=CARTESIAN_POINT('Ctrl Pts',(6.8654241266606,-1.45700838285753,2.87648092634403));
#23542=CARTESIAN_POINT('Ctrl Pts',(6.85897514951523,-1.36305018959993,2.92217236843239));
#23543=CARTESIAN_POINT('Ctrl Pts',(6.85252617236985,-1.2671457715718,2.9631839558299));
#23544=CARTESIAN_POINT('Ctrl Pts',(6.84969016297138,-1.22497073749248,2.98121925734884));
#23545=CARTESIAN_POINT('Ctrl Pts',(6.84685415357291,-1.18241959261408,2.99835014558505));
#23546=CARTESIAN_POINT('Ctrl Pts',(6.84401814417444,-1.13953246495152,3.01456187924904));
#23547=CARTESIAN_POINT('Ctrl Pts',(6.8377129402968,-1.04418296301259,3.05060487897125));
#23548=CARTESIAN_POINT('Ctrl Pts',(6.83140773641917,-0.947043815550281,
3.08214952814751));
#23549=CARTESIAN_POINT('Ctrl Pts',(6.82510253254154,-0.848566836014205,
3.10902748256056));
#23550=CARTESIAN_POINT('Ctrl Pts',(6.81880149482907,-0.750154925168804,
3.13588767735801));
#23551=CARTESIAN_POINT('Ctrl Pts',(6.81250045711659,-0.650407334833339,
3.15808720518624));
#23552=CARTESIAN_POINT('Ctrl Pts',(6.80619941940412,-0.54979185252027,3.1755072793811));
#23553=CARTESIAN_POINT('Ctrl Pts',(6.79990115212197,-0.449220608663864,
3.19291969434519));
#23554=CARTESIAN_POINT('Ctrl Pts',(6.79360288483982,-0.347782635016613,
3.20555676842139));
#23555=CARTESIAN_POINT('Ctrl Pts',(6.78730461755768,-0.245956077419378,
3.21335076990989));
#23556=CARTESIAN_POINT('Ctrl Pts',(6.78100772780445,-0.144151790872555,
3.22114306672915));
#23557=CARTESIAN_POINT('Ctrl Pts',(6.77471083805123,-0.0419594974512284,
3.22409436944162));
#23558=CARTESIAN_POINT('Ctrl Pts',(6.768413948298,0.060138048957664,3.2221888488367));
#23559=CARTESIAN_POINT('Ctrl Pts',(6.76211492886047,0.162270125992154,3.22028268376165));
#23560=CARTESIAN_POINT('Ctrl Pts',(6.75581590942294,0.264306982419248,3.21351641681952));
#23561=CARTESIAN_POINT('Ctrl Pts',(6.74951688998541,0.365766580528667,3.20192635316123));
#23562=CARTESIAN_POINT('Ctrl Pts',(6.74321688366827,0.467242074510221,3.19033447366517));
#23563=CARTESIAN_POINT('Ctrl Pts',(6.73691687735114,0.568139724143099,3.173917346508));
#23564=CARTESIAN_POINT('Ctrl Pts',(6.73061687103401,0.667984589626474,3.15276293915695));
#23565=CARTESIAN_POINT('Ctrl Pts',(6.72431153406959,0.767913937209478,3.13159063235017));
#23566=CARTESIAN_POINT('Ctrl Pts',(6.71800619710517,0.86678832208374,3.10567313109845));
#23567=CARTESIAN_POINT('Ctrl Pts',(6.71170086014075,0.964144956797867,3.07514911260921));
#23568=CARTESIAN_POINT('Ctrl Pts',(6.70787620898025,1.02319892457826,3.05663404776865));
#23569=CARTESIAN_POINT('Ctrl Pts',(6.70405155781976,1.08169475021288,3.03642507406251));
#23570=CARTESIAN_POINT('Ctrl Pts',(6.70022690665927,1.13953246495153,3.01456187924904));
#23571=CARTESIAN_POINT('Ctrl Pts',(6.6937781820509,1.23705233766024,2.9776984591632));
#23572=CARTESIAN_POINT('Ctrl Pts',(6.68732945744253,1.33283380889837,2.93607926380706));
#23573=CARTESIAN_POINT('Ctrl Pts',(6.68088073283417,1.42641007316879,2.88989132419588));
#23574=CARTESIAN_POINT('Ctrl Pts',(6.6744359174242,1.51992961177559,2.84373138358152));
#23575=CARTESIAN_POINT('Ctrl Pts',(6.66799110201424,1.61124626690784,2.79300838362011));
#23576=CARTESIAN_POINT('Ctrl Pts',(6.66154628660428,1.69991484634418,2.73795673407719));
#23577=CARTESIAN_POINT('Ctrl Pts',(6.65510447644813,1.78854207912121,2.68293075542934));
#23578=CARTESIAN_POINT('Ctrl Pts',(6.64866266629199,1.8745233746496,2.62358034887997));
#23579=CARTESIAN_POINT('Ctrl Pts',(6.64222085613585,1.95744001609221,2.56018478745205));
#23580=CARTESIAN_POINT('Ctrl Pts',(6.63578115003153,2.04032957494374,2.49680993255586));
#23581=CARTESIAN_POINT('Ctrl Pts',(6.6293414439272,2.12015617361231,2.42939278637265));
#23582=CARTESIAN_POINT('Ctrl Pts',(6.62290173782288,2.19653213803325,2.35825446656782));
#23583=CARTESIAN_POINT('Ctrl Pts',(6.61646227479629,2.27290521951257,2.28711883200074));
#23584=CARTESIAN_POINT('Ctrl Pts',(6.61002281176971,2.34582764520509,2.21226255849171));
#23585=CARTESIAN_POINT('Ctrl Pts',(6.60358334874312,2.41494684908908,2.13404528503374));
#23586=CARTESIAN_POINT('Ctrl Pts',(6.59714443377973,2.48406017023226,2.05583466865398));
#23587=CARTESIAN_POINT('Ctrl Pts',(6.59070551881635,2.54937066628114,1.9742639092255));
#23588=CARTESIAN_POINT('Ctrl Pts',(6.58426660385296,2.61056491799165,1.88972706268689));
#23589=CARTESIAN_POINT('Ctrl Pts',(6.57782597397146,2.6717754679654,1.80516770089988));
#23590=CARTESIAN_POINT('Ctrl Pts',(6.57138534408995,2.72886736191435,1.71764098199117));
#23591=CARTESIAN_POINT('Ctrl Pts',(6.56494471420844,2.78156953731932,1.6275713414647));
#23592=CARTESIAN_POINT('Ctrl Pts',(6.56210836585366,2.80477871580865,1.58790614078966));
#23593=CARTESIAN_POINT('Ctrl Pts',(6.55927201749887,2.8271371365645,1.54774813502967));
#23594=CARTESIAN_POINT('Ctrl Pts',(6.55643566914408,2.84862442585766,1.50713517738362));
#23595=CARTESIAN_POINT('Ctrl Pts',(6.74126248314343,-2.84862442585767,1.50713517738358));
#23596=CARTESIAN_POINT('Ctrl Pts',(6.7348208129161,-2.79982434406511,1.59937183078017));
#23597=CARTESIAN_POINT('Ctrl Pts',(6.72837914268876,-2.74652803790824,1.68925997627709));
#23598=CARTESIAN_POINT('Ctrl Pts',(6.72193747246143,-2.68898696649982,1.77636332333621));
#23599=CARTESIAN_POINT('Ctrl Pts',(6.71549726125213,-2.63145892796298,1.86344694176137));
#23600=CARTESIAN_POINT('Ctrl Pts',(6.70905705004283,-2.56968824914852,1.94774670241053));
#23601=CARTESIAN_POINT('Ctrl Pts',(6.70261683883353,-2.50397018027766,2.02885457802679));
#23602=CARTESIAN_POINT('Ctrl Pts',(6.69617719134728,-2.43825786382539,2.1099553541275));
#23603=CARTESIAN_POINT('Ctrl Pts',(6.68973754386104,-2.36859908529649,2.18786450789556));
#23604=CARTESIAN_POINT('Ctrl Pts',(6.68329789637479,-2.29532968091904,2.26220671433716));
#23605=CARTESIAN_POINT('Ctrl Pts',(6.6768579178349,-2.22205650985969,2.33655274261197));
#23606=CARTESIAN_POINT('Ctrl Pts',(6.67041793929501,-2.14517261031037,2.40733118911841));
#23607=CARTESIAN_POINT('Ctrl Pts',(6.66397796075512,-2.06505074601119,2.47420350393791));
#23608=CARTESIAN_POINT('Ctrl Pts',(6.6575346001408,-1.98488680422579,2.54111093799645));
#23609=CARTESIAN_POINT('Ctrl Pts',(6.65109123952648,-1.90148179122128,2.60410789805176));
#23610=CARTESIAN_POINT('Ctrl Pts',(6.64464787891216,-1.81524174078208,2.66289597713137));
#23611=CARTESIAN_POINT('Ctrl Pts',(6.63820298409013,-1.72898115600406,2.72169805404991));
#23612=CARTESIAN_POINT('Ctrl Pts',(6.63175808926811,-1.63988450576559,2.7762890446133));
#23613=CARTESIAN_POINT('Ctrl Pts',(6.62531319444608,-1.54838616294132,2.8264143102015));
#23614=CARTESIAN_POINT('Ctrl Pts',(6.61886350296394,-1.45681972180614,2.87657688188527));
#23615=CARTESIAN_POINT('Ctrl Pts',(6.61241381148181,-1.36284835328739,2.92226691237498));
#23616=CARTESIAN_POINT('Ctrl Pts',(6.60596411999967,-1.26693050609646,2.96327600051399));
#23617=CARTESIAN_POINT('Ctrl Pts',(6.60313316187586,-1.22482935916943,2.98127608804355));
#23618=CARTESIAN_POINT('Ctrl Pts',(6.60030220375205,-1.18235347438299,2.9983749717808));
#23619=CARTESIAN_POINT('Ctrl Pts',(6.59747124562824,-1.1395427597969,3.01455798768152));
#23620=CARTESIAN_POINT('Ctrl Pts',(6.59116716115003,-1.04421024355315,3.05059493873793));
#23621=CARTESIAN_POINT('Ctrl Pts',(6.58486307667181,-0.947088367349843,
3.08213526022758));
#23622=CARTESIAN_POINT('Ctrl Pts',(6.5785589921936,-0.848628768111771,3.10901057837266));
#23623=CARTESIAN_POINT('Ctrl Pts',(6.57225908253034,-0.750234372728276,
3.13586809861535));
#23624=CARTESIAN_POINT('Ctrl Pts',(6.56595917286709,-0.650504410890921,
3.15806665478402));
#23625=CARTESIAN_POINT('Ctrl Pts',(6.55965926320383,-0.549906504144592,
3.17548742702589));
#23626=CARTESIAN_POINT('Ctrl Pts',(6.55336212990721,-0.44935293083903,3.19290052194325));
#23627=CARTESIAN_POINT('Ctrl Pts',(6.54706499661059,-0.347932576815247,
3.20553995383521));
#23628=CARTESIAN_POINT('Ctrl Pts',(6.54076786331396,-0.246123430343797,
3.2133379560102));
#23629=CARTESIAN_POINT('Ctrl Pts',(6.53447211077298,-0.144336607292632,
3.22113424833802));
#23630=CARTESIAN_POINT('Ctrl Pts',(6.528176358232,-0.0421615695926382,3.22409119397625));
#23631=CARTESIAN_POINT('Ctrl Pts',(6.52188060569102,0.0599190804475121,
3.22219292816217));
#23632=CARTESIAN_POINT('Ctrl Pts',(6.51558272027298,0.162034313402983,3.220294019253));
#23633=CARTESIAN_POINT('Ctrl Pts',(6.50928483485493,0.264054685027798,3.21353661588369));
#23634=CARTESIAN_POINT('Ctrl Pts',(6.50298694943689,0.365498304951598,3.20195698777755));
#23635=CARTESIAN_POINT('Ctrl Pts',(6.49668807502886,0.466957855099198,3.19037554126167));
#23636=CARTESIAN_POINT('Ctrl Pts',(6.49038920062083,0.567840067045023,3.17397041608279));
#23637=CARTESIAN_POINT('Ctrl Pts',(6.4840903262128,0.667670147477321,3.15282954449929));
#23638=CARTESIAN_POINT('Ctrl Pts',(6.47778610842939,0.767584914404384,3.13167073897942));
#23639=CARTESIAN_POINT('Ctrl Pts',(6.47148189064597,0.866445367585899,3.10576825487636));
#23640=CARTESIAN_POINT('Ctrl Pts',(6.46517767286255,0.963788866079588,3.07526073433149));
#23641=CARTESIAN_POINT('Ctrl Pts',(6.46134511794606,1.02296739013412,3.05671414348212));
#23642=CARTESIAN_POINT('Ctrl Pts',(6.45751256302956,1.08158555679706,3.03646657637891));
#23643=CARTESIAN_POINT('Ctrl Pts',(6.45368000811307,1.13954275979688,3.01455798768153));
#23644=CARTESIAN_POINT('Ctrl Pts',(6.44723056816595,1.23707339103231,2.97769012010794));
#23645=CARTESIAN_POINT('Ctrl Pts',(6.44078112821883,1.33286501155701,2.93606550000405));
#23646=CARTESIAN_POINT('Ctrl Pts',(6.43433168827171,1.4264507385462,2.88987125197663));
#23647=CARTESIAN_POINT('Ctrl Pts',(6.42788614959502,1.5199798554682,2.84370494687992));
#23648=CARTESIAN_POINT('Ctrl Pts',(6.42144061091833,1.61130539763696,2.79297468800413));
#23649=CARTESIAN_POINT('Ctrl Pts',(6.41499507224163,1.69998210197784,2.73791497593607));
#23650=CARTESIAN_POINT('Ctrl Pts',(6.40855253408015,1.78861752570373,2.68288089516308));
#23651=CARTESIAN_POINT('Ctrl Pts',(6.40210999591867,1.87460624675235,2.62352157678041));
#23652=CARTESIAN_POINT('Ctrl Pts',(6.39566745775719,1.95752948212021,2.56011638195028));
#23653=CARTESIAN_POINT('Ctrl Pts',(6.38922702208823,2.04042565587394,2.49673187911206));
#23654=CARTESIAN_POINT('Ctrl Pts',(6.38278658641927,2.12025803682909,2.42930436156649));
#23655=CARTESIAN_POINT('Ctrl Pts',(6.3763461507503,2.19663888778923,2.35815503289163));
#23656=CARTESIAN_POINT('Ctrl Pts',(6.36990596336282,2.27301679423575,2.28700844705302));
#23657=CARTESIAN_POINT('Ctrl Pts',(6.36346577597533,2.34594315489066,2.2121405907003));
#23658=CARTESIAN_POINT('Ctrl Pts',(6.35702558858784,2.41506534274487,2.13391118671153));
#23659=CARTESIAN_POINT('Ctrl Pts',(6.35058595389354,2.48418159857257,2.05568849632534));
#23660=CARTESIAN_POINT('Ctrl Pts',(6.34414631919925,2.54949408396817,1.97410511993885));
#23661=CARTESIAN_POINT('Ctrl Pts',(6.33770668450495,2.61068931895004,1.88955519697631));
#23662=CARTESIAN_POINT('Ctrl Pts',(6.33126534859332,2.6719007204381,1.80498293768557));
#23663=CARTESIAN_POINT('Ctrl Pts',(6.3248240126817,2.72899247713051,1.71744287422061));
#23664=CARTESIAN_POINT('Ctrl Pts',(6.31838267677007,2.78169346579974,1.62735952537448));
#23665=CARTESIAN_POINT('Ctrl Pts',(6.31555137471267,2.80485829056485,1.58776320957532));
#23666=CARTESIAN_POINT('Ctrl Pts',(6.31272007265528,2.82717536573749,1.54767587836842));
#23667=CARTESIAN_POINT('Ctrl Pts',(6.30988877059788,2.84862442585767,1.5071351773836));
#23668=CARTESIAN_POINT('Origin',(13.3346225254169,0.,0.));
#23669=CARTESIAN_POINT('Ctrl Pts',(7.36626248314343,2.84862442585767,-1.50713517738359));
#23670=CARTESIAN_POINT('Ctrl Pts',(7.3598212383318,2.7998275668816,-1.59936573935991));
#23671=CARTESIAN_POINT('Ctrl Pts',(7.35337999352017,2.74653501817546,-1.6892482143296));
#23672=CARTESIAN_POINT('Ctrl Pts',(7.34693874870854,2.68899817887566,-1.77634635037861));
#23673=CARTESIAN_POINT('Ctrl Pts',(7.34049896912302,2.63147442780365,-1.86342467372571));
#23674=CARTESIAN_POINT('Ctrl Pts',(7.3340591895375,2.56970851921407,-1.94771960395087));
#23675=CARTESIAN_POINT('Ctrl Pts',(7.32761940995198,2.50399564535328,-2.02882314915614));
#23676=CARTESIAN_POINT('Ctrl Pts',(7.32118019838482,2.438288567672,-2.10991954065347));
#23677=CARTESIAN_POINT('Ctrl Pts',(7.31474098681766,2.36863545796846,-2.18782481394358));
#23678=CARTESIAN_POINT('Ctrl Pts',(7.30830177525049,2.29537209625576,-2.26216367715301));
#23679=CARTESIAN_POINT('Ctrl Pts',(7.30186223501736,2.22210499508307,-2.33650633471747));
#23680=CARTESIAN_POINT('Ctrl Pts',(7.29542269478422,2.14522754200268,-2.40728195035351));
#23681=CARTESIAN_POINT('Ctrl Pts',(7.28898315455109,2.0651124458537,-2.47415200593661));
#23682=CARTESIAN_POINT('Ctrl Pts',(7.28254023110834,1.9849552587862,-2.54105719375067));
#23683=CARTESIAN_POINT('Ctrl Pts',(7.2760973076656,1.90155732121291,-2.6040524780719));
#23684=CARTESIAN_POINT('Ctrl Pts',(7.26965438422285,1.81532461298809,-2.66283948295417));
#23685=CARTESIAN_POINT('Ctrl Pts',(7.26320992503554,1.72907135020997,-2.72164050039212));
#23686=CARTESIAN_POINT('Ctrl Pts',(7.25676546584822,1.63998228752049,-2.77623103110752));
#23687=CARTESIAN_POINT('Ctrl Pts',(7.2503210066609,1.54849174383152,-2.82635646757192));
#23688=CARTESIAN_POINT('Ctrl Pts',(7.24387174407473,1.45693300736477,-2.87651926519532));
#23689=CARTESIAN_POINT('Ctrl Pts',(7.23742248148855,1.36296955024028,-2.92221014346359));
#23690=CARTESIAN_POINT('Ctrl Pts',(7.23097321890238,1.26705976694849,-2.96322073249369));
#23691=CARTESIAN_POINT('Ctrl Pts',(7.228139227811,1.22491425530386,-2.98124196242664));
#23692=CARTESIAN_POINT('Ctrl Pts',(7.22530523671962,1.18239318176599,-2.99836006216386));
#23693=CARTESIAN_POINT('Ctrl Pts',(7.22247124562824,1.1395365863639,-3.01456032131356));
#23694=CARTESIAN_POINT('Ctrl Pts',(7.21616649090883,1.04419390058717,-3.05060089343833));
#23695=CARTESIAN_POINT('Ctrl Pts',(7.20986173618941,0.947061683914143,-3.08214380566377));
#23696=CARTESIAN_POINT('Ctrl Pts',(7.20355698147,0.848591678948619,-3.10902070191229));
#23697=CARTESIAN_POINT('Ctrl Pts',(7.19725639639098,0.75018679697814,-3.13587982316442));
#23698=CARTESIAN_POINT('Ctrl Pts',(7.19095581131196,0.650446280904561,-3.15807896084573));
#23699=CARTESIAN_POINT('Ctrl Pts',(7.18465522623294,0.549837851630633,-3.17549931497618));
#23700=CARTESIAN_POINT('Ctrl Pts',(7.17835741396893,0.449273698969032,-3.19291200260919));
#23701=CARTESIAN_POINT('Ctrl Pts',(7.17205960170492,0.347842796098622,-3.20555002271385));
#23702=CARTESIAN_POINT('Ctrl Pts',(7.16576178944092,0.246023225619735,-3.21334562955118));
#23703=CARTESIAN_POINT('Ctrl Pts',(7.15946535600154,0.144225947220338,-3.22113952964111));
#23704=CARTESIAN_POINT('Ctrl Pts',(7.15316892256216,0.0420405785782795,
-3.22409309677057));
#23705=CARTESIAN_POINT('Ctrl Pts',(7.14687248912278,-0.0600501872561559,
-3.22219048746509));
#23706=CARTESIAN_POINT('Ctrl Pts',(7.14057392471624,-0.162175504725535,
-3.22028723423984));
#23707=CARTESIAN_POINT('Ctrl Pts',(7.1342753603097,-0.264205745761719,-3.21352452423829));
#23708=CARTESIAN_POINT('Ctrl Pts',(7.12797679590316,-0.365658931790838,
-3.2019386483975));
#23709=CARTESIAN_POINT('Ctrl Pts',(7.12167724376763,-0.467128027517231,
-3.1903509556815));
#23710=CARTESIAN_POINT('Ctrl Pts',(7.1153776916321,-0.568019482016492,-3.17393864498104));
#23711=CARTESIAN_POINT('Ctrl Pts',(7.10907813949657,-0.667858414283587,
-3.15278966963713));
#23712=CARTESIAN_POINT('Ctrl Pts',(7.10277325160128,-0.767781910746003,
-3.13162278097984));
#23713=CARTESIAN_POINT('Ctrl Pts',(7.09646836370599,-0.866650704941091,
-3.10571130622614));
#23714=CARTESIAN_POINT('Ctrl Pts',(7.09016347581069,-0.964002068221984,
-3.07519390851435));
#23715=CARTESIAN_POINT('Ctrl Pts',(7.08633565324482,-1.02310601287161,-3.0566661907257));
#23716=CARTESIAN_POINT('Ctrl Pts',(7.08250783067894,-1.08165092699262,-3.03644173009248));
#23717=CARTESIAN_POINT('Ctrl Pts',(7.07868000811307,-1.13953658636387,-3.01456032131357));
#23718=CARTESIAN_POINT('Ctrl Pts',(7.07223099766582,-1.2370607572487,-2.97769512409316));
#23719=CARTESIAN_POINT('Ctrl Pts',(7.06578198721857,-1.33284628329249,-2.93607376116759));
#23720=CARTESIAN_POINT('Ctrl Pts',(7.05933297677132,-1.42642632810164,-2.88988330093076));
#23721=CARTESIAN_POINT('Ctrl Pts',(7.05288787236158,-1.51994969333675,-2.84372081733806));
#23722=CARTESIAN_POINT('Ctrl Pts',(7.04644276795183,-1.61126989895293,-2.79299491705124));
#23723=CARTESIAN_POINT('Ctrl Pts',(7.03999766354209,-1.69994172441788,-2.73794004610824));
#23724=CARTESIAN_POINT('Ctrl Pts',(7.03355556249848,-1.78857222953475,-2.68291083028645));
#23725=CARTESIAN_POINT('Ctrl Pts',(7.02711346145488,-1.87455649163518,-2.62355686305991));
#23726=CARTESIAN_POINT('Ctrl Pts',(7.02067136041127,-1.95747576744255,-2.5601574526531));
#23727=CARTESIAN_POINT('Ctrl Pts',(7.01423136280101,-2.04036796898196,-2.4967787430135));
#23728=CARTESIAN_POINT('Ctrl Pts',(7.00779136519075,-2.12019687772764,-2.42935745305116));
#23729=CARTESIAN_POINT('Ctrl Pts',(7.00135136758049,-2.19657479438669,-2.35821473474428));
#23730=CARTESIAN_POINT('Ctrl Pts',(6.99491161513201,-2.27294980344431,-2.28707472474209));
#23731=CARTESIAN_POINT('Ctrl Pts',(6.98847186268353,-2.34587380117559,-2.21221382345213));
#23732=CARTESIAN_POINT('Ctrl Pts',(6.98203211023506,-2.41499419718648,-2.13399170337085));
#23733=CARTESIAN_POINT('Ctrl Pts',(6.97559290770146,-2.48410869074474,-2.05577626297292));
#23734=CARTESIAN_POINT('Ctrl Pts',(6.96915370516785,-2.54941998155791,-1.97420046257777));
#23735=CARTESIAN_POINT('Ctrl Pts',(6.96271450263425,-2.61061462610829,-1.88965839146908));
#23736=CARTESIAN_POINT('Ctrl Pts',(6.9562735906587,-2.67182551625611,-1.80509387662426));
#23737=CARTESIAN_POINT('Ctrl Pts',(6.94983267868315,-2.72891735537074,-1.71756182601585));
#23738=CARTESIAN_POINT('Ctrl Pts',(6.9433917667076,-2.78161905667021,-1.62748670841551));
#23739=CARTESIAN_POINT('Ctrl Pts',(6.94055743467103,-2.80481051169119,-1.58784903094343));
#23740=CARTESIAN_POINT('Ctrl Pts',(6.93772310263445,-2.82715241156155,-1.54771926387705));
#23741=CARTESIAN_POINT('Ctrl Pts',(6.93488877059788,-2.84862442585766,-1.50713517738361));
#23742=CARTESIAN_POINT('Ctrl Pts',(7.61280938168963,2.84862442585768,-1.50713517738358));
#23743=CARTESIAN_POINT('Ctrl Pts',(7.60636879765673,2.79983257273495,-1.5993562778356));
#23744=CARTESIAN_POINT('Ctrl Pts',(7.59992821362384,2.74654586008821,-1.68922994525756));
#23745=CARTESIAN_POINT('Ctrl Pts',(7.59348762959095,2.68901559383708,-1.77631998767143));
#23746=CARTESIAN_POINT('Ctrl Pts',(7.58704852043615,2.63149850187716,-1.86339008667715));
#23747=CARTESIAN_POINT('Ctrl Pts',(7.58060941128135,2.56974000198426,-1.9476775144583));
#23748=CARTESIAN_POINT('Ctrl Pts',(7.57417030212655,2.504035196303,-2.0287743339701));
#23749=CARTESIAN_POINT('Ctrl Pts',(7.5677317676774,2.43833625493031,-2.10986391539985));
#23750=CARTESIAN_POINT('Ctrl Pts',(7.56129323322826,2.36869194922073,-2.18776316177445));
#23751=CARTESIAN_POINT('Ctrl Pts',(7.55485469877911,2.29543797182663,-2.26209683258618));
#23752=CARTESIAN_POINT('Ctrl Pts',(7.54841583939461,2.22218029750323,-2.33643425481643));
#23753=CARTESIAN_POINT('Ctrl Pts',(7.54197698001011,2.14531285588115,-2.40720547368891));
#23754=CARTESIAN_POINT('Ctrl Pts',(7.53553812062562,2.06520827048847,-2.47407202037573));
#23755=CARTESIAN_POINT('Ctrl Pts',(7.52909587631248,1.98506157386324,-2.54097371901651));
#23756=CARTESIAN_POINT('Ctrl Pts',(7.52265363199935,1.90167462457078,-2.60396640034054));
#23757=CARTESIAN_POINT('Ctrl Pts',(7.51621138768622,1.81545331866872,-2.66275173650018));
#23758=CARTESIAN_POINT('Ctrl Pts',(7.50976760527285,1.72921142723714,-2.72155110779024));
#23759=CARTESIAN_POINT('Ctrl Pts',(7.50332382285949,1.6401341480468,-2.77614092371629));
#23760=CARTESIAN_POINT('Ctrl Pts',(7.49688004044613,1.54865571617306,-2.82626662494261));
#23761=CARTESIAN_POINT('Ctrl Pts',(7.490431444218,1.45710894551977,-2.87642977247378));
#23762=CARTESIAN_POINT('Ctrl Pts',(7.48398284798987,1.36315777501308,-2.92212196647321));
#23763=CARTESIAN_POINT('Ctrl Pts',(7.47753425176174,1.26726051491456,-2.96313488552892));
#23764=CARTESIAN_POINT('Ctrl Pts',(7.47469554923264,1.22504608790665,-2.98118896628243));
#23765=CARTESIAN_POINT('Ctrl Pts',(7.47185684670354,1.18245481698266,-2.99833692023175));
#23766=CARTESIAN_POINT('Ctrl Pts',(7.46901814417444,1.1395269477687,-3.01456396478976));
#23767=CARTESIAN_POINT('Ctrl Pts',(7.46271233675157,1.04416828529453,-3.05061022781874));
#23768=CARTESIAN_POINT('Ctrl Pts',(7.4564065293287,0.94701982317167,-3.08215721203173));
#23769=CARTESIAN_POINT('Ctrl Pts',(7.45010072190583,0.848533470080481,-3.10903658914674));
#23770=CARTESIAN_POINT('Ctrl Pts',(7.44379907596876,0.750112112561231,-3.1358982273524));
#23771=CARTESIAN_POINT('Ctrl Pts',(7.43749743003169,0.650355014495849,-3.15809828004157));
#23772=CARTESIAN_POINT('Ctrl Pts',(7.43119578409462,0.549730052935245,-3.17551797844065));
#23773=CARTESIAN_POINT('Ctrl Pts',(7.42489690537768,0.449149278468226,-3.19293002738744));
#23774=CARTESIAN_POINT('Ctrl Pts',(7.41859802666074,0.347701801609882,-3.20556583037678));
#23775=CARTESIAN_POINT('Ctrl Pts',(7.4122991479438,0.245865853212699,-3.21335767457095));
#23776=CARTESIAN_POINT('Ctrl Pts',(7.4060016450126,0.144052147575286,-3.22114781688949));
#23777=CARTESIAN_POINT('Ctrl Pts',(7.3997041420814,0.0418505470841928,-3.22409607643666));
#23778=CARTESIAN_POINT('Ctrl Pts',(7.3934066391502,-0.0602561125912675,
-3.22218664316569));
#23779=CARTESIAN_POINT('Ctrl Pts',(7.38710700826225,-0.162397274601838,
-3.22027656468797));
#23780=CARTESIAN_POINT('Ctrl Pts',(7.38080737737429,-0.264443022243322,
-3.2135055172559));
#23781=CARTESIAN_POINT('Ctrl Pts',(7.37450774648634,-0.365911238306918,
-3.20190982511699));
#23782=CARTESIAN_POINT('Ctrl Pts',(7.36820712986566,-0.467395331577122,
-3.19031231854586));
#23783=CARTESIAN_POINT('Ctrl Pts',(7.36190651324498,-0.568301307493712,
-3.17388871794434));
#23784=CARTESIAN_POINT('Ctrl Pts',(7.3556058966243,-0.668154147213363,-3.15272700975863));
#23785=CARTESIAN_POINT('Ctrl Pts',(7.34929995623743,-0.768091358543565,
-3.13154742078549));
#23786=CARTESIAN_POINT('Ctrl Pts',(7.34299401585056,-0.866973257105538,
-3.10562181967257));
#23787=CARTESIAN_POINT('Ctrl Pts',(7.33668807546369,-0.964336976392172,
-3.07508890252994));
#23788=CARTESIAN_POINT('Ctrl Pts',(7.33286768586222,-1.02332379166532,-3.05659084641172));
#23789=CARTESIAN_POINT('Ctrl Pts',(7.32904729626074,-1.08175365751474,-3.03640268570416));
#23790=CARTESIAN_POINT('Ctrl Pts',(7.32522690665927,-1.13952694776869,-3.01456396478976));
#23791=CARTESIAN_POINT('Ctrl Pts',(7.31877856349444,-1.23704108642474,-2.97770291619869));
#23792=CARTESIAN_POINT('Ctrl Pts',(7.31233022032962,-1.33281714821767,-2.93608661322007));
#23793=CARTESIAN_POINT('Ctrl Pts',(7.3058818771648,-1.42638836887556,-2.88990203703111));
#23794=CARTESIAN_POINT('Ctrl Pts',(7.2994374474012,-1.51990280258513,-2.84374548955784));
#23795=CARTESIAN_POINT('Ctrl Pts',(7.29299301763761,-1.61121472114748,-2.79302635948626));
#23796=CARTESIAN_POINT('Ctrl Pts',(7.28654858787402,-1.69987897011956,-2.73797900821852));
#23797=CARTESIAN_POINT('Ctrl Pts',(7.28010716587054,-1.78850183749525,-2.68295734878599));
#23798=CARTESIAN_POINT('Ctrl Pts',(7.27366574386706,-1.87447917546878,-2.62361169306084));
#23799=CARTESIAN_POINT('Ctrl Pts',(7.26722432186358,-1.95739230248724,-2.56022126712979));
#23800=CARTESIAN_POINT('Ctrl Pts',(7.26078500472703,-2.04027833593858,-2.49685155532233));
#23801=CARTESIAN_POINT('Ctrl Pts',(7.25434568759048,-2.12010185286642,-2.42943993786715));
#23802=CARTESIAN_POINT('Ctrl Pts',(7.24790637045393,-2.19647521287681,-2.35830748667721));
#23803=CARTESIAN_POINT('Ctrl Pts',(7.24146729360321,-2.27284572298322,-2.28717768982453));
#23804=CARTESIAN_POINT('Ctrl Pts',(7.23502821675248,-2.34576605155333,-2.2123275907323));
#23805=CARTESIAN_POINT('Ctrl Pts',(7.22858913990176,-2.41488366509613,-2.13411678371917));
#23806=CARTESIAN_POINT('Ctrl Pts',(7.22215060863931,-2.4839954222467,-2.05591260357204));
#23807=CARTESIAN_POINT('Ctrl Pts',(7.21571207737686,-2.54930485806267,-1.97434856987299));
#23808=CARTESIAN_POINT('Ctrl Pts',(7.20927354611441,-2.6104985857016,-1.88981869409475));
#23809=CARTESIAN_POINT('Ctrl Pts',(7.20283329262207,-2.67170868192873,-1.80526620758855));
#23810=CARTESIAN_POINT('Ctrl Pts',(7.19639303912973,-2.72880064905917,-1.71774660236723));
#23811=CARTESIAN_POINT('Ctrl Pts',(7.1899527856374,-2.78150345696278,-1.62768426956953));
#23812=CARTESIAN_POINT('Ctrl Pts',(7.18711374680629,-2.80473628752211,-1.58798234474052));
#23813=CARTESIAN_POINT('Ctrl Pts',(7.18427470797519,-2.82711675435621,-1.54778665928234));
#23814=CARTESIAN_POINT('Ctrl Pts',(7.18143566914408,-2.84862442585767,-1.50713517738359));
#23815=CARTESIAN_POINT('Origin',(13.3346225254169,0.,0.));
#23816=CARTESIAN_POINT('Ctrl Pts',(8.23780938168963,-2.84862442585767,1.50713517738358));
#23817=CARTESIAN_POINT('Ctrl Pts',(8.23136915062113,-2.79983524668294,1.59935122382739));
#23818=CARTESIAN_POINT('Ctrl Pts',(8.22492891955262,-2.74655165133479,1.68922018669765));
#23819=CARTESIAN_POINT('Ctrl Pts',(8.21848868848412,-2.6890248959066,1.77630590600113));
#23820=CARTESIAN_POINT('Ctrl Pts',(8.21204993745551,-2.63151136079486,1.86337161199501));
#23821=CARTESIAN_POINT('Ctrl Pts',(8.20561118642689,-2.56975681800966,1.94765503247493));
#23822=CARTESIAN_POINT('Ctrl Pts',(8.19917243539828,-2.50405632153669,2.02874825965967));
#23823=CARTESIAN_POINT('Ctrl Pts',(8.19273426265664,-2.43836172585738,2.10983420357524));
#23824=CARTESIAN_POINT('Ctrl Pts',(8.18629608991499,-2.36872212233407,2.18773023083762));
#23825=CARTESIAN_POINT('Ctrl Pts',(8.17985791717335,-2.29547315692851,2.26206112833421));
#23826=CARTESIAN_POINT('Ctrl Pts',(8.17341942150152,-2.22222051745221,2.33639575416982));
#23827=CARTESIAN_POINT('Ctrl Pts',(8.16698092582969,-2.14535842278167,2.40716462462289));
#23828=CARTESIAN_POINT('Ctrl Pts',(8.16054243015786,-2.06525945085394,2.4740292971504));
#23829=CARTESIAN_POINT('Ctrl Pts',(8.15410054866333,-1.98511835714327,2.54092913191725));
#23830=CARTESIAN_POINT('Ctrl Pts',(8.14765866716881,-1.90173727652333,2.60392042275362));
#23831=CARTESIAN_POINT('Ctrl Pts',(8.14121678567428,-1.81552206027324,2.66270486745362));
#23832=CARTESIAN_POINT('Ctrl Pts',(8.13477336483815,-1.72928624217425,2.72150335918964));
#23833=CARTESIAN_POINT('Ctrl Pts',(8.12832994400202,-1.64021525630153,2.77609279305437));
#23834=CARTESIAN_POINT('Ctrl Pts',(8.12188652316589,-1.54874329293665,2.82621863540026));
#23835=CARTESIAN_POINT('Ctrl Pts',(8.11543828297856,-1.45720291319351,2.87638196932789));
#23836=CARTESIAN_POINT('Ctrl Pts',(8.10899004279122,-1.36325830479589,2.92207486561085));
#23837=CARTESIAN_POINT('Ctrl Pts',(8.10254180260388,-1.26736773300675,2.96308902867149));
#23838=CARTESIAN_POINT('Ctrl Pts',(8.0997005831274,-1.22511649045642,2.98116066302658));
#23839=CARTESIAN_POINT('Ctrl Pts',(8.09685936365092,-1.18248771812384,2.99832456767142));
#23840=CARTESIAN_POINT('Ctrl Pts',(8.09401814417444,-1.13952177176646,3.01456592135091));
#23841=CARTESIAN_POINT('Ctrl Pts',(8.08771176801016,-1.04415447535482,3.05061526092775));
#23842=CARTESIAN_POINT('Ctrl Pts',(8.08140539184588,-0.946997233950487,
3.08216444669572));
#23843=CARTESIAN_POINT('Ctrl Pts',(8.0750990156816,-0.848502046009037,3.10904516538735));
#23844=CARTESIAN_POINT('Ctrl Pts',(8.06879679658347,-0.750071784580219,
3.13590816472276));
#23845=CARTESIAN_POINT('Ctrl Pts',(8.06249457748534,-0.650305724995536,
3.15810871269302));
#23846=CARTESIAN_POINT('Ctrl Pts',(8.05619235838721,-0.549671828716999,
3.17552805738115));
#23847=CARTESIAN_POINT('Ctrl Pts',(8.04989290347794,-0.449082071033278,
3.1929397618464));
#23848=CARTESIAN_POINT('Ctrl Pts',(8.04359344856868,-0.347625636737641,
3.2055743671937));
#23849=CARTESIAN_POINT('Ctrl Pts',(8.03729399365941,-0.245780836828313,
3.213364178357));
#23850=CARTESIAN_POINT('Ctrl Pts',(8.03099591289099,-0.143958252984028,
3.22115229027841));
#23851=CARTESIAN_POINT('Ctrl Pts',(8.02469783212257,-0.0417478798431903,
3.22409768172038));
#23852=CARTESIAN_POINT('Ctrl Pts',(8.01839975135415,0.0603673698212518,
3.22218456069184));
#23853=CARTESIAN_POINT('Ctrl Pts',(8.01209954426089,0.16251709509833,3.22027079376546));
#23854=CARTESIAN_POINT('Ctrl Pts',(8.00579933716762,0.264571223385071,3.21349524051306));
#23855=CARTESIAN_POINT('Ctrl Pts',(7.99949913007435,0.366047562520342,3.20189424317433));
#23856=CARTESIAN_POINT('Ctrl Pts',(7.99319793833492,0.467539761179954,3.19029143274005));
#23857=CARTESIAN_POINT('Ctrl Pts',(7.9868967465955,0.568453585154214,3.17386173043288));
#23858=CARTESIAN_POINT('Ctrl Pts',(7.98059555485607,0.668313941075423,3.15269314058064));
#23859=CARTESIAN_POINT('Ctrl Pts',(7.97428904584675,0.768258564304382,3.13150668758283));
#23860=CARTESIAN_POINT('Ctrl Pts',(7.96798253683744,0.867147544787304,3.10557345163986));
#23861=CARTESIAN_POINT('Ctrl Pts',(7.96167602782812,0.964517941478652,3.07503214667193));
#23862=CARTESIAN_POINT('Ctrl Pts',(7.95785965410517,1.02344147948959,3.0565501253869));
#23863=CARTESIAN_POINT('Ctrl Pts',(7.95404328038221,1.08180919094779,3.03638158040879));
#23864=CARTESIAN_POINT('Ctrl Pts',(7.95022690665925,1.13952177176659,3.01456592135085));
#23865=CARTESIAN_POINT('Ctrl Pts',(7.94377892002184,1.23703055286201,2.97770708930154));
#23866=CARTESIAN_POINT('Ctrl Pts',(7.93733093338443,1.33280156031643,2.93609348956797));
#23867=CARTESIAN_POINT('Ctrl Pts',(7.93088294674702,1.42636806838486,2.88991205679205));
#23868=CARTESIAN_POINT('Ctrl Pts',(7.92443887742247,1.51987773246369,2.84375868038948));
#23869=CARTESIAN_POINT('Ctrl Pts',(7.91799480809792,1.61118522546438,2.7930431668641));
#23870=CARTESIAN_POINT('Ctrl Pts',(7.91155073877338,1.69984542825306,2.73799983245931));
#23871=CARTESIAN_POINT('Ctrl Pts',(7.90510967953751,1.78846421698174,2.6829822093419));
#23872=CARTESIAN_POINT('Ctrl Pts',(7.89866862030166,1.87443785730202,2.62364099324265));
#23873=CARTESIAN_POINT('Ctrl Pts',(7.89222756106579,1.95734770064261,2.5602553664213));
#23874=CARTESIAN_POINT('Ctrl Pts',(7.88578860744736,2.04023044030286,2.49689046070734));
#23875=CARTESIAN_POINT('Ctrl Pts',(7.87934965382892,2.12005107789844,2.42948400971865));
#23876=CARTESIAN_POINT('Ctrl Pts',(7.87291070021048,2.19642200451226,2.35835704264523));
#23877=CARTESIAN_POINT('Ctrl Pts',(7.86647198425604,2.27279011224884,2.2872327008927));
#23878=CARTESIAN_POINT('Ctrl Pts',(7.8600332683016,2.34570848149363,2.21238837156018));
#23879=CARTESIAN_POINT('Ctrl Pts',(7.85359455234716,2.41482460916936,2.13418360724893));
#23880=CARTESIAN_POINT('Ctrl Pts',(7.84715637966308,2.48393490513216,2.05598544150953));
#23881=CARTESIAN_POINT('Ctrl Pts',(7.84071820697899,2.54924335038943,1.97442769278971));
#23882=CARTESIAN_POINT('Ctrl Pts',(7.8342800342949,2.61043658839468,1.88990433103646));
#23883=CARTESIAN_POINT('Ctrl Pts',(7.82784013254177,2.67164626077324,1.80535826925087));
#23884=CARTESIAN_POINT('Ctrl Pts',(7.82140023078864,2.7287382963448,1.71784531159995));
#23885=CARTESIAN_POINT('Ctrl Pts',(7.81496032903552,2.78144169526556,1.62778980778792));
#23886=CARTESIAN_POINT('Ctrl Pts',(7.81211877573837,2.80469663341757,1.58805356279649));
#23887=CARTESIAN_POINT('Ctrl Pts',(7.80927722244123,2.8270977055468,1.54782266328821));
#23888=CARTESIAN_POINT('Ctrl Pts',(7.80643566914408,2.84862442585766,1.50713517738361));
#23889=CARTESIAN_POINT('Ctrl Pts',(7.99126248314343,-2.84862442585767,1.50713517738358));
#23890=CARTESIAN_POINT('Ctrl Pts',(7.98482163489325,-2.79983057110731,1.59936006109635));
#23891=CARTESIAN_POINT('Ctrl Pts',(7.97838078664307,-2.74654152490177,1.68923725024687));
#23892=CARTESIAN_POINT('Ctrl Pts',(7.97193993839289,-2.68900863044322,1.77633052889993));
#23893=CARTESIAN_POINT('Ctrl Pts',(7.96550056115981,-2.6314888758489,1.8634039164304));
#23894=CARTESIAN_POINT('Ctrl Pts',(7.95906118392673,-2.56972741363481,1.94769434405312));
#23895=CARTESIAN_POINT('Ctrl Pts',(7.95262180669365,-2.50401938198163,2.02879385280032));
#23896=CARTESIAN_POINT('Ctrl Pts',(7.94618300148975,-2.43831718736983,2.10988615723509));
#23897=CARTESIAN_POINT('Ctrl Pts',(7.93974419628585,-2.36866936148764,2.18778781344658));
#23898=CARTESIAN_POINT('Ctrl Pts',(7.93330539108195,-2.29541163192632,2.26212356040012));
#23899=CARTESIAN_POINT('Ctrl Pts',(7.92686625944756,-2.22215018839074,2.33646307598059));
#23900=CARTESIAN_POINT('Ctrl Pts',(7.92042712781316,-2.14527874384496,2.40723605288399));
#23901=CARTESIAN_POINT('Ctrl Pts',(7.91398799617877,-2.06516995593504,2.47410400258422));
#23902=CARTESIAN_POINT('Ctrl Pts',(7.90754548029631,-1.98501906483074,2.54100709642228));
#23903=CARTESIAN_POINT('Ctrl Pts',(7.90110296441384,-1.90162772204247,2.60400081859401));
#23904=CARTESIAN_POINT('Ctrl Pts',(7.89466044853138,-1.81540185713925,2.66278682203352));
#23905=CARTESIAN_POINT('Ctrl Pts',(7.88821639548582,-1.72915541902836,2.72158685162003));
#23906=CARTESIAN_POINT('Ctrl Pts',(7.88177234244027,-1.64007342840465,2.77617695343437));
#23907=CARTESIAN_POINT('Ctrl Pts',(7.87532828939471,-1.54859015386917,2.82630254888599));
#23908=CARTESIAN_POINT('Ctrl Pts',(7.86887942669151,-1.45703859882338,2.87646555665429));
#23909=CARTESIAN_POINT('Ctrl Pts',(7.86243056398832,-1.36308251569372,2.92215722470595));
#23910=CARTESIAN_POINT('Ctrl Pts',(7.85598170128512,-1.267180248423,2.96316921226356));
#23911=CARTESIAN_POINT('Ctrl Pts',(7.85314488273283,-1.22499337865672,2.98121015568635));
#23912=CARTESIAN_POINT('Ctrl Pts',(7.85030806418053,-1.18243017790787,2.99834617116936));
#23913=CARTESIAN_POINT('Ctrl Pts',(7.84747124562824,-1.13953080950289,3.01456250502352));
#23914=CARTESIAN_POINT('Ctrl Pts',(7.84116586093479,-1.04417856334637,3.05060648224064));
#23915=CARTESIAN_POINT('Ctrl Pts',(7.83486047624134,-0.947036625504087,
3.08215183084003));
#23916=CARTESIAN_POINT('Ctrl Pts',(7.82855509154788,-0.848556837951724,
3.10903021137868));
#23917=CARTESIAN_POINT('Ctrl Pts',(7.82225387161886,-0.750142097202377,
3.13589083850043));
#23918=CARTESIAN_POINT('Ctrl Pts',(7.81595265168983,-0.650391658679559,
3.15809052349607));
#23919=CARTESIAN_POINT('Ctrl Pts',(7.80965143176081,-0.549773336716463,
3.17551048506152));
#23920=CARTESIAN_POINT('Ctrl Pts',(7.80335298130107,-0.449199237833256,
3.19292279032405));
#23921=CARTESIAN_POINT('Ctrl Pts',(7.79705453084133,-0.347758417372287,
3.20555948358099));
#23922=CARTESIAN_POINT('Ctrl Pts',(7.79075608038159,-0.245929046638912,
3.2133528387837));
#23923=CARTESIAN_POINT('Ctrl Pts',(7.78445900692879,-0.144121938484396,
3.22114449015398));
#23924=CARTESIAN_POINT('Ctrl Pts',(7.77816193347599,-0.0419268570160417,
3.22409488121527));
#23925=CARTESIAN_POINT('Ctrl Pts',(7.77186486002319,0.0601734193822794,
3.22218818849859));
#23926=CARTESIAN_POINT('Ctrl Pts',(7.76556565740319,0.162308217937866,3.22028085109076));
#23927=CARTESIAN_POINT('Ctrl Pts',(7.75926645478319,0.264347737840848,3.21351315207759));
#23928=CARTESIAN_POINT('Ctrl Pts',(7.75296725216318,0.365809917568325,3.20192140233152));
#23929=CARTESIAN_POINT('Ctrl Pts',(7.74666706300651,0.467287987586547,3.19032783716739));
#23930=CARTESIAN_POINT('Ctrl Pts',(7.74036687384983,0.568188131474593,3.17390877081012));
#23931=CARTESIAN_POINT('Ctrl Pts',(7.73406668469315,0.668035385755841,3.15275217641318));
#23932=CARTESIAN_POINT('Ctrl Pts',(7.72776116694932,0.767967089056463,3.13157768814762));
#23933=CARTESIAN_POINT('Ctrl Pts',(7.7214556492055,0.866843724786049,3.10565776049382));
#23934=CARTESIAN_POINT('Ctrl Pts',(7.71515013146167,0.964202481813624,3.07513107632251));
#23935=CARTESIAN_POINT('Ctrl Pts',(7.71132675701214,1.02323633108352,3.05662110631983));
#23936=CARTESIAN_POINT('Ctrl Pts',(7.7075033825626,1.08171239565747,3.03641836763166));
#23937=CARTESIAN_POINT('Ctrl Pts',(7.70368000811307,1.13953080950288,3.01456250502353));
#23938=CARTESIAN_POINT('Ctrl Pts',(7.6972313981056,1.23704895925796,2.97769979743446));
#23939=CARTESIAN_POINT('Ctrl Pts',(7.69078278809813,1.33282880508769,2.93608147108646));
#23940=CARTESIAN_POINT('Ctrl Pts',(7.68433417809066,1.42640355388129,2.88989454201617));
#23941=CARTESIAN_POINT('Ctrl Pts',(7.67788947854617,1.51992155857184,2.84373562088494));
#23942=CARTESIAN_POINT('Ctrl Pts',(7.67144477900168,1.61123679047021,2.79301378365583));
#23943=CARTESIAN_POINT('Ctrl Pts',(7.66500007945719,1.69990406870537,2.73796342555903));
#23944=CARTESIAN_POINT('Ctrl Pts',(7.65855838592108,1.78852998976323,2.68293874466203));
#23945=CARTESIAN_POINT('Ctrl Pts',(7.65211669238497,1.87451009612947,2.62358976554795));
#23946=CARTESIAN_POINT('Ctrl Pts',(7.64567499884886,1.95742568156753,2.56019574713339));
#23947=CARTESIAN_POINT('Ctrl Pts',(7.63923540961072,2.04031418110074,2.49682243754385));
#23948=CARTESIAN_POINT('Ctrl Pts',(7.63279582037259,2.12013985376864,2.42940695253737));
#23949=CARTESIAN_POINT('Ctrl Pts',(7.62635623113445,2.19651503562203,2.35827039602891));
#23950=CARTESIAN_POINT('Ctrl Pts',(7.61991688413659,2.27288734444354,2.28713651548913));
#23951=CARTESIAN_POINT('Ctrl Pts',(7.61347753713873,2.34580913998748,2.21228209717184));
#23952=CARTESIAN_POINT('Ctrl Pts',(7.60703819014087,2.41492786600483,2.13406676664376));
#23953=CARTESIAN_POINT('Ctrl Pts',(7.60059939046314,2.48404071719197,2.05585808412285));
#23954=CARTESIAN_POINT('Ctrl Pts',(7.59416059078541,2.54935089465948,1.9742893455314));
#23955=CARTESIAN_POINT('Ctrl Pts',(7.58772179110768,2.61054498889689,1.8897545934447));
#23956=CARTESIAN_POINT('Ctrl Pts',(7.5812812743156,2.67175540252035,1.80519729743));
#23957=CARTESIAN_POINT('Ctrl Pts',(7.57484075752352,2.72884731845376,1.7176727159187));
#23958=CARTESIAN_POINT('Ctrl Pts',(7.56840024073143,2.78154968390752,1.62760527108202));
#23959=CARTESIAN_POINT('Ctrl Pts',(7.56556308402025,2.80476596835634,1.58792903642151));
#23960=CARTESIAN_POINT('Ctrl Pts',(7.56272592730906,2.82713101270891,1.54775970968128));
#23961=CARTESIAN_POINT('Ctrl Pts',(7.55988877059788,2.84862442585767,1.5071351773836));
#23962=CARTESIAN_POINT('Origin',(13.3346225254169,0.,0.));
#23963=CARTESIAN_POINT('Ctrl Pts',(8.61626248314343,2.84862442585767,-1.50713517738358));
#23964=CARTESIAN_POINT('Ctrl Pts',(8.60982200511013,2.79983337575478,-1.59935476005409));
#23965=CARTESIAN_POINT('Ctrl Pts',(8.60338152707683,2.74654759928038,-1.68922701463086));
#23966=CARTESIAN_POINT('Ctrl Pts',(8.59694104904353,2.68901838739325,-1.77631575874364));
#23967=CARTESIAN_POINT('Ctrl Pts',(8.59050204743798,2.63150236361482,-1.86338453846292));
#23968=CARTESIAN_POINT('Ctrl Pts',(8.58406304583242,2.56974505211714,-1.94767076278352));
#23969=CARTESIAN_POINT('Ctrl Pts',(8.57762404422686,2.50404154058441,-2.0287665034517));
#23970=CARTESIAN_POINT('Ctrl Pts',(8.57118561840174,2.43834390430984,-2.10985499247685));
#23971=CARTESIAN_POINT('Ctrl Pts',(8.56474719257662,2.36870101076993,-2.18775327209251));
#23972=CARTESIAN_POINT('Ctrl Pts',(8.55830876675151,2.29544853859728,-2.26208611002137));
#23973=CARTESIAN_POINT('Ctrl Pts',(8.55187001659225,2.22219237634915,-2.33642269244887));
#23974=CARTESIAN_POINT('Ctrl Pts',(8.545431266433,2.14532654054445,-2.40719320604775));
#23975=CARTESIAN_POINT('Ctrl Pts',(8.53899251627374,2.06522364102136,-2.47405918988744));
#23976=CARTESIAN_POINT('Ctrl Pts',(8.53255038091548,1.98507862707395,-2.54096032878934));
#23977=CARTESIAN_POINT('Ctrl Pts',(8.52610824555721,1.90169344028278,-2.60395259253624));
#23978=CARTESIAN_POINT('Ctrl Pts',(8.51966611019894,1.81547396325931,-2.66273766098494));
#23979=CARTESIAN_POINT('Ctrl Pts',(8.51322243636635,1.72923389578805,-2.72153676815117));
#23980=CARTESIAN_POINT('Ctrl Pts',(8.50677876253376,1.64015850663556,-2.77612646935679));
#23981=CARTESIAN_POINT('Ctrl Pts',(8.50033508870116,1.548682017426,-2.82625221298478));
#23982=CARTESIAN_POINT('Ctrl Pts',(8.49388659938907,1.45713716610344,-2.87641541653039));
#23983=CARTESIAN_POINT('Ctrl Pts',(8.48743811007697,1.36318796635332,-2.92210782147296));
#23984=CARTESIAN_POINT('Ctrl Pts',(8.48098962076488,1.26729271492413,-2.96312111416328));
#23985=CARTESIAN_POINT('Ctrl Pts',(8.478150162386,1.22506723202623,-2.98118046604224));
#23986=CARTESIAN_POINT('Ctrl Pts',(8.47531070400712,1.18246469931592,-2.99833320990822));
#23987=CARTESIAN_POINT('Ctrl Pts',(8.47247124562825,1.13952539547046,-3.01456455156925));
#23988=CARTESIAN_POINT('Ctrl Pts',(8.46616526790204,1.04416414783162,-3.05061173568797));
#23989=CARTESIAN_POINT('Ctrl Pts',(8.45985929017584,0.947013057033462,-3.08215937900991));
#23990=CARTESIAN_POINT('Ctrl Pts',(8.45355331244963,0.84852405863481,-3.10903915774921));
#23991=CARTESIAN_POINT('Ctrl Pts',(8.44725149488684,0.750100035145118,-3.13590120342994));
#23992=CARTESIAN_POINT('Ctrl Pts',(8.44094967732406,0.650340253866413,-3.15810140435334));
#23993=CARTESIAN_POINT('Ctrl Pts',(8.43464785976127,0.549712617121871,-3.1755209967936));
#23994=CARTESIAN_POINT('Ctrl Pts',(8.42834880851157,0.449129152958476,-3.19293294254369));
#23995=CARTESIAN_POINT('Ctrl Pts',(8.42204975726187,0.347678994127284,-3.20556838689609));
#23996=CARTESIAN_POINT('Ctrl Pts',(8.41575070601216,0.245840395475785,-3.2133596223349));
#23997=CARTESIAN_POINT('Ctrl Pts',(8.40945303005588,0.144024031594194,-3.22114915668661));
#23998=CARTESIAN_POINT('Ctrl Pts',(8.4031553540996,0.0418198044672765,-3.22409655745443));
#23999=CARTESIAN_POINT('Ctrl Pts',(8.39685767814332,-0.0602894271516658,
-3.22218601999849));
#24000=CARTESIAN_POINT('Ctrl Pts',(8.39055787471853,-0.162433153110444,
-3.22027483712855));
#24001=CARTESIAN_POINT('Ctrl Pts',(8.38425807129375,-0.264481410019586,
-3.21350244058091));
#24002=CARTESIAN_POINT('Ctrl Pts',(8.37795826786896,-0.36595205823057,-3.20190515999097));
#24003=CARTESIAN_POINT('Ctrl Pts',(8.37165747903621,-0.467438578362893,
-3.19030606536782));
#24004=CARTESIAN_POINT('Ctrl Pts',(8.36535669020346,-0.568346904093618,
-3.17388063783813));
#24005=CARTESIAN_POINT('Ctrl Pts',(8.35905590137072,-0.668201994268032,
-3.15271686920285));
#24006=CARTESIAN_POINT('Ctrl Pts',(8.3527497907158,-0.768141424839589,-3.13153522505768));
#24007=CARTESIAN_POINT('Ctrl Pts',(8.34644368006089,-0.867025443845474,
-3.1056073379909));
#24008=CARTESIAN_POINT('Ctrl Pts',(8.34013756940597,-0.964391162463139,
-3.07507190944586));
#24009=CARTESIAN_POINT('Ctrl Pts',(8.33631838230833,-1.02335902976613,-3.05657865407787));
#24010=CARTESIAN_POINT('Ctrl Pts',(8.33249919521069,-1.08177028398587,-3.03639636678802));
#24011=CARTESIAN_POINT('Ctrl Pts',(8.32868000811305,-1.13952539547056,-3.01456455156921));
#24012=CARTESIAN_POINT('Ctrl Pts',(8.32223177201094,-1.23703792508388,-2.97770416859512));
#24013=CARTESIAN_POINT('Ctrl Pts',(8.31578353590882,-1.3328124689087,-2.93608867740333));
#24014=CARTESIAN_POINT('Ctrl Pts',(8.3093352998067,-1.42638227424303,-2.88990504519185));
#24015=CARTESIAN_POINT('Ctrl Pts',(8.30289097828219,-1.51989527547491,-2.84374945001395));
#24016=CARTESIAN_POINT('Ctrl Pts',(8.29644665675767,-1.611205864902,-2.7930314060247));
#24017=CARTESIAN_POINT('Ctrl Pts',(8.29000233523316,-1.69986889868451,-2.7379852610606));
#24018=CARTESIAN_POINT('Ctrl Pts',(8.28356102216947,-1.78849054110208,-2.68296481378559));
#24019=CARTESIAN_POINT('Ctrl Pts',(8.27711970910578,-1.8744667685495,-2.62362049134033));
#24020=CARTESIAN_POINT('Ctrl Pts',(8.2706783960421,-1.95737890937776,-2.56023150664606));
#24021=CARTESIAN_POINT('Ctrl Pts',(8.26423918807191,-2.04026395358663,-2.49686323818434));
#24022=CARTESIAN_POINT('Ctrl Pts',(8.25779998010172,-2.12008660575422,-2.4294531723003));
#24023=CARTESIAN_POINT('Ctrl Pts',(8.25136077213152,-2.19645923493826,-2.35832236807321));
#24024=CARTESIAN_POINT('Ctrl Pts',(8.24492180366115,-2.27282902351977,-2.28719420948427));
#24025=CARTESIAN_POINT('Ctrl Pts',(8.23848283519077,-2.34574876363202,-2.21234584315096));
#24026=CARTESIAN_POINT('Ctrl Pts',(8.23204386672039,-2.41486593091617,-2.1341368508604));
#24027=CARTESIAN_POINT('Ctrl Pts',(8.22560544314274,-2.48397724921349,-2.05593447694535));
#24028=CARTESIAN_POINT('Ctrl Pts',(8.21916701956509,-2.54928638752638,-1.97437233073066));
#24029=CARTESIAN_POINT('Ctrl Pts',(8.21272859598744,-2.61047996810889,-1.88984441121544));
#24030=CARTESIAN_POINT('Ctrl Pts',(8.2062884481267,-2.67168993702854,-1.80529385416162));
#24031=CARTESIAN_POINT('Ctrl Pts',(8.19984830026596,-2.72878192470561,-1.71777624531121));
#24032=CARTESIAN_POINT('Ctrl Pts',(8.19340815240522,-2.78148491010336,-1.62771596335704));
#24033=CARTESIAN_POINT('Ctrl Pts',(8.19056835846944,-2.8047243793774,-1.58800373188684));
#24034=CARTESIAN_POINT('Ctrl Pts',(8.18772856453366,-2.82711103391902,-1.54779747143598));
#24035=CARTESIAN_POINT('Ctrl Pts',(8.18488877059788,-2.84862442585766,-1.50713517738361));
#24036=CARTESIAN_POINT('Ctrl Pts',(8.86280938168963,2.84862442585767,-1.50713517738358));
#24037=CARTESIAN_POINT('Ctrl Pts',(8.85636948091779,2.79983774890731,-1.59934649439264));
#24038=CARTESIAN_POINT('Ctrl Pts',(8.84992958014595,2.74655707058332,-1.68921105493153));
#24039=CARTESIAN_POINT('Ctrl Pts',(8.84348967937412,2.68903360032897,-1.77629272891656));
#24040=CARTESIAN_POINT('Ctrl Pts',(8.83705126347726,2.63152339350284,-1.86335432411414));
#24041=CARTESIAN_POINT('Ctrl Pts',(8.8306128475804,2.56977255346136,-1.94763399480922));
#24042=CARTESIAN_POINT('Ctrl Pts',(8.82417443168354,2.50407608910275,-2.02872386057933));
#24043=CARTESIAN_POINT('Ctrl Pts',(8.81773659743177,2.43838555974841,-2.10980640070863));
#24044=CARTESIAN_POINT('Ctrl Pts',(8.81129876318,2.36875035603891,-2.18769941576884));
#24045=CARTESIAN_POINT('Ctrl Pts',(8.80486092892823,2.29550608022533,-2.26202771825382));
#24046=CARTESIAN_POINT('Ctrl Pts',(8.79842277363146,2.22225815183108,-2.33635972737822));
#24047=CARTESIAN_POINT('Ctrl Pts',(8.79198461833468,2.14540106018473,-2.40712640035833));
#24048=CARTESIAN_POINT('Ctrl Pts',(8.78554646303791,2.06530734054498,-2.47398931921523));
#24049=CARTESIAN_POINT('Ctrl Pts',(8.77910492109857,1.98517148945806,-2.54088740976282));
#24050=CARTESIAN_POINT('Ctrl Pts',(8.77266337915924,1.9017959000354,-2.60387739938502));
#24051=CARTESIAN_POINT('Ctrl Pts',(8.76622183721991,1.81558638164062,-2.66266100983605));
#24052=CARTESIAN_POINT('Ctrl Pts',(8.75977875478887,1.72935624628037,-2.72145867835966));
#24053=CARTESIAN_POINT('Ctrl Pts',(8.75333567235783,1.64029114888392,-2.77604775455572));
#24054=CARTESIAN_POINT('Ctrl Pts',(8.7468925899268,1.54882523780716,-2.82617372877741));
#24055=CARTESIAN_POINT('Ctrl Pts',(8.7404446829822,1.45729083800118,-2.87633723681071));
#24056=CARTESIAN_POINT('Ctrl Pts',(8.73399677603761,1.36335236963033,-2.92203078994484));
#24057=CARTESIAN_POINT('Ctrl Pts',(8.72754886909302,1.26746805584356,-2.963046116738));
#24058=CARTESIAN_POINT('Ctrl Pts',(8.72470529412016,1.22518235952123,-2.98113418124867));
#24059=CARTESIAN_POINT('Ctrl Pts',(8.72186171914731,1.18251849092217,-2.99831301466322));
#24060=CARTESIAN_POINT('Ctrl Pts',(8.71901814417445,1.1395169090585,-3.01456775947561));
#24061=CARTESIAN_POINT('Ctrl Pts',(8.71271123131444,1.04414146362609,-3.05062000359505));
#24062=CARTESIAN_POINT('Ctrl Pts',(8.70640431845443,0.946975935947859,-3.08217126797956));
#24063=CARTESIAN_POINT('Ctrl Pts',(8.70009740559442,0.848472409229412,-3.10905325352855));
#24064=CARTESIAN_POINT('Ctrl Pts',(8.69379464562084,0.75003374371466,-3.13591753820937));
#24065=CARTESIAN_POINT('Ctrl Pts',(8.68749188564727,0.650259225611314,-3.158118554212));
#24066=CARTESIAN_POINT('Ctrl Pts',(8.68118912567369,0.54961689606934,-3.17553756552416));
#24067=CARTESIAN_POINT('Ctrl Pts',(8.67488912702297,0.449018659268668,-3.1929489453361));
#24068=CARTESIAN_POINT('Ctrl Pts',(8.66858912837225,0.347553770145556,-3.20558242067925));
#24069=CARTESIAN_POINT('Ctrl Pts',(8.66228912972153,0.245700615361503,-3.21337031325538));
#24070=CARTESIAN_POINT('Ctrl Pts',(8.65599050365746,0.143869651420295,-3.22115650907601));
#24071=CARTESIAN_POINT('Ctrl Pts',(8.64969187759338,0.0416509977878185,
-3.22409919364228));
#24072=CARTESIAN_POINT('Ctrl Pts',(8.64339325152931,-0.060472359969582,
-3.22218259199874));
#24073=CARTESIAN_POINT('Ctrl Pts',(8.63709250068388,-0.162630168066401,
-3.22026534380794));
#24074=CARTESIAN_POINT('Ctrl Pts',(8.63079174983846,-0.264692206811846,
-3.21348553770968));
#24075=CARTESIAN_POINT('Ctrl Pts',(8.62449099899304,-0.366176213280718,
-3.20187953291928));
#24076=CARTESIAN_POINT('Ctrl Pts',(8.61818926453202,-0.467676062504604,
-3.19027171630556));
#24077=CARTESIAN_POINT('Ctrl Pts',(8.61188753007099,-0.56859729414741,-3.17383625467164));
#24078=CARTESIAN_POINT('Ctrl Pts',(8.60558579560997,-0.668464744479618,
-3.15266116921686));
#24079=CARTESIAN_POINT('Ctrl Pts',(8.59927875002009,-0.768416363527621,
-3.13146823730916));
#24080=CARTESIAN_POINT('Ctrl Pts',(8.59297170443021,-0.867312028348975,
-3.10552779483726));
#24081=CARTESIAN_POINT('Ctrl Pts',(8.58666465884034,-0.964688727521637,
-3.07497857252578));
#24082=CARTESIAN_POINT('Ctrl Pts',(8.58285207477998,-1.02355255620746,-3.05651168872394));
#24083=CARTESIAN_POINT('Ctrl Pts',(8.57903949071962,-1.08186161698839,-3.03636165679441));
#24084=CARTESIAN_POINT('Ctrl Pts',(8.57522690665926,-1.13951690905862,-3.01456775947556));
#24085=CARTESIAN_POINT('Ctrl Pts',(8.56877925371523,-1.23702067757096,-2.97771100196281));
#24086=CARTESIAN_POINT('Ctrl Pts',(8.56233160077121,-1.33278695607169,-2.93609993215246));
#24087=CARTESIAN_POINT('Ctrl Pts',(8.55588394782718,-1.42634905487053,-2.8899214411762));
#24088=CARTESIAN_POINT('Ctrl Pts',(8.54944021584167,-1.51985425651467,-2.84377103234837));
#24089=CARTESIAN_POINT('Ctrl Pts',(8.54299648385614,-1.61115760892541,-2.79305890321962));
#24090=CARTESIAN_POINT('Ctrl Pts',(8.53655275187063,-1.69981402601576,-2.73801932780982));
#24091=CARTESIAN_POINT('Ctrl Pts',(8.53011203214013,-1.78842899884087,-2.68300548178134));
#24092=CARTESIAN_POINT('Ctrl Pts',(8.52367131240963,-1.87439917965038,-2.62366842015394));
#24093=CARTESIAN_POINT('Ctrl Pts',(8.51723059267913,-1.9573059507449,-2.56028728420828));
#24094=CARTESIAN_POINT('Ctrl Pts',(8.51079197925771,-2.04018560883168,-2.49692687580039));
#24095=CARTESIAN_POINT('Ctrl Pts',(8.50435336583628,-2.12000355256081,-2.4295252593403));
#24096=CARTESIAN_POINT('Ctrl Pts',(8.49791475241485,-2.19637220248192,-2.35840342406992));
#24097=CARTESIAN_POINT('Ctrl Pts',(8.4914763741916,-2.27273806270812,-2.28728418683188));
#24098=CARTESIAN_POINT('Ctrl Pts',(8.48503799596835,-2.34565459889792,-2.21244525647574));
#24099=CARTESIAN_POINT('Ctrl Pts',(8.4785996177451,-2.41476933644808,-2.13424614659371));
#24100=CARTESIAN_POINT('Ctrl Pts',(8.472161780618,-2.48387826543627,-2.05605360874526));
#24101=CARTESIAN_POINT('Ctrl Pts',(8.46572394349091,-2.5491857839952,-1.97450174114556));
#24102=CARTESIAN_POINT('Ctrl Pts',(8.45928610636381,-2.61037856394492,-1.88998447490894));
#24103=CARTESIAN_POINT('Ctrl Pts',(8.45284653376126,-2.67158783989571,-1.80544442498911));
#24104=CARTESIAN_POINT('Ctrl Pts',(8.4464069611587,-2.72867993959428,-1.71793768779669));
#24105=CARTESIAN_POINT('Ctrl Pts',(8.43996738855614,-2.78138389155642,-1.62788857428586));
#24106=CARTESIAN_POINT('Ctrl Pts',(8.43712348208546,-2.80465952167455,-1.58812021194276));
#24107=CARTESIAN_POINT('Ctrl Pts',(8.43427957561477,-2.82707987863898,-1.54785635778742));
#24108=CARTESIAN_POINT('Ctrl Pts',(8.43143566914408,-2.84862442585766,-1.5071351773836));
#24109=CARTESIAN_POINT('Origin',(13.3346225254169,0.,0.));
#24110=CARTESIAN_POINT('Ctrl Pts',(9.48780938168963,-2.84862442585767,1.50713517738359));
#24111=CARTESIAN_POINT('Ctrl Pts',(9.48136979040113,-2.79984009345644,1.59934206297865));
#24112=CARTESIAN_POINT('Ctrl Pts',(9.47493019911264,-2.74656214827031,1.68920249868086));
#24113=CARTESIAN_POINT('Ctrl Pts',(9.46849060782414,-2.68904175600906,1.77628038241144));
#24114=CARTESIAN_POINT('Ctrl Pts',(9.46205250594599,-2.63153466761499,1.86333812593513));
#24115=CARTESIAN_POINT('Ctrl Pts',(9.45561440406783,-2.56978729677783,1.94761428328878));
#24116=CARTESIAN_POINT('Ctrl Pts',(9.44917630218968,-2.50409461012863,2.02870099966081));
#24117=CARTESIAN_POINT('Ctrl Pts',(9.44273878510985,-2.43840789060658,2.10978035060493));
#24118=CARTESIAN_POINT('Ctrl Pts',(9.43630126803001,-2.36877680910113,2.18767054344086));
#24119=CARTESIAN_POINT('Ctrl Pts',(9.42986375095017,-2.29553692688901,2.26199641462779));
#24120=CARTESIAN_POINT('Ctrl Pts',(9.42342591460022,-2.22229341232837,2.33632597202311));
#24121=CARTESIAN_POINT('Ctrl Pts',(9.41698807825027,-2.14544100795,2.40709058612817));
#24122=CARTESIAN_POINT('Ctrl Pts',(9.41055024190032,-2.06535220900859,2.47395186194949));
#24123=CARTESIAN_POINT('Ctrl Pts',(9.40410901815544,-1.98522126976148,2.54084831815358));
#24124=CARTESIAN_POINT('Ctrl Pts',(9.39766779441055,-1.90185082497803,2.60383708854403));
#24125=CARTESIAN_POINT('Ctrl Pts',(9.39122657066567,-1.815646644735,2.66261991729246));
#24126=CARTESIAN_POINT('Ctrl Pts',(9.38478380536225,-1.72942183350709,2.72141681435694));
#24127=CARTESIAN_POINT('Ctrl Pts',(9.37834104005883,-1.64036225290246,2.77600555530531));
#24128=CARTESIAN_POINT('Ctrl Pts',(9.37189827475541,-1.54890201198458,2.82613165294367));
#24129=CARTESIAN_POINT('Ctrl Pts',(9.36545068011865,-1.45737321479151,2.87629532383254));
#24130=CARTESIAN_POINT('Ctrl Pts',(9.35900308548189,-1.36344049892566,2.9219894921406));
#24131=CARTESIAN_POINT('Ctrl Pts',(9.35255549084513,-1.26756204807032,2.96300590900386));
#24132=CARTESIAN_POINT('Ctrl Pts',(9.34970970862157,-1.22524406649145,2.98110937185465));
#24133=CARTESIAN_POINT('Ctrl Pts',(9.34686392639801,-1.18254731002768,2.99830219557313));
#24134=CARTESIAN_POINT('Ctrl Pts',(9.34401814417445,-1.13951233461232,3.01456948862792));
#24135=CARTESIAN_POINT('Ctrl Pts',(9.33771072418351,-1.04412918758265,3.05062447855748));
#24136=CARTESIAN_POINT('Ctrl Pts',(9.33140330419258,-0.946955828523528,
3.08217770810489));
#24137=CARTESIAN_POINT('Ctrl Pts',(9.32509588420165,-0.84844442075252,3.10906089155454));
#24138=CARTESIAN_POINT('Ctrl Pts',(9.31879261313949,-0.7499978123472,3.13592639163863));
#24139=CARTESIAN_POINT('Ctrl Pts',(9.31248934207733,-0.650215299854983,
3.15812785052148));
#24140=CARTESIAN_POINT('Ctrl Pts',(9.30618607101517,-0.549564999754426,
3.17554654721749));
#24141=CARTESIAN_POINT('Ctrl Pts',(9.29988555856276,-0.448958748988868,
3.19295762066742));
#24142=CARTESIAN_POINT('Ctrl Pts',(9.29358504611035,-0.347485868817361,
3.2055900284188));
#24143=CARTESIAN_POINT('Ctrl Pts',(9.28728453365794,-0.245624817427304,
3.21337610801534));
#24144=CARTESIAN_POINT('Ctrl Pts',(9.28098539232177,-0.143785933018701,
3.22116049320681));
#24145=CARTESIAN_POINT('Ctrl Pts',(9.27468625098561,-0.0415594530327246,
3.2241006196819));
#24146=CARTESIAN_POINT('Ctrl Pts',(9.26838710964944,0.0605715681494443,
3.22218072857993));
#24147=CARTESIAN_POINT('Ctrl Pts',(9.26208584499361,0.162737015739041,3.22026019031953));
#24148=CARTESIAN_POINT('Ctrl Pts',(9.25578458033778,0.264806531084418,3.21347636482852));
#24149=CARTESIAN_POINT('Ctrl Pts',(9.24948331568195,0.366297784362431,3.20186562736027));
#24150=CARTESIAN_POINT('Ctrl Pts',(9.243181068389,0.467804864474859,3.19025307928063));
#24151=CARTESIAN_POINT('Ctrl Pts',(9.23687882109605,0.568733097433191,3.17381217428114));
#24152=CARTESIAN_POINT('Ctrl Pts',(9.23057657380311,0.668607252988596,3.15263094950092));
#24153=CARTESIAN_POINT('Ctrl Pts',(9.22426902119375,0.768565483949464,3.13143189408121));
#24154=CARTESIAN_POINT('Ctrl Pts',(9.21796146858439,0.867467466274419,3.10548464033273));
#24155=CARTESIAN_POINT('Ctrl Pts',(9.21165391597503,0.964850122006924,3.07492793485688));
#24156=CARTESIAN_POINT('Ctrl Pts',(9.20784491286977,1.02365753290874,3.0564753601021));
#24157=CARTESIAN_POINT('Ctrl Pts',(9.20403590976451,1.08191117538282,3.03634282365224));
#24158=CARTESIAN_POINT('Ctrl Pts',(9.20022690665925,1.13951233461235,3.01456948862791));
#24159=CARTESIAN_POINT('Ctrl Pts',(9.19377956644096,1.23701140727205,2.97771467525302));
#24160=CARTESIAN_POINT('Ctrl Pts',(9.18733222622268,1.3327732555634,2.93610597621625));
#24161=CARTESIAN_POINT('Ctrl Pts',(9.18088488600439,1.42633122358117,2.88993024191544));
#24162=CARTESIAN_POINT('Ctrl Pts',(9.17444147014678,1.51983224482733,2.843782613815));
#24163=CARTESIAN_POINT('Ctrl Pts',(9.16799805428917,1.61113171828328,2.79307365592956));
#24164=CARTESIAN_POINT('Ctrl Pts',(9.16155463843156,1.69978458883192,2.73803760274937));
#24165=CARTESIAN_POINT('Ctrl Pts',(9.15511423684688,1.78839598697616,2.68302729580209));
#24166=CARTESIAN_POINT('Ctrl Pts',(9.14867383526221,1.8743629269146,2.62369412683514));
#24167=CARTESIAN_POINT('Ctrl Pts',(9.14223343367753,1.95726681988284,2.5603171987638));
#24168=CARTESIAN_POINT('Ctrl Pts',(9.13579513903988,2.0401435912332,2.4969610041558));
#24169=CARTESIAN_POINT('Ctrl Pts',(9.12935684440223,2.11995901137559,2.42956391746386));
#24170=CARTESIAN_POINT('Ctrl Pts',(9.12291854976458,2.19632552848083,2.35844689052846));
#24171=CARTESIAN_POINT('Ctrl Pts',(9.11648048800268,2.27268928337791,2.28733243592503));
#24172=CARTESIAN_POINT('Ctrl Pts',(9.11004242624078,2.34560410244999,2.2124985641213));
#24173=CARTESIAN_POINT('Ctrl Pts',(9.10360436447888,2.41471753778688,2.13430475218617));
#24174=CARTESIAN_POINT('Ctrl Pts',(9.09716684177078,2.48382518631067,2.05611748735687));
#24175=CARTESIAN_POINT('Ctrl Pts',(9.09072931906268,2.54913183681801,1.97457113008197));
#24176=CARTESIAN_POINT('Ctrl Pts',(9.08429179635459,2.61032418772396,1.89005957511482));
#24177=CARTESIAN_POINT('Ctrl Pts',(9.07785253216167,2.67153309244341,1.80552515800072));
#24178=CARTESIAN_POINT('Ctrl Pts',(9.07141326796875,2.72862525233257,1.71802424911479));
#24179=CARTESIAN_POINT('Ctrl Pts',(9.06497400377584,2.78132972249762,1.627981123125));
#24180=CARTESIAN_POINT('Ctrl Pts',(9.06212789223192,2.80462474448441,1.58818266593297));
#24181=CARTESIAN_POINT('Ctrl Pts',(9.059281780688,2.82706317369287,1.54788793167558));
#24182=CARTESIAN_POINT('Ctrl Pts',(9.05643566914408,2.84862442585766,1.50713517738361));
#24183=CARTESIAN_POINT('Ctrl Pts',(9.24126248314343,-2.84862442585767,1.50713517738359));
#24184=CARTESIAN_POINT('Ctrl Pts',(9.23482235122126,-2.79983599778463,1.59934980417595));
#24185=CARTESIAN_POINT('Ctrl Pts',(9.2283822192991,-2.74655327805828,1.68921744557311));
#24186=CARTESIAN_POINT('Ctrl Pts',(9.22194208737694,-2.68902750877139,1.77630195056211));
#24187=CARTESIAN_POINT('Ctrl Pts',(9.2155034369455,-2.63151497273731,1.86336642259395));
#24188=CARTESIAN_POINT('Ctrl Pts',(9.20906478651407,-2.56976154144227,1.94764871747033));
#24189=CARTESIAN_POINT('Ctrl Pts',(9.20262613608263,-2.50406225534015,2.02874093562506));
#24190=CARTESIAN_POINT('Ctrl Pts',(9.19618806494546,-2.43836888029341,2.10982585780106));
#24191=CARTESIAN_POINT('Ctrl Pts',(9.18974999380828,-2.36873059751867,2.18772098086146));
#24192=CARTESIAN_POINT('Ctrl Pts',(9.18331192267111,-2.29548303985887,2.2620510993831));
#24193=CARTESIAN_POINT('Ctrl Pts',(9.17687352916871,-2.22223181456864,2.33638493974084));
#24194=CARTESIAN_POINT('Ctrl Pts',(9.1704351356663,-2.14537122172991,2.40715315055674));
#24195=CARTESIAN_POINT('Ctrl Pts',(9.1639967421639,-2.06527382647043,2.47401729666471));
#24196=CARTESIAN_POINT('Ctrl Pts',(9.15755496259094,-1.98513430650513,2.54091660786734));
#24197=CARTESIAN_POINT('Ctrl Pts',(9.15111318301797,-1.90175487425804,2.60390750811563));
#24198=CARTESIAN_POINT('Ctrl Pts',(9.14467140344501,-1.81554136842773,2.66269170239958));
#24199=CARTESIAN_POINT('Ctrl Pts',(9.138228084184,-1.7293072561948,2.72148994704331));
#24200=CARTESIAN_POINT('Ctrl Pts',(9.131784764923,-1.64023803795771,2.77607927355949));
#24201=CARTESIAN_POINT('Ctrl Pts',(9.125341445662,-1.54876789141397,2.82620515550891));
#24202=CARTESIAN_POINT('Ctrl Pts',(9.11889330549825,-1.45722930674659,2.87636854173088));
#24203=CARTESIAN_POINT('Ctrl Pts',(9.11244516533451,-1.3632865414915,2.92206163521662));
#24204=CARTESIAN_POINT('Ctrl Pts',(9.10599702517076,-1.26739784827073,2.96307614763757));
#24205=CARTESIAN_POINT('Ctrl Pts',(9.1031550986566,-1.22513626388314,2.98115271349298));
#24206=CARTESIAN_POINT('Ctrl Pts',(9.10031317214242,-1.18249695692235,2.99832109910658));
#24207=CARTESIAN_POINT('Ctrl Pts',(9.09747124562826,-1.1395203141202,3.01456647234845));
#24208=CARTESIAN_POINT('Ctrl Pts',(9.09116470883316,-1.04415057890354,3.05061668110268));
#24209=CARTESIAN_POINT('Ctrl Pts',(9.08485817203806,-0.946990857625094,
3.08216648887611));
#24210=CARTESIAN_POINT('Ctrl Pts',(9.07855163524296,-0.848493174102343,
3.10904758664156));
#24211=CARTESIAN_POINT('Ctrl Pts',(9.07224925426397,-0.750060397559917,
3.13591097058044));
#24212=CARTESIAN_POINT('Ctrl Pts',(9.06594687328498,-0.650291806577286,
3.15811165856173));
#24213=CARTESIAN_POINT('Ctrl Pts',(9.05964449230599,-0.549655386463332,
3.17553090342888));
#24214=CARTESIAN_POINT('Ctrl Pts',(9.05334487465865,-0.449063091229409,
3.19294251068244));
#24215=CARTESIAN_POINT('Ctrl Pts',(9.0470452570113,-0.347604126657197,3.20557677780699));
#24216=CARTESIAN_POINT('Ctrl Pts',(9.04074563936396,-0.245756826387187,
3.21336601475526));
#24217=CARTESIAN_POINT('Ctrl Pts',(9.0344473953925,-0.14393173463654,3.22115355320569));
#24218=CARTESIAN_POINT('Ctrl Pts',(9.02814915142105,-0.0417188834012557,
3.22409813452873));
#24219=CARTESIAN_POINT('Ctrl Pts',(9.02185090744959,0.0603987927624763,
3.22218397183228));
#24220=CARTESIAN_POINT('Ctrl Pts',(9.01555053761488,0.162550936980487,3.22026916304333));
#24221=CARTESIAN_POINT('Ctrl Pts',(9.00925016778017,0.264607432624234,3.21349233702463));
#24222=CARTESIAN_POINT('Ctrl Pts',(9.00294979794547,0.366086066356794,3.20188984109688));
#24223=CARTESIAN_POINT('Ctrl Pts',(8.99664844377251,0.46758055460317,3.19028553245325));
#24224=CARTESIAN_POINT('Ctrl Pts',(8.99034708959955,0.568496595473008,3.17385410654971));
#24225=CARTESIAN_POINT('Ctrl Pts',(8.9840457354266,0.668359074543371,3.15268357276393));
#24226=CARTESIAN_POINT('Ctrl Pts',(8.97773906582064,0.768305791430331,3.13149518082403));
#24227=CARTESIAN_POINT('Ctrl Pts',(8.97143239621467,0.867196772356202,3.10555978819097));
#24228=CARTESIAN_POINT('Ctrl Pts',(8.96512572660871,0.964569055215959,3.07501611381466));
#24229=CARTESIAN_POINT('Ctrl Pts',(8.96131048711016,1.02347472220693,3.0565386224932));
#24230=CARTESIAN_POINT('Ctrl Pts',(8.95749524761161,1.08182487959139,3.03637561813463));
#24231=CARTESIAN_POINT('Ctrl Pts',(8.95368000811306,1.1395203141202,3.01456647234845));
#24232=CARTESIAN_POINT('Ctrl Pts',(8.947232121635,1.23702759047468,2.97770826298414));
#24233=CARTESIAN_POINT('Ctrl Pts',(8.94078423515694,1.33279717833878,2.93609542263685));
#24234=CARTESIAN_POINT('Ctrl Pts',(8.93433634867889,1.42636236278996,2.88991487288402));
#24235=CARTESIAN_POINT('Ctrl Pts',(8.92789238060956,1.51987068727056,2.84376238725264));
#24236=CARTESIAN_POINT('Ctrl Pts',(8.92144841254023,1.61117693729572,2.79304788962198));
#24237=CARTESIAN_POINT('Ctrl Pts',(8.9150044444709,1.69983600365082,2.73800568355736));
#24238=CARTESIAN_POINT('Ctrl Pts',(8.90856348714187,1.78845364686092,2.68298919422287));
#24239=CARTESIAN_POINT('Ctrl Pts',(8.90212252981284,1.87442624865628,2.62364922518965));
#24240=CARTESIAN_POINT('Ctrl Pts',(8.89568157248381,1.95733516973162,2.5602649464131));
#24241=CARTESIAN_POINT('Ctrl Pts',(8.88924272098093,2.04021698431255,2.49690139068512));
#24242=CARTESIAN_POINT('Ctrl Pts',(8.88280386947804,2.12003681322233,2.42949639090833));
#24243=CARTESIAN_POINT('Ctrl Pts',(8.87636501797516,2.19640705638776,2.35837096427811));
#24244=CARTESIAN_POINT('Ctrl Pts',(8.86992640339741,2.27277448941996,2.28724815479191));
#24245=CARTESIAN_POINT('Ctrl Pts',(8.86348778881967,2.34569230838318,2.21240544611426));
#24246=CARTESIAN_POINT('Ctrl Pts',(8.85704917424192,2.41480801874585,2.13420237913388));
#24247=CARTESIAN_POINT('Ctrl Pts',(8.85061110228246,2.4839179043387,2.056005902766));
#24248=CARTESIAN_POINT('Ctrl Pts',(8.844173030323,2.54922607139876,1.97444991942677));
#24249=CARTESIAN_POINT('Ctrl Pts',(8.83773495836353,2.61041917189268,1.88992838740391));
#24250=CARTESIAN_POINT('Ctrl Pts',(8.83129515541268,2.67162872525172,1.80538413024774));
#24251=CARTESIAN_POINT('Ctrl Pts',(8.82485535246184,2.72872078006262,1.71787303983451));
#24252=CARTESIAN_POINT('Ctrl Pts',(8.81841554951099,2.78142434499242,1.62781945423424));
#24253=CARTESIAN_POINT('Ctrl Pts',(8.81557328987329,2.80468549389814,1.58807356860144));
#24254=CARTESIAN_POINT('Ctrl Pts',(8.81273103023558,2.82709235453134,1.54783277720073));
#24255=CARTESIAN_POINT('Ctrl Pts',(8.80988877059788,2.84862442585767,1.50713517738359));
#24256=CARTESIAN_POINT('Origin',(13.3346225254169,0.,0.));
#24257=CARTESIAN_POINT('Ctrl Pts',(9.86626248314343,2.84862442585767,-1.50713517738359));
#24258=CARTESIAN_POINT('Ctrl Pts',(9.85982267522957,2.79983845237032,-1.59934516478271));
#24259=CARTESIAN_POINT('Ctrl Pts',(9.8533828673157,2.74655859410983,-1.68920848768861));
#24260=CARTESIAN_POINT('Ctrl Pts',(9.84694305940184,2.68903604740003,-1.77628902442232));
#24261=CARTESIAN_POINT('Ctrl Pts',(9.84050473772321,2.63152677624702,-1.86334946394761));
#24262=CARTESIAN_POINT('Ctrl Pts',(9.83406641604458,2.5697769771344,-1.94762808047689));
#24263=CARTESIAN_POINT('Ctrl Pts',(9.82762809436595,2.50408164628066,-2.02871700127454));
#24264=CARTESIAN_POINT('Ctrl Pts',(9.8211903552778,2.43839226006218,-2.10979858450265));
#24265=CARTESIAN_POINT('Ctrl Pts',(9.81475261618964,2.36875829322387,-2.18769075275974));
#24266=CARTESIAN_POINT('Ctrl Pts',(9.80831487710149,2.29551533572473,-2.26201832573315));
#24267=CARTESIAN_POINT('Ctrl Pts',(9.80187681749998,2.22226873170531,-2.33634959922618));
#24268=CARTESIAN_POINT('Ctrl Pts',(9.79543875789847,2.14541304648722,-2.40711565444394));
#24269=CARTESIAN_POINT('Ctrl Pts',(9.78900069829696,2.06532080332786,-2.47397808030733));
#24270=CARTESIAN_POINT('Ctrl Pts',(9.78255925182548,1.98518642604269,-2.54087568048664));
#24271=CARTESIAN_POINT('Ctrl Pts',(9.776117805354,1.90181238028295,-2.60386530428902));
#24272=CARTESIAN_POINT('Ctrl Pts',(9.76967635888252,1.81560446362589,-2.6626486801983));
#24273=CARTESIAN_POINT('Ctrl Pts',(9.76323337159812,1.72937592578187,-2.72144611726382));
#24274=CARTESIAN_POINT('Ctrl Pts',(9.75679038431372,1.64031248371951,-2.77603509288299));
#24275=CARTESIAN_POINT('Ctrl Pts',(9.75034739702932,1.54884827400627,-2.82616110414955));
#24276=CARTESIAN_POINT('Ctrl Pts',(9.74389958378342,1.45731555527158,-2.87632466107459));
#24277=CARTESIAN_POINT('Ctrl Pts',(9.73745177053753,1.36337881295747,-2.92201839881558));
#24278=CARTESIAN_POINT('Ctrl Pts',(9.73100395729163,1.26749625837215,-2.96303405270891));
#24279=CARTESIAN_POINT('Ctrl Pts',(9.72815972007051,1.22520087539378,-2.98112673700408));
#24280=CARTESIAN_POINT('Ctrl Pts',(9.72531548284938,1.18252713939225,-2.99830976786173));
#24281=CARTESIAN_POINT('Ctrl Pts',(9.72247124562825,1.13951553844249,-3.01456827757278));
#24282=CARTESIAN_POINT('Ctrl Pts',(9.71616418105511,1.04413778915726,-3.05062134299537));
#24283=CARTESIAN_POINT('Ctrl Pts',(9.70985711648197,0.94696991880963,-3.08217319516756));
#24284=CARTESIAN_POINT('Ctrl Pts',(9.70355005190883,0.84846403456833,-3.10905553899316));
#24285=CARTESIAN_POINT('Ctrl Pts',(9.69724713903899,0.750022993044205,-3.1359201871833));
#24286=CARTESIAN_POINT('Ctrl Pts',(9.69094422616915,0.650246083531913,-3.15812133561167));
#24287=CARTESIAN_POINT('Ctrl Pts',(9.68464131329931,0.54960136971356,-3.17554025276156));
#24288=CARTESIAN_POINT('Ctrl Pts',(9.67834116094118,0.449000735659186,-3.19295154087931));
#24289=CARTESIAN_POINT('Ctrl Pts',(9.67204100858305,0.347533456141694,-3.20558469682421));
#24290=CARTESIAN_POINT('Ctrl Pts',(9.66574085622492,0.245677939217087,-3.21337204703751));
#24291=CARTESIAN_POINT('Ctrl Pts',(9.65944207601374,0.143844605999829,-3.22115770119838));
#24292=CARTESIAN_POINT('Ctrl Pts',(9.65314329580256,0.041623611246871,-3.2240996205201));
#24293=CARTESIAN_POINT('Ctrl Pts',(9.64684451559137,-0.0605020388920546,
-3.22218203486239));
#24294=CARTESIAN_POINT('Ctrl Pts',(9.64054361103579,-0.162662132216087,
-3.22026380247432));
#24295=CARTESIAN_POINT('Ctrl Pts',(9.63424270648021,-0.264726407460492,
-3.21348279402017));
#24296=CARTESIAN_POINT('Ctrl Pts',(9.62794180192462,-0.366212581690208,
-3.20187537351343));
#24297=CARTESIAN_POINT('Ctrl Pts',(9.62163991404569,-0.46771459391978,-3.19026614154494));
#24298=CARTESIAN_POINT('Ctrl Pts',(9.61533802616675,-0.5686379198952,-3.17382905160953));
#24299=CARTESIAN_POINT('Ctrl Pts',(9.60903613828781,-0.668507375990506,
-3.15265212967531));
#24300=CARTESIAN_POINT('Ctrl Pts',(9.60272894101787,-0.768460972902217,
-3.13145736601481));
#24301=CARTESIAN_POINT('Ctrl Pts',(9.59642174374794,-0.867358527520858,
-3.10551488606228));
#24302=CARTESIAN_POINT('Ctrl Pts',(9.59011454647801,-0.964737008523535,
-3.07496342529225));
#24303=CARTESIAN_POINT('Ctrl Pts',(9.58630303368969,-1.02358395904113,-3.05650082162806));
#24304=CARTESIAN_POINT('Ctrl Pts',(9.58249152090137,-1.08187644074406,-3.03635602341281));
#24305=CARTESIAN_POINT('Ctrl Pts',(9.57868000811306,-1.13951553844249,-3.01456827757278));
#24306=CARTESIAN_POINT('Ctrl Pts',(9.57223244899357,-1.23701789791085,-2.97771210334857));
#24307=CARTESIAN_POINT('Ctrl Pts',(9.56578488987408,-1.33278284708364,-2.93610174484108));
#24308=CARTESIAN_POINT('Ctrl Pts',(9.55933733075459,-1.42634370640727,-2.88992408095652));
#24309=CARTESIAN_POINT('Ctrl Pts',(9.55289369361583,-1.5198476536684,-2.84377450644728));
#24310=CARTESIAN_POINT('Ctrl Pts',(9.54645005647707,-1.61114984215441,-2.7930633288124));
#24311=CARTESIAN_POINT('Ctrl Pts',(9.54000641933832,-1.69980519506997,-2.73802481020774));
#24312=CARTESIAN_POINT('Ctrl Pts',(9.53356579506128,-1.78841909526034,-2.68301202605128));
#24313=CARTESIAN_POINT('Ctrl Pts',(9.52712517078425,-1.87438830360516,-2.62367613238684));
#24314=CARTESIAN_POINT('Ctrl Pts',(9.52068454650722,-1.95729421108584,-2.56029625898056));
#24315=CARTESIAN_POINT('Ctrl Pts',(9.51424602873174,-2.04017300296176,-2.49693711490045));
#24316=CARTESIAN_POINT('Ctrl Pts',(9.50780751095625,-2.11999018945337,-2.42953685757224));
#24317=CARTESIAN_POINT('Ctrl Pts',(9.50136899318077,-2.1963581993966,-2.35841646501277));
#24318=CARTESIAN_POINT('Ctrl Pts',(9.4949307099079,-2.27272342787692,-2.28729866278837));
#24319=CARTESIAN_POINT('Ctrl Pts',(9.48849242663504,-2.34563944881386,-2.21246125023154));
#24320=CARTESIAN_POINT('Ctrl Pts',(9.48205414336218,-2.41475379561177,-2.13426372997307));
#24321=CARTESIAN_POINT('Ctrl Pts',(9.47561640057324,-2.48386234036715,-2.05607277427549));
#24322=CARTESIAN_POINT('Ctrl Pts',(9.4691786577843,-2.54916959844693,-1.97452256002475));
#24323=CARTESIAN_POINT('Ctrl Pts',(9.46274091499536,-2.61036224964905,-1.89000700742276));
#24324=CARTESIAN_POINT('Ctrl Pts',(9.45630143492861,-2.6715714141911,-1.80546864760419));
#24325=CARTESIAN_POINT('Ctrl Pts',(9.44986195486186,-2.72866353193724,-1.71796365916594));
#24326=CARTESIAN_POINT('Ctrl Pts',(9.44342247479511,-2.78136763937955,-1.62791634217248));
#24327=CARTESIAN_POINT('Ctrl Pts',(9.44057790672937,-2.80464908747939,-1.58813895026034));
#24328=CARTESIAN_POINT('Ctrl Pts',(9.43773333866362,-2.82707486660146,-1.54786583100038));
#24329=CARTESIAN_POINT('Ctrl Pts',(9.43488877059788,-2.84862442585766,-1.5071351773836));
#24330=CARTESIAN_POINT('Ctrl Pts',(10.1128093816896,2.84862442585767,-1.50713517738358));
#24331=CARTESIAN_POINT('Ctrl Pts',(10.1063700807377,2.79984229295584,-1.59933790572201));
#24332=CARTESIAN_POINT('Ctrl Pts',(10.0999307797858,2.74656691174921,-1.68919447186086));
#24333=CARTESIAN_POINT('Ctrl Pts',(10.0934914788339,2.68904940689746,-1.77626879997494));
#24334=CARTESIAN_POINT('Ctrl Pts',(10.0870536715522,2.63154524389488,-1.86332293019352));
#24335=CARTESIAN_POINT('Ctrl Pts',(10.0806158642705,2.56980112743642,-1.94759579171096));
#24336=CARTESIAN_POINT('Ctrl Pts',(10.0741780569888,2.50411198448077,-2.02867955371956));
#24337=CARTESIAN_POINT('Ctrl Pts',(10.0677408374702,2.43842883885472,-2.10975591289073));
#24338=CARTESIAN_POINT('Ctrl Pts',(10.0613036179515,2.3688016241954,-2.18764345826353));
#24339=CARTESIAN_POINT('Ctrl Pts',(10.0548663984329,2.29556586332255,-2.26196704875385));
#24340=CARTESIAN_POINT('Ctrl Pts',(10.0484288613174,2.22232648917418,-2.33629430619057));
#24341=CARTESIAN_POINT('Ctrl Pts',(10.0419913242019,2.14547848162114,-2.40705698892092));
#24342=CARTESIAN_POINT('Ctrl Pts',(10.0355537870864,2.06539429837441,-2.47391672348575));
#24343=CARTESIAN_POINT('Ctrl Pts',(10.0291128618851,1.98526796669807,-2.54081164643239));
#24344=CARTESIAN_POINT('Ctrl Pts',(10.0226719366838,1.90190234777773,-2.6037992730192));
#24345=CARTESIAN_POINT('Ctrl Pts',(10.0162310114826,1.8157031748215,-2.66258136841733));
#24346=CARTESIAN_POINT('Ctrl Pts',(10.0097885437321,1.72948335786382,-2.72137754164965));
#24347=CARTESIAN_POINT('Ctrl Pts',(10.0033460759816,1.64042895216162,-2.77596596799634));
#24348=CARTESIAN_POINT('Ctrl Pts',(9.99690360823108,1.54897402990824,-2.82609218129378));
#24349=CARTESIAN_POINT('Ctrl Pts',(9.99045630664174,1.45745048824178,-2.87625600471926));
#24350=CARTESIAN_POINT('Ctrl Pts',(9.98400900505239,1.36352316841648,-2.92195074989421));
#24351=CARTESIAN_POINT('Ctrl Pts',(9.97756170346304,1.26765021708599,-2.96296818910056));
#24352=CARTESIAN_POINT('Ctrl Pts',(9.97471385036684,1.22530194509901,-2.98108610085371));
#24353=CARTESIAN_POINT('Ctrl Pts',(9.97186599727065,1.18257433236595,-2.99829205143002));
#24354=CARTESIAN_POINT('Ctrl Pts',(9.96901814417446,1.13950802589812,-3.01457111732561));
#24355=CARTESIAN_POINT('Ctrl Pts',(9.96271024438015,1.04411759088132,-3.0506287063043));
#24356=CARTESIAN_POINT('Ctrl Pts',(9.95640234458584,0.946936820960122,-3.08218379611568));
#24357=CARTESIAN_POINT('Ctrl Pts',(9.95009444479154,0.848417955275339,-3.10906811370649));
#24358=CARTESIAN_POINT('Ctrl Pts',(9.94379069017424,0.749963830336331,-3.1359347645209));
#24359=CARTESIAN_POINT('Ctrl Pts',(9.93748693555695,0.650173752527543,-3.15813664302233));
#24360=CARTESIAN_POINT('Ctrl Pts',(9.93118318093965,0.549515909624953,-3.17555504244046));
#24361=CARTESIAN_POINT('Ctrl Pts',(9.92488218236069,0.448902074919152,-3.19296582643265));
#24362=CARTESIAN_POINT('Ctrl Pts',(9.91858118378173,0.347421632456268,-3.20559722429035));
#24363=CARTESIAN_POINT('Ctrl Pts',(9.91228018520277,0.245553108123589,-3.21338158854358));
#24364=CARTESIAN_POINT('Ctrl Pts',(9.90598055634726,0.143706728170867,-3.22116426061641));
#24365=CARTESIAN_POINT('Ctrl Pts',(9.89968092749175,0.04147284167858,-3.22410196655805));
#24366=CARTESIAN_POINT('Ctrl Pts',(9.89338129863624,-0.0606654318365552,
-3.22217896273315));
#24367=CARTESIAN_POINT('Ctrl Pts',(9.88707954784687,-0.162838109070619,
-3.22025531117376));
#24368=CARTESIAN_POINT('Ctrl Pts',(9.8807777970575,-0.264914699921362,-3.21346768213288));
#24369=CARTESIAN_POINT('Ctrl Pts',(9.87447604626814,-0.366412811243082,
-3.2018524660354));
#24370=CARTESIAN_POINT('Ctrl Pts',(9.86817331377162,-0.467926734269368,
-3.19023544048193));
#24371=CARTESIAN_POINT('Ctrl Pts',(9.8618705812751,-0.568861592886876,-3.1737893842466));
#24372=CARTESIAN_POINT('Ctrl Pts',(9.85556784877859,-0.668742093881155,
-3.15260234954735));
#24373=CARTESIAN_POINT('Ctrl Pts',(9.84925981647365,-0.768706581863708,
-3.13139749920623));
#24374=CARTESIAN_POINT('Ctrl Pts',(9.84295178416871,-0.867614542586038,
-3.10544379962069));
#24375=CARTESIAN_POINT('Ctrl Pts',(9.83664375186377,-0.965002835110426,
-3.07488001241168));
#24376=CARTESIAN_POINT('Ctrl Pts',(9.8328381367956,-1.02375687053349,-3.05644098047268));
#24377=CARTESIAN_POINT('Ctrl Pts',(9.82903252172743,-1.08195808238332,-3.03632499871464));
#24378=CARTESIAN_POINT('Ctrl Pts',(9.82522690665926,-1.13950802589812,-3.01457111732561));
#24379=CARTESIAN_POINT('Ctrl Pts',(9.81877985987646,-1.23700269405064,-2.97771812812142));
#24380=CARTESIAN_POINT('Ctrl Pts',(9.81233281309366,-1.33276038693557,-2.93611165344557));
#24381=CARTESIAN_POINT('Ctrl Pts',(9.80588576631086,-1.42631448034508,-2.88993850551494));
#24382=CARTESIAN_POINT('Ctrl Pts',(9.7994426470676,-1.51981158062054,-2.84379348625634));
#24383=CARTESIAN_POINT('Ctrl Pts',(9.79299952782435,-1.61110741578519,-2.79308750353223));
#24384=CARTESIAN_POINT('Ctrl Pts',(9.7865564085811,-1.69975695978144,-2.73805475478022));
#24385=CARTESIAN_POINT('Ctrl Pts',(9.78011630549264,-1.78836500512812,-2.68304776797409));
#24386=CARTESIAN_POINT('Ctrl Pts',(9.77367620240419,-1.8743289053089,-2.62371825083255));
#24387=CARTESIAN_POINT('Ctrl Pts',(9.76723609931573,-1.95723009871279,-2.56034527030882));
#24388=CARTESIAN_POINT('Ctrl Pts',(9.76079810376318,-2.04010416254446,-2.49699302871274));
#24389=CARTESIAN_POINT('Ctrl Pts',(9.75436010821063,-2.11991721573218,-2.42960019145055));
#24390=CARTESIAN_POINT('Ctrl Pts',(9.74792211265809,-2.19628173237039,-2.35848767530299));
#24391=CARTESIAN_POINT('Ctrl Pts',(9.74148434779094,-2.27264351272534,-2.28737770724971));
#24392=CARTESIAN_POINT('Ctrl Pts',(9.7350465829238,-2.34555672132969,-2.21254858085581));
#24393=CARTESIAN_POINT('Ctrl Pts',(9.72860881805666,-2.41466893532812,-2.1343597389525));
#24394=CARTESIAN_POINT('Ctrl Pts',(9.7221715903222,-2.48377538297294,-2.0561774207081));
#24395=CARTESIAN_POINT('Ctrl Pts',(9.71573436258774,-2.54908121938732,-1.97463623267522));
#24396=CARTESIAN_POINT('Ctrl Pts',(9.70929713485327,-2.61027316795172,-1.89013003551906));
#24397=CARTESIAN_POINT('Ctrl Pts',(9.70285815998966,-2.67148172463404,-1.80560090252054));
#24398=CARTESIAN_POINT('Ctrl Pts',(9.69641918512605,-2.72857394111304,-1.71810546120604));
#24399=CARTESIAN_POINT('Ctrl Pts',(9.68998021026243,-2.78127889745783,-1.62806795222305));
#24400=CARTESIAN_POINT('Ctrl Pts',(9.68713202988965,-2.80459211507232,-1.58824126065622));
#24401=CARTESIAN_POINT('Ctrl Pts',(9.68428384951686,-2.82704750089152,-1.54791755471499));
#24402=CARTESIAN_POINT('Ctrl Pts',(9.68143566914408,-2.84862442585766,-1.5071351773836));
#24403=CARTESIAN_POINT('Origin',(13.3346225254169,0.,0.));
#24404=CARTESIAN_POINT('Ctrl Pts',(10.7378093816896,-2.84862442585766,1.5071351773836));
#24405=CARTESIAN_POINT('Ctrl Pts',(10.7313703534291,-2.7998443587803,1.59933400112333));
#24406=CARTESIAN_POINT('Ctrl Pts',(10.7249313251685,-2.74657138566347,1.68918693295203));
#24407=CARTESIAN_POINT('Ctrl Pts',(10.718492296908,-2.68905659259001,1.77625792168486));
#24408=CARTESIAN_POINT('Ctrl Pts',(10.7120547663237,-2.63155517708473,1.86330865826993));
#24409=CARTESIAN_POINT('Ctrl Pts',(10.7056172357394,-2.56981411703793,1.94757842439466));
#24410=CARTESIAN_POINT('Ctrl Pts',(10.6991797051551,-2.50412830212752,2.02865941177516));
#24411=CARTESIAN_POINT('Ctrl Pts',(10.6927427651249,-2.43844851297953,2.10973296109971));
#24412=CARTESIAN_POINT('Ctrl Pts',(10.6863058250947,-2.36882492985391,2.18761802006119));
#24413=CARTESIAN_POINT('Ctrl Pts',(10.6798688850646,-2.29559303943354,2.26193946864285));
#24414=CARTESIAN_POINT('Ctrl Pts',(10.673431629017,-2.22235755374044,2.3362645659884));
#24415=CARTESIAN_POINT('Ctrl Pts',(10.6669943729694,-2.14551367537334,2.40702543484564));
#24416=CARTESIAN_POINT('Ctrl Pts',(10.6605571169217,-2.06543382676692,2.47388372195359));
#24417=CARTESIAN_POINT('Ctrl Pts',(10.6541164721538,-1.98531182227798,2.54077720480862));
#24418=CARTESIAN_POINT('Ctrl Pts',(10.6476758273859,-1.90195073547167,2.60376375711341));
#24419=CARTESIAN_POINT('Ctrl Pts',(10.641235182618,-1.81575626491601,2.66254516373305));
#24420=CARTESIAN_POINT('Ctrl Pts',(10.6347929943798,-1.72954113826053,2.72134065704056));
#24421=CARTESIAN_POINT('Ctrl Pts',(10.6283508061416,-1.64049159241196,2.77592878782993));
#24422=CARTESIAN_POINT('Ctrl Pts',(10.6219086179034,-1.5490416649257,2.82605510965802));
#24423=CARTESIAN_POINT('Ctrl Pts',(10.6154615916098,-1.45752305894043,2.87621907613646));
#24424=CARTESIAN_POINT('Ctrl Pts',(10.6090145653162,-1.36360080667019,2.92191436290365));
#24425=CARTESIAN_POINT('Ctrl Pts',(10.6025675390226,-1.26773301998384,2.96293276206914));
#24426=CARTESIAN_POINT('Ctrl Pts',(10.5997177407399,-1.22535629598354,2.98106424752897));
#24427=CARTESIAN_POINT('Ctrl Pts',(10.5968679424572,-1.18259969928859,2.99828252911706));
#24428=CARTESIAN_POINT('Ctrl Pts',(10.5940181441744,-1.13950396258885,3.01457265325358));
#24429=CARTESIAN_POINT('Ctrl Pts',(10.5877097898818,-1.04410662262551,3.05063270534465));
#24430=CARTESIAN_POINT('Ctrl Pts',(10.5814014355892,-0.946918831284225,
3.08218955825583));
#24431=CARTESIAN_POINT('Ctrl Pts',(10.5750930812966,-0.848392899556238,
3.10907495092713));
#24432=CARTESIAN_POINT('Ctrl Pts',(10.5687888686204,-0.749931652942532,
3.13594269256315));
#24433=CARTESIAN_POINT('Ctrl Pts',(10.5624846559442,-0.650134407193353,
3.1581449691306));
#24434=CARTESIAN_POINT('Ctrl Pts',(10.556180443268,-0.549469417647791,3.17556308732322));
#24435=CARTESIAN_POINT('Ctrl Pts',(10.5498789841903,-0.4488483972663,3.19297359750734));
#24436=CARTESIAN_POINT('Ctrl Pts',(10.5435775251126,-0.347360789604111,
3.20560403890608));
#24437=CARTESIAN_POINT('Ctrl Pts',(10.5372760660349,-0.24548518470401,3.21338677824361));
#24438=CARTESIAN_POINT('Ctrl Pts',(10.5309759753598,-0.14363170275086,3.22116782750892));
#24439=CARTESIAN_POINT('Ctrl Pts',(10.5246758846847,-0.0413907985953394,
3.22410324032225));
#24440=CARTESIAN_POINT('Ctrl Pts',(10.5183757940096,0.0607543465188861,
3.22217728746869));
#24441=CARTESIAN_POINT('Ctrl Pts',(10.512073582716,0.162933873818505,3.22025068633695));
#24442=CARTESIAN_POINT('Ctrl Pts',(10.5057713714224,0.26501716870336,3.21345945366387));
#24443=CARTESIAN_POINT('Ctrl Pts',(10.4994691601288,0.366521778017622,3.20183999424375));
#24444=CARTESIAN_POINT('Ctrl Pts',(10.4931659680128,0.468042184643721,3.19021872647004));
#24445=CARTESIAN_POINT('Ctrl Pts',(10.4868627758968,0.56898332101638,3.17376778957782));
#24446=CARTESIAN_POINT('Ctrl Pts',(10.4805595837808,0.668869834247954,3.1525752500667));
#24447=CARTESIAN_POINT('Ctrl Pts',(10.4742510970817,0.768840250591654,3.13136490915316));
#24448=CARTESIAN_POINT('Ctrl Pts',(10.4679426103827,0.867753875672361,3.10540510221069));
#24449=CARTESIAN_POINT('Ctrl Pts',(10.4616341236837,0.965147508863338,3.07483460508608));
#24450=CARTESIAN_POINT('Ctrl Pts',(10.4578317180089,1.02385098581493,3.05640840601582));
#24451=CARTESIAN_POINT('Ctrl Pts',(10.4540293123341,1.08200253352952,3.0363081075963));
#24452=CARTESIAN_POINT('Ctrl Pts',(10.4502269066593,1.13950396258886,3.01457265325358));
#24453=CARTESIAN_POINT('Ctrl Pts',(10.443780135533,1.23699449471016,2.97772137765163));
#24454=CARTESIAN_POINT('Ctrl Pts',(10.4373333644067,1.33274828542264,2.93611699239956));
#24455=CARTESIAN_POINT('Ctrl Pts',(10.4308865932805,1.42629874029213,2.88994627388488));
#24456=CARTESIAN_POINT('Ctrl Pts',(10.4244437526675,1.51979215865555,2.84380370506193));
#24457=CARTESIAN_POINT('Ctrl Pts',(10.4180009120544,1.61108457729918,2.79310051679673));
#24458=CARTESIAN_POINT('Ctrl Pts',(10.4115580714414,1.69973099746441,2.738070871756));
#24459=CARTESIAN_POINT('Ctrl Pts',(10.4051182487401,1.78833589447452,2.6830670033285));
#24460=CARTESIAN_POINT('Ctrl Pts',(10.3986784260388,1.87429694022193,2.62374091607416));
#24461=CARTESIAN_POINT('Ctrl Pts',(10.3922386033375,1.95719559860731,2.56037164319795));
#24462=CARTESIAN_POINT('Ctrl Pts',(10.385800888716,2.04006712006665,2.49702311429161));
#24463=CARTESIAN_POINT('Ctrl Pts',(10.3793631740946,2.11987795063644,2.42963426812137));
#24464=CARTESIAN_POINT('Ctrl Pts',(10.3729254594731,2.19624058877033,2.35852598856527));
#24465=CARTESIAN_POINT('Ctrl Pts',(10.3664879734686,2.27260051510442,2.28742023421551));
#24466=CARTESIAN_POINT('Ctrl Pts',(10.3600504874641,2.3455122115232,2.21259556466524));
#24467=CARTESIAN_POINT('Ctrl Pts',(10.3536130014596,2.4146232787165,2.13441139061344));
#24468=CARTESIAN_POINT('Ctrl Pts',(10.3471760507783,2.4837285988282,2.05623371813723));
#24469=CARTESIAN_POINT('Ctrl Pts',(10.340739100097,2.5490336708833,1.97469738502973));
#24470=CARTESIAN_POINT('Ctrl Pts',(10.3343021494157,2.61022524172581,1.89019621996168));
#24471=CARTESIAN_POINT('Ctrl Pts',(10.3278634462972,2.67143347175855,1.80567204974826));
#24472=CARTESIAN_POINT('Ctrl Pts',(10.3214247431787,2.72852574152598,1.71818174357321));
#24473=CARTESIAN_POINT('Ctrl Pts',(10.3149860400602,2.78123115456013,1.62814951015074));
#24474=CARTESIAN_POINT('Ctrl Pts',(10.3121359164215,2.80456146515386,1.58829629872004));
#24475=CARTESIAN_POINT('Ctrl Pts',(10.3092857927828,2.82703277931589,1.54794537985008));
#24476=CARTESIAN_POINT('Ctrl Pts',(10.3064356691441,2.84862442585766,1.50713517738361));
#24477=CARTESIAN_POINT('Ctrl Pts',(10.4912624831434,-2.84862442585767,1.50713517738359));
#24478=CARTESIAN_POINT('Ctrl Pts',(10.4848229789318,-2.7998407531234,1.59934081614728));
#24479=CARTESIAN_POINT('Ctrl Pts',(10.4783834747201,-2.74656357692504,1.68920009129343));
#24480=CARTESIAN_POINT('Ctrl Pts',(10.4719439705085,-2.68904405066309,1.7762769086191));
#24481=CARTESIAN_POINT('Ctrl Pts',(10.4655059569842,-2.63153783965492,1.86333356844357));
#24482=CARTESIAN_POINT('Ctrl Pts',(10.4590679434599,-2.56979144488121,1.94760873730506));
#24483=CARTESIAN_POINT('Ctrl Pts',(10.4526299299357,-2.50409982107675,2.02869456759351));
#24484=CARTESIAN_POINT('Ctrl Pts',(10.4461925020982,-2.43841417345056,2.10977302124322));
#24485=CARTESIAN_POINT('Ctrl Pts',(10.4397550742607,-2.36878425171169,2.18766242004355));
#24486=CARTESIAN_POINT('Ctrl Pts',(10.4333176464233,-2.29554560560487,2.26198760719155));
#24487=CARTESIAN_POINT('Ctrl Pts',(10.4268798998167,-2.2223033328601,2.33631647478094));
#24488=CARTESIAN_POINT('Ctrl Pts',(10.4204421532101,-2.14545224721117,2.40708050962087));
#24489=CARTESIAN_POINT('Ctrl Pts',(10.4140044066035,-2.06536483265434,2.47394132317942));
#24490=CARTESIAN_POINT('Ctrl Pts',(10.4075632723932,-1.98523527533568,2.54083731953612));
#24491=CARTESIAN_POINT('Ctrl Pts',(10.4011221381828,-1.90186627796118,2.60382574688035));
#24492=CARTESIAN_POINT('Ctrl Pts',(10.3946810039725,-1.81566359955142,2.66260835568508));
#24493=CARTESIAN_POINT('Ctrl Pts',(10.3882383279055,-1.72944028623876,2.72140503567004));
#24494=CARTESIAN_POINT('Ctrl Pts',(10.3817956518385,-1.64038225773539,2.77599368227329));
#24495=CARTESIAN_POINT('Ctrl Pts',(10.3753529757714,-1.54892361204772,2.82611981461173));
#24496=CARTESIAN_POINT('Ctrl Pts',(10.3689054690181,-1.4573963911248,2.87628353127358));
#24497=CARTESIAN_POINT('Ctrl Pts',(10.3624579622648,-1.36346529368264,2.92197787261881));
#24498=CARTESIAN_POINT('Ctrl Pts',(10.3560104555115,-1.26758849229933,2.96299459612911));
#24499=CARTESIAN_POINT('Ctrl Pts',(10.3531640522171,-1.22526142638758,2.98110239211788));
#24500=CARTESIAN_POINT('Ctrl Pts',(10.3503176489226,-1.18255541593426,2.99829915258518));
#24501=CARTESIAN_POINT('Ctrl Pts',(10.3474712456282,-1.13951104417291,3.01456997641587));
#24502=CARTESIAN_POINT('Ctrl Pts',(10.3411636821617,-1.04412571796369,3.05062574341341));
#24503=CARTESIAN_POINT('Ctrl Pts',(10.3348561186953,-0.946950142990533,
3.08217952913117));
#24504=CARTESIAN_POINT('Ctrl Pts',(10.3285485552288,-0.848436505241506,
3.10906305164009));
#24505=CARTESIAN_POINT('Ctrl Pts',(10.3222451395699,-0.749987649340766,
3.13592889574106));
#24506=CARTESIAN_POINT('Ctrl Pts',(10.3159417239111,-0.650202874771774,
3.15813048003906));
#24507=CARTESIAN_POINT('Ctrl Pts',(10.3096383082522,-0.54955031933025,3.17554908779947));
#24508=CARTESIAN_POINT('Ctrl Pts',(10.3033376504346,-0.448941800929435,
3.19296007465114));
#24509=CARTESIAN_POINT('Ctrl Pts',(10.2970369926171,-0.347466659599731,
3.20559218039583));
#24510=CARTESIAN_POINT('Ctrl Pts',(10.2907363347995,-0.245603373769911,
3.21337774705882));
#24511=CARTESIAN_POINT('Ctrl Pts',(10.2844370476819,-0.143762248165569,
3.2211616199819));
#24512=CARTESIAN_POINT('Ctrl Pts',(10.2781377605642,-0.0415335536093207,
3.22410102267434));
#24513=CARTESIAN_POINT('Ctrl Pts',(10.2718384734466,0.0605996360431658,
3.22218020082854));
#24514=CARTESIAN_POINT('Ctrl Pts',(10.2655370634233,0.162767245323142,3.22025873165181));
#24515=CARTESIAN_POINT('Ctrl Pts',(10.2592356534001,0.264838876269155,3.21347376886252));
#24516=CARTESIAN_POINT('Ctrl Pts',(10.2529342433769,0.366332180125763,3.20186169225098));
#24517=CARTESIAN_POINT('Ctrl Pts',(10.2466318509943,0.467841306299447,3.19024780537265));
#24518=CARTESIAN_POINT('Ctrl Pts',(10.2403294586116,0.568771520358791,3.17380536012273));
#24519=CARTESIAN_POINT('Ctrl Pts',(10.2340270662289,0.668647573229539,3.15262239814955));
#24520=CARTESIAN_POINT('Ctrl Pts',(10.227719370176,0.768607675080177,3.13142161001792));
#24521=CARTESIAN_POINT('Ctrl Pts',(10.2214116741231,0.867511444986111,3.1054724289363));
#24522=CARTESIAN_POINT('Ctrl Pts',(10.2151039780701,0.96489578616085,3.07491360599758));
#24523=CARTESIAN_POINT('Ctrl Pts',(10.2112959880844,1.02368723597793,3.05646508045848));
#24524=CARTESIAN_POINT('Ctrl Pts',(10.2074879980988,1.08192519998495,3.0363374941559));
#24525=CARTESIAN_POINT('Ctrl Pts',(10.2036800081131,1.13951104417291,3.01456997641587));
#24526=CARTESIAN_POINT('Ctrl Pts',(10.197232755895,1.23700879575944,2.97771571010789));
#24527=CARTESIAN_POINT('Ctrl Pts',(10.1907855036769,1.33276939769849,2.93610767816709));
#24528=CARTESIAN_POINT('Ctrl Pts',(10.1843382514589,1.42632620359115,2.88993271953678));
#24529=CARTESIAN_POINT('Ctrl Pts',(10.1778949245562,1.51982604878806,2.84378587385608));
#24530=CARTESIAN_POINT('Ctrl Pts',(10.1714515976536,1.61112443098708,2.79307780825953));
#24531=CARTESIAN_POINT('Ctrl Pts',(10.165008270751,1.69977630378595,2.73804274612135));
#24532=CARTESIAN_POINT('Ctrl Pts',(10.1585679586868,1.78838669629298,2.68303343493877));
#24533=CARTESIAN_POINT('Ctrl Pts',(10.1521276466227,1.87435272449252,2.62370136121625));
#24534=CARTESIAN_POINT('Ctrl Pts',(10.1456873345586,1.95725580776304,2.56032561708034));
#24535=CARTESIAN_POINT('Ctrl Pts',(10.1392491296191,2.04013176701713,2.49697060805654));
#24536=CARTESIAN_POINT('Ctrl Pts',(10.1328109246796,2.11994647721657,2.42957479584968));
#24537=CARTESIAN_POINT('Ctrl Pts',(10.1263727197401,2.1963123943059,2.35845912178233));
#24538=CARTESIAN_POINT('Ctrl Pts',(10.1199347470207,2.27267555694775,2.28734601279109));
#24539=CARTESIAN_POINT('Ctrl Pts',(10.1134967743013,2.34558989296914,2.21251356423462));
#24540=CARTESIAN_POINT('Ctrl Pts',(10.1070588015818,2.41470296197287,2.1343212429106));
#24541=CARTESIAN_POINT('Ctrl Pts',(10.1006213673406,2.48381025029353,2.05613546166699));
#24542=CARTESIAN_POINT('Ctrl Pts',(10.0941839330994,2.5491166566131,1.97459065475291));
#24543=CARTESIAN_POINT('Ctrl Pts',(10.0877464988581,2.61030888683252,1.89008070669567));
#24544=CARTESIAN_POINT('Ctrl Pts',(10.0813073214399,2.67151768714493,1.80554787439817));
#24545=CARTESIAN_POINT('Ctrl Pts',(10.0748681440218,2.72860986399238,1.71804860534506));
#24546=CARTESIAN_POINT('Ctrl Pts',(10.0684289666036,2.781314479966,1.62800716399882));
#24547=CARTESIAN_POINT('Ctrl Pts',(10.0655822346017,2.80461495876892,1.58820023899394));
#24548=CARTESIAN_POINT('Ctrl Pts',(10.0627355025998,2.82705847329692,1.54789681585724));
#24549=CARTESIAN_POINT('Ctrl Pts',(10.0598887705979,2.84862442585767,1.50713517738359));
#24550=CARTESIAN_POINT('Origin',(13.3346225254169,0.,0.));
#24551=CARTESIAN_POINT('',(11.0238490761438,1.87105265221536,-2.62398161867378));
#24552=CARTESIAN_POINT('Ctrl Pts',(11.0238490761438,1.87105265221536,-2.62398161867378));
#24553=CARTESIAN_POINT('Ctrl Pts',(11.0171010612196,1.78198399703447,-2.68749278899581));
#24554=CARTESIAN_POINT('Ctrl Pts',(11.0103530462954,1.6897328614071,-2.74642706210009));
#24555=CARTESIAN_POINT('Ctrl Pts',(11.0036050313713,1.59477453685249,-2.80050205125919));
#24556=CARTESIAN_POINT('Ctrl Pts',(10.9968363324979,1.49952514697184,-2.85474279054524));
#24557=CARTESIAN_POINT('Ctrl Pts',(10.9900676336245,1.40155221258743,-2.90409427015761));
#24558=CARTESIAN_POINT('Ctrl Pts',(10.9832989347511,1.30135856293772,-2.94831875026576));
#24559=CARTESIAN_POINT('Ctrl Pts',(10.9765302358777,1.20116491328801,-2.99254323037392));
#24560=CARTESIAN_POINT('Ctrl Pts',(10.9697615370043,1.09875083290288,-3.03164061448522));
#24561=CARTESIAN_POINT('Ctrl Pts',(10.962992838131,0.99463811646416,-3.06542208835531));
#24562=CARTESIAN_POINT('Ctrl Pts',(10.9566676158604,0.897346733735724,-3.09699024271578));
#24563=CARTESIAN_POINT('Ctrl Pts',(10.9503423935899,0.798480009417802,-3.12394554759593));
#24564=CARTESIAN_POINT('Ctrl Pts',(10.9440171713194,0.698500851313238,-3.14614273726013));
#24565=CARTESIAN_POINT('Ctrl Pts',(10.9376957912064,0.598582423987644,-3.16832644358796));
#24566=CARTESIAN_POINT('Ctrl Pts',(10.9313744110934,0.497553302409718,-3.18575769915854));
#24567=CARTESIAN_POINT('Ctrl Pts',(10.9250530309804,0.395889691787329,-3.19834158814166));
#24568=CARTESIAN_POINT('Ctrl Pts',(10.9187341516616,0.294266300193852,-3.21092049882634));
#24569=CARTESIAN_POINT('Ctrl Pts',(10.9124152723428,0.192009320978601,-3.21865581095524));
#24570=CARTESIAN_POINT('Ctrl Pts',(10.906096393024,0.0896026158676177,-3.22150414150435));
#24571=CARTESIAN_POINT('Ctrl Pts',(10.8997786757475,-0.0127852566451852,
-3.22435194824533));
#24572=CARTESIAN_POINT('Ctrl Pts',(10.8934609584709,-0.115322395341751,
-3.22231455286083));
#24573=CARTESIAN_POINT('Ctrl Pts',(10.8871432411943,-0.217523020598734,
-3.21540064346725));
#24574=CARTESIAN_POINT('Ctrl Pts',(10.8808234830682,-0.319756660328726,
-3.20848450063259));
#24575=CARTESIAN_POINT('Ctrl Pts',(10.874503724942,-0.421653164719666,-3.19668872134875));
#24576=CARTESIAN_POINT('Ctrl Pts',(10.8681839668158,-0.522730172436479,
-3.18007401318342));
#24577=CARTESIAN_POINT('Ctrl Pts',(10.8618631165486,-0.623824647649185,
-3.16345643376822));
#24578=CARTESIAN_POINT('Ctrl Pts',(10.8555422662814,-0.724098945437443,
-3.14201834014415));
#24579=CARTESIAN_POINT('Ctrl Pts',(10.8492214160142,-0.823080366901728,
-3.11587167131782));
#24580=CARTESIAN_POINT('Ctrl Pts',(10.8428959208975,-0.922134524435214,
-3.08970578872506));
#24581=CARTESIAN_POINT('Ctrl Pts',(10.8365704257808,-1.01989351873125,-3.05882453322215));
#24582=CARTESIAN_POINT('Ctrl Pts',(10.8302449306641,-1.11589942283804,-3.0233898261074));
#24583=CARTESIAN_POINT('Ctrl Pts',(10.8281435552309,-1.14779328167668,-3.0116181589665));
#24584=CARTESIAN_POINT('Ctrl Pts',(10.8260421797977,-1.17949382102355,-2.99934436333468));
#24585=CARTESIAN_POINT('Ctrl Pts',(10.8239408043644,-1.21098474892435,-2.98657554740754));
#24586=CARTESIAN_POINT('Ctrl Pts',(10.8174850956538,-1.30772912612473,-2.94734802294879));
#24587=CARTESIAN_POINT('Ctrl Pts',(10.8110293869433,-1.4026126142313,-2.90339672979654));
#24588=CARTESIAN_POINT('Ctrl Pts',(10.8045736782327,-1.49517238600333,-2.85492155735199));
#24589=CARTESIAN_POINT('Ctrl Pts',(10.7981215694289,-1.58768054352744,-2.80647341619242));
#24590=CARTESIAN_POINT('Ctrl Pts',(10.7916694606252,-1.67786723238977,-2.75350659665608));
#24591=CARTESIAN_POINT('Ctrl Pts',(10.7852173518214,-1.76529252213514,-2.69626776745073));
#24592=CARTESIAN_POINT('Ctrl Pts',(10.7787679761062,-1.8526807788622,-2.63905318439448));
#24593=CARTESIAN_POINT('Ctrl Pts',(10.772318600391,-1.93730965183885,-2.57757040437331));
#24594=CARTESIAN_POINT('Ctrl Pts',(10.7658692246759,-2.01876688252812,-2.5121102357396));
#24595=CARTESIAN_POINT('Ctrl Pts',(10.7591208535027,-2.10400050074261,-2.44361530933014));
#24596=CARTESIAN_POINT('Ctrl Pts',(10.7523724823295,-2.18576095349918,-2.37076556946754));
#24597=CARTESIAN_POINT('Ctrl Pts',(10.7456241111564,-2.26361331126617,-2.29394253187794));
#24598=CARTESIAN_POINT('Ctrl Pts',(10.7391767794815,-2.33799273695526,-2.22054650920761));
#24599=CARTESIAN_POINT('Ctrl Pts',(10.7327294478066,-2.40880496089534,-2.14352435156969));
#24600=CARTESIAN_POINT('Ctrl Pts',(10.7262821161317,-2.47570777028153,-2.06324710072925));
#24601=CARTESIAN_POINT('Ctrl Pts',(10.7198351359104,-2.54260693269592,-1.98297422592133));
#24602=CARTESIAN_POINT('Ctrl Pts',(10.7133881556892,-2.6055968665912,-1.89944690412764));
#24603=CARTESIAN_POINT('Ctrl Pts',(10.7069411754679,-2.66437553899544,-1.8130693725566));
#24604=CARTESIAN_POINT('Ctrl Pts',(10.7004927241863,-2.72316762341218,-1.72667213151467));
#24605=CARTESIAN_POINT('Ctrl Pts',(10.6940442729046,-2.77774631691511,-1.63742369544976));
#24606=CARTESIAN_POINT('Ctrl Pts',(10.6875958216229,-2.82785288593765,-1.54575729595371));
#24607=CARTESIAN_POINT('Ctrl Pts',(10.6866934712812,-2.83486444231021,-1.53293015292487));
#24608=CARTESIAN_POINT('Ctrl Pts',(10.6857911209396,-2.84178850148947,-1.52005570463342));
#24609=CARTESIAN_POINT('Ctrl Pts',(10.6848887705979,-2.84862442585766,-1.5071351773836));
#24610=CARTESIAN_POINT('',(11.0238490761438,-1.87158653173898,-2.62360084935061));
#24611=CARTESIAN_POINT('Origin',(11.0238490761438,0.,0.));
#24612=CARTESIAN_POINT('Ctrl Pts',(11.0238490761438,-1.87158653173898,-2.62360084935061));
#24613=CARTESIAN_POINT('Ctrl Pts',(11.0084294243278,-2.07493559933386,-2.47853862456651));
#24614=CARTESIAN_POINT('Ctrl Pts',(10.9932849210064,-2.26073288354223,-2.31032499875892));
#24615=CARTESIAN_POINT('Ctrl Pts',(10.9624483041142,-2.58973185199326,-1.93437311771314));
#24616=CARTESIAN_POINT('Ctrl Pts',(10.9468547252081,-2.73181447276606,-1.72791675726662));
#24617=CARTESIAN_POINT('Ctrl Pts',(10.9314356691441,-2.84862442585767,-1.5071351773836));
#24618=CARTESIAN_POINT('Ctrl Pts',(11.1008112312664,1.68942544263115,3.40346056344526));
#24619=CARTESIAN_POINT('Ctrl Pts',(11.0751571795589,2.12830620414844,3.18560690803575));
#24620=CARTESIAN_POINT('Ctrl Pts',(11.0495031278513,2.52436782889846,2.88189967479167));
#24621=CARTESIAN_POINT('Ctrl Pts',(11.0238490761438,2.84862442585767,2.51456577037539));
#24622=CARTESIAN_POINT('Ctrl Pts',(11.0751571795589,1.70918178686444,3.44326104044715));
#24623=CARTESIAN_POINT('Ctrl Pts',(11.0495031278513,2.15319487277031,3.22285977820035));
#24624=CARTESIAN_POINT('Ctrl Pts',(11.0238490761438,2.55388808977572,2.91560095605822));
#24625=CARTESIAN_POINT('Ctrl Pts',(10.9981950244362,2.88193658236276,2.54397140480186));
#24626=CARTESIAN_POINT('Ctrl Pts',(11.0495031278513,1.72893813109773,3.48306151744904));
#24627=CARTESIAN_POINT('Ctrl Pts',(11.0238490761438,2.17808354139218,3.26011264836494));
#24628=CARTESIAN_POINT('Ctrl Pts',(10.9981950244362,2.58340835065299,2.94930223732478));
#24629=CARTESIAN_POINT('Ctrl Pts',(10.9725409727286,2.91524873886784,2.57337703922832));
#24630=CARTESIAN_POINT('Ctrl Pts',(11.0238490761438,1.74869447533101,3.52286199445093));
#24631=CARTESIAN_POINT('Ctrl Pts',(10.9981950244362,2.20297221001404,3.29736551852953));
#24632=CARTESIAN_POINT('Ctrl Pts',(10.9725409727286,2.61292861153025,2.98300351859134));
#24633=CARTESIAN_POINT('Ctrl Pts',(10.9468869210211,2.94856089537293,2.60278267365479));
#24634=CARTESIAN_POINT('',(11.0238490761438,1.74869447533103,3.52286199445092));
#24635=CARTESIAN_POINT('Ctrl Pts',(11.0238490761438,1.74869447533103,3.52286199445092));
#24636=CARTESIAN_POINT('Ctrl Pts',(11.0006887763626,2.15881326042978,3.31928534147352));
#24637=CARTESIAN_POINT('Ctrl Pts',(10.9775284765815,2.53280859423868,3.0432801490367));
#24638=CARTESIAN_POINT('Ctrl Pts',(10.9543681768003,2.84860418144656,2.71177492056083));
#24639=CARTESIAN_POINT('Origin',(11.0238490761448,0.32028972767158,0.987026521741422));
#24640=CARTESIAN_POINT('Ctrl Pts',(3.61717341366717,2.84754707936762,-1.50592664679481));
#24641=CARTESIAN_POINT('Ctrl Pts',(3.56923138188706,2.48464894021009,-2.1921402390435));
#24642=CARTESIAN_POINT('Ctrl Pts',(3.47335893760189,1.24438661619661,-3.28829531364372));
#24643=CARTESIAN_POINT('Ctrl Pts',(3.32954446153663,-1.24438661619659,-3.28829531364374));
#24644=CARTESIAN_POINT('Ctrl Pts',(3.23367201725147,-2.48464894021008,-2.19214023904351));
#24645=CARTESIAN_POINT('Ctrl Pts',(3.18572998547137,-2.84754707936761,-1.50592664679483));
#24646=CARTESIAN_POINT('Ctrl Pts',(3.48019371320366,3.05727954735629,-1.61684376368135));
#24647=CARTESIAN_POINT('Ctrl Pts',(3.43225168142354,2.66765260609905,-2.35359954759826));
#24648=CARTESIAN_POINT('Ctrl Pts',(3.33637923713838,1.33604033389561,-3.53049053373441));
#24649=CARTESIAN_POINT('Ctrl Pts',(3.19256476107312,-1.33604033389558,-3.53049053373443));
#24650=CARTESIAN_POINT('Ctrl Pts',(3.09669231678796,-2.66765260609903,-2.35359954759828));
#24651=CARTESIAN_POINT('Ctrl Pts',(3.04875028500786,-3.05727954735627,-1.61684376368138));
#24652=CARTESIAN_POINT('Ctrl Pts',(3.34321401274013,3.26701201534495,-1.7277608805679));
#24653=CARTESIAN_POINT('Ctrl Pts',(3.29527198096003,2.85065627198801,-2.51505885615301));
#24654=CARTESIAN_POINT('Ctrl Pts',(3.19939953667487,1.42769405159462,-3.77268575382511));
#24655=CARTESIAN_POINT('Ctrl Pts',(3.05558506060961,-1.42769405159458,-3.77268575382512));
#24656=CARTESIAN_POINT('Ctrl Pts',(2.95971261632444,-2.85065627198798,-2.51505885615305));
#24657=CARTESIAN_POINT('Ctrl Pts',(2.91177058454434,-3.26701201534493,-1.72776088056793));
#24658=CARTESIAN_POINT('Ctrl Pts',(3.20623431227662,3.47674448333362,-1.83867799745444));
#24659=CARTESIAN_POINT('Ctrl Pts',(3.15829228049652,3.03365993787697,-2.67651816470778));
#24660=CARTESIAN_POINT('Ctrl Pts',(3.06241983621135,1.51934776929363,-4.01488097391579));
#24661=CARTESIAN_POINT('Ctrl Pts',(2.91860536014609,-1.51934776929357,-4.01488097391582));
#24662=CARTESIAN_POINT('Ctrl Pts',(2.82273291586093,-3.03365993787694,-2.67651816470782));
#24663=CARTESIAN_POINT('Ctrl Pts',(2.77479088408083,-3.47674448333358,-1.83867799745449));
#24664=CARTESIAN_POINT('',(3.02384907614375,0.656739510617909,-3.87731438084271));
#24665=CARTESIAN_POINT('Ctrl Pts',(3.02384907614375,0.656739510617945,-3.8773143808427));
#24666=CARTESIAN_POINT('Ctrl Pts',(3.02384907614375,0.535250361035218,-3.88669383362465));
#24667=CARTESIAN_POINT('Ctrl Pts',(3.02384907614375,0.413571785996884,-3.89044850980247));
#24668=CARTESIAN_POINT('Ctrl Pts',(3.02384907614375,0.292110716985867,-3.88864428500737));
#24669=CARTESIAN_POINT('Ctrl Pts',(3.02384907614375,0.170355994992987,-3.88683569818915));
#24670=CARTESIAN_POINT('Ctrl Pts',(3.02384907614375,0.0488189541319484,
-3.87944114112614));
#24671=CARTESIAN_POINT('Ctrl Pts',(3.02384907614375,-0.0720841979465033,
-3.86647526033853));
#24672=CARTESIAN_POINT('Ctrl Pts',(3.02384907614375,-0.190730889393864,
-3.8537513666211));
#24673=CARTESIAN_POINT('Ctrl Pts',(3.02384907614375,-0.308767877441656,
-3.83566186693603));
#24674=CARTESIAN_POINT('Ctrl Pts',(3.02384907614376,-0.425783805981553,
-3.81217453448968));
#24675=CARTESIAN_POINT('Ctrl Pts',(3.02384907614376,-0.503663330587906,
-3.79654262601349));
#24676=CARTESIAN_POINT('Ctrl Pts',(3.02384907614375,-0.581090188608406,
-3.77851880307661));
#24677=CARTESIAN_POINT('Ctrl Pts',(3.02384907614375,-0.657936144092792,
-3.7580828506885));
#24678=CARTESIAN_POINT('Ctrl Pts',(3.02384907614375,-0.701243993644106,
-3.7465658209908));
#24679=CARTESIAN_POINT('Ctrl Pts',(3.02384907614375,-0.744367230915085,
-3.73428252775564));
#24680=CARTESIAN_POINT('Ctrl Pts',(3.02384907614375,-0.787281908431366,
-3.72122819379682));
#24681=CARTESIAN_POINT('Ctrl Pts',(3.02384907614375,-0.813120406729992,
-3.71336830982923));
#24682=CARTESIAN_POINT('Ctrl Pts',(3.02384907614375,-0.838889973343018,
-3.70522654477816));
#24683=CARTESIAN_POINT('Ctrl Pts',(3.02384907614375,-0.864545043675188,
-3.69681537290214));
#24684=CARTESIAN_POINT('Ctrl Pts',(3.02384907614375,-0.976135859364577,
-3.66022964078777));
#24685=CARTESIAN_POINT('Ctrl Pts',(3.02384907614374,-1.08569188131441,-3.6185141205333));
#24686=CARTESIAN_POINT('Ctrl Pts',(3.02384907614375,-1.19283428496982,-3.57167684930927));
#24687=CARTESIAN_POINT('Ctrl Pts',(3.02384907614375,-1.23792927339732,-3.55196358796956));
#24688=CARTESIAN_POINT('Ctrl Pts',(3.02384907614375,-1.28259643581524,-3.53134245497185));
#24689=CARTESIAN_POINT('Ctrl Pts',(3.02384907614375,-1.32680617741714,-3.50981161930699));
#24690=CARTESIAN_POINT('Ctrl Pts',(3.02384907614375,-1.43295276301009,-3.45811657183608));
#24691=CARTESIAN_POINT('Ctrl Pts',(3.02384907614375,-1.53646498001698,-3.40117991937055));
#24692=CARTESIAN_POINT('Ctrl Pts',(3.02384907614376,-1.63705571648453,-3.33929701181508));
#24693=CARTESIAN_POINT('Ctrl Pts',(3.02384907614375,-1.73742382560611,-3.27755106346635));
#24694=CARTESIAN_POINT('Ctrl Pts',(3.02384907614375,-1.8348839104347,-3.21088000755977));
#24695=CARTESIAN_POINT('Ctrl Pts',(3.02384907614375,-1.92911029541134,-3.13954526120031));
#24696=CARTESIAN_POINT('Ctrl Pts',(3.02384907614375,-1.98067917691666,-3.10050467736453));
#24697=CARTESIAN_POINT('Ctrl Pts',(3.02384907614375,-2.0312787351562,-3.06006671454503));
#24698=CARTESIAN_POINT('Ctrl Pts',(3.02384907614375,-2.08084955088305,-3.01827133086486));
#24699=CARTESIAN_POINT('Ctrl Pts',(3.02384907614375,-2.10068222578663,-3.00154951088178));
#24700=CARTESIAN_POINT('Ctrl Pts',(3.02384907614375,-2.12033510199988,-2.98462300334752));
#24701=CARTESIAN_POINT('Ctrl Pts',(3.02384907614375,-2.13979707289644,-2.96750248510469));
#24702=CARTESIAN_POINT('Ctrl Pts',(3.02384907614375,-2.22654408713123,-2.89119192809017));
#24703=CARTESIAN_POINT('Ctrl Pts',(3.02384907614375,-2.30955532853918,-2.81098435880976));
#24704=CARTESIAN_POINT('Ctrl Pts',(3.02384907614375,-2.38857390968403,-2.7271714464646));
#24705=CARTESIAN_POINT('Ctrl Pts',(3.02384907614375,-2.46731588582698,-2.64365192170554));
#24706=CARTESIAN_POINT('Ctrl Pts',(3.02384907614375,-2.54209358615361,-2.55655152694044));
#24707=CARTESIAN_POINT('Ctrl Pts',(3.02384907614375,-2.61261003092816,-2.46613020119734));
#24708=CARTESIAN_POINT('Ctrl Pts',(3.02384907614375,-2.68187774753533,-2.37731008573575));
#24709=CARTESIAN_POINT('Ctrl Pts',(3.02384907614376,-2.74703411602985,-2.28528492198977));
#24710=CARTESIAN_POINT('Ctrl Pts',(3.02384907614376,-2.80775053351277,-2.19028389748536));
#24711=CARTESIAN_POINT('Ctrl Pts',(3.02384907614376,-2.82131446704313,-2.16906084719494));
#24712=CARTESIAN_POINT('Ctrl Pts',(3.02384907614375,-2.83465661709219,-2.14768923548602));
#24713=CARTESIAN_POINT('Ctrl Pts',(3.02384907614375,-2.84777296580223,-2.12617155036607));
#24714=CARTESIAN_POINT('Ctrl Pts',(3.15165719587644,2.84680317627431,-2.71057532546662));
#24715=CARTESIAN_POINT('Ctrl Pts',(3.12190753622973,2.44054601589642,-3.13625204053632));
#24716=CARTESIAN_POINT('Ctrl Pts',(3.07930482965216,1.72451086510843,-3.61812557132028));
#24717=CARTESIAN_POINT('Ctrl Pts',(3.03670212307461,0.907492295035082,-3.83572132698351));
#24718=CARTESIAN_POINT('Ctrl Pts',(3.02384907614375,0.656739510617909,-3.87731438084271));
#24719=CARTESIAN_POINT('Ctrl Pts',(4.86717770674282,2.84754200119055,-1.50592095217182));
#24720=CARTESIAN_POINT('Ctrl Pts',(4.81923562020286,2.48464485522122,-2.19213412441211));
#24721=CARTESIAN_POINT('Ctrl Pts',(4.72336312115783,1.24432634307189,-3.28827073269437));
#24722=CARTESIAN_POINT('Ctrl Pts',(4.57954853557285,-1.24432634307187,-3.28827073269438));
#24723=CARTESIAN_POINT('Ctrl Pts',(4.48367603652783,-2.48464485522121,-2.19213412441212));
#24724=CARTESIAN_POINT('Ctrl Pts',(4.43573394998787,-2.84754200119054,-1.50592095217184));
#24725=CARTESIAN_POINT('Ctrl Pts',(4.73019663001395,3.05727666799789,-1.61683901027592));
#24726=CARTESIAN_POINT('Ctrl Pts',(4.68225454347398,2.66765046519168,-2.35359496326481));
#24727=CARTESIAN_POINT('Ctrl Pts',(4.58638204442896,1.33597674571904,-3.5304671133643));
#24728=CARTESIAN_POINT('Ctrl Pts',(4.44256745884398,-1.33597674571901,-3.53046711336431));
#24729=CARTESIAN_POINT('Ctrl Pts',(4.34669495979896,-2.66765046519166,-2.35359496326483));
#24730=CARTESIAN_POINT('Ctrl Pts',(4.29875287325899,-3.05727666799787,-1.61683901027595));
#24731=CARTESIAN_POINT('Ctrl Pts',(4.59321555328507,3.26701133480523,-1.72775706838004));
#24732=CARTESIAN_POINT('Ctrl Pts',(4.54527346674511,2.85065607516215,-2.51505580211753));
#24733=CARTESIAN_POINT('Ctrl Pts',(4.44940096770009,1.4276271483662,-3.77266349403423));
#24734=CARTESIAN_POINT('Ctrl Pts',(4.30558638211511,-1.42762714836615,-3.77266349403425));
#24735=CARTESIAN_POINT('Ctrl Pts',(4.20971388307008,-2.85065607516212,-2.51505580211756));
#24736=CARTESIAN_POINT('Ctrl Pts',(4.16177179653012,-3.26701133480521,-1.72775706838007));
#24737=CARTESIAN_POINT('Ctrl Pts',(4.4562344765562,3.47674600161257,-1.83867512648414));
#24738=CARTESIAN_POINT('Ctrl Pts',(4.40829239001624,3.03366168513261,-2.67651664097024));
#24739=CARTESIAN_POINT('Ctrl Pts',(4.31241989097121,1.51927755101335,-4.01485987470417));
#24740=CARTESIAN_POINT('Ctrl Pts',(4.16860530538623,-1.5192775510133,-4.01485987470418));
#24741=CARTESIAN_POINT('Ctrl Pts',(4.07273280634121,-3.03366168513258,-2.67651664097028));
#24742=CARTESIAN_POINT('Ctrl Pts',(4.02479071980125,-3.47674600161254,-1.83867512648419));
#24743=CARTESIAN_POINT('Ctrl Pts',(4.40165719587644,2.84679199383306,-2.71057163545836));
#24744=CARTESIAN_POINT('Ctrl Pts',(4.37190753622973,2.44052493609236,-3.13624479621667));
#24745=CARTESIAN_POINT('Ctrl Pts',(4.29422746407797,1.13490282761621,-4.01485987470402));
#24746=CARTESIAN_POINT('Ctrl Pts',(4.18679773227948,-1.13490282761596,-4.01485987470424));
#24747=CARTESIAN_POINT('Ctrl Pts',(4.10911766012771,-2.44052493609232,-3.1362447962167));
#24748=CARTESIAN_POINT('Ctrl Pts',(4.079368000481,-2.84679199383302,-2.7105716354584));
#24749=CARTESIAN_POINT('Ctrl Pts',(6.11718155610245,2.8475374478682,-1.50591584613134));
#24750=CARTESIAN_POINT('Ctrl Pts',(6.06923942046241,2.484641192321,-2.19212864202859));
#24751=CARTESIAN_POINT('Ctrl Pts',(5.9733668723173,1.24427323296847,-3.28824777229012));
#24752=CARTESIAN_POINT('Ctrl Pts',(5.82955218853213,-1.24427323296843,-3.28824777229013));
#24753=CARTESIAN_POINT('Ctrl Pts',(5.73367964038703,-2.48464119232097,-2.19212864202862));
#24754=CARTESIAN_POINT('Ctrl Pts',(5.68573750474698,-2.84753744786818,-1.50591584613138));
#24755=CARTESIAN_POINT('Ctrl Pts',(5.98019924535379,3.05727408623409,-1.61683474816929));
#24756=CARTESIAN_POINT('Ctrl Pts',(5.93225710971374,2.66764854543341,-2.35359085303088));
#24757=CARTESIAN_POINT('Ctrl Pts',(5.83638456156864,1.33592073185802,-3.53044512579308));
#24758=CARTESIAN_POINT('Ctrl Pts',(5.69256987778346,-1.33592073185797,-3.5304451257931));
#24759=CARTESIAN_POINT('Ctrl Pts',(5.59669732963837,-2.66764854543338,-2.35359085303092));
#24760=CARTESIAN_POINT('Ctrl Pts',(5.54875519399832,-3.05727408623406,-1.61683474816934));
#24761=CARTESIAN_POINT('Ctrl Pts',(5.84321693460512,3.26701072459998,-1.72775365020725));
#24762=CARTESIAN_POINT('Ctrl Pts',(5.79527479896508,2.85065589854583,-2.51505306403319));
#24763=CARTESIAN_POINT('Ctrl Pts',(5.69940225081997,1.42756823074758,-3.77264247929604));
#24764=CARTESIAN_POINT('Ctrl Pts',(5.5555875670348,-1.42756823074751,-3.77264247929606));
#24765=CARTESIAN_POINT('Ctrl Pts',(5.4597150188897,-2.85065589854579,-2.51505306403324));
#24766=CARTESIAN_POINT('Ctrl Pts',(5.41177288324965,-3.26701072459995,-1.7277536502073));
#24767=CARTESIAN_POINT('Ctrl Pts',(5.70623462385646,3.47674736296587,-1.8386725522452));
#24768=CARTESIAN_POINT('Ctrl Pts',(5.65829248821641,3.03366325165824,-2.67651527503548));
#24769=CARTESIAN_POINT('Ctrl Pts',(5.56241994007131,1.51921572963714,-4.01483983279899));
#24770=CARTESIAN_POINT('Ctrl Pts',(5.41860525628614,-1.51921572963706,-4.01483983279902));
#24771=CARTESIAN_POINT('Ctrl Pts',(5.32273270814104,-3.03366325165819,-2.67651527503554));
#24772=CARTESIAN_POINT('Ctrl Pts',(5.27479057250099,-3.47674736296583,-1.83867255224527));
#24773=CARTESIAN_POINT('Ctrl Pts',(5.65165719587644,2.8467821456932,-2.71056813036079));
#24774=CARTESIAN_POINT('Ctrl Pts',(5.62190753622973,2.44050637155411,-3.13623791491845));
#24775=CARTESIAN_POINT('Ctrl Pts',(5.54422746407797,1.13485587203874,-4.01483983279886));
#24776=CARTESIAN_POINT('Ctrl Pts',(5.43679773227948,-1.13485587203849,-4.01483983279907));
#24777=CARTESIAN_POINT('Ctrl Pts',(5.35911766012771,-2.44050637155405,-3.1362379149185));
#24778=CARTESIAN_POINT('Ctrl Pts',(5.329368000481,-2.84678214569315,-2.71056813036084));
#24779=CARTESIAN_POINT('Ctrl Pts',(7.36718503194766,2.8475333363626,-1.505911235551));
#24780=CARTESIAN_POINT('Ctrl Pts',(7.31924285197185,2.48463788473179,-2.19212369184276));
#24781=CARTESIAN_POINT('Ctrl Pts',(7.22337025949097,1.24422607800448,-3.28822624954172));
#24782=CARTESIAN_POINT('Ctrl Pts',(7.07955548703428,-1.24422607800445,-3.28822624954172));
#24783=CARTESIAN_POINT('Ctrl Pts',(6.98368289455341,-2.48463788473177,-2.19212369184278));
#24784=CARTESIAN_POINT('Ctrl Pts',(6.9357407145776,-2.8475333363626,-1.50591123555103));
#24785=CARTESIAN_POINT('Ctrl Pts',(7.2302016069197,3.05727175498223,-1.61683089963102));
#24786=CARTESIAN_POINT('Ctrl Pts',(7.18225942694387,2.6676468118377,-2.35358714186614));
#24787=CARTESIAN_POINT('Ctrl Pts',(7.086386834463,1.33587101387704,-3.53042442325068));
#24788=CARTESIAN_POINT('Ctrl Pts',(6.94257206200631,-1.335871013877,-3.53042442325069));
#24789=CARTESIAN_POINT('Ctrl Pts',(6.84669946952544,-2.66764681183767,-2.35358714186617));
#24790=CARTESIAN_POINT('Ctrl Pts',(6.79875728954964,-3.05727175498221,-1.61683089963105));
#24791=CARTESIAN_POINT('Ctrl Pts',(7.09321818189172,3.26701017360185,-1.72775056371102));
#24792=CARTESIAN_POINT('Ctrl Pts',(7.04527600191591,2.85065573894362,-2.51505059188952));
#24793=CARTESIAN_POINT('Ctrl Pts',(6.94940340943504,1.42751594974962,-3.77262259695963));
#24794=CARTESIAN_POINT('Ctrl Pts',(6.80558863697834,-1.42751594974956,-3.77262259695965));
#24795=CARTESIAN_POINT('Ctrl Pts',(6.70971604449747,-2.85065573894359,-2.51505059188955));
#24796=CARTESIAN_POINT('Ctrl Pts',(6.66177386452166,-3.26701017360182,-1.72775056371106));
#24797=CARTESIAN_POINT('Ctrl Pts',(6.95623475686376,3.47674859222147,-1.83867022779103));
#24798=CARTESIAN_POINT('Ctrl Pts',(6.90829257688794,3.03366466604953,-2.67651404191289));
#24799=CARTESIAN_POINT('Ctrl Pts',(6.81241998440707,1.51916088562219,-4.01482077066858));
#24800=CARTESIAN_POINT('Ctrl Pts',(6.66860521195038,-1.51916088562212,-4.01482077066861));
#24801=CARTESIAN_POINT('Ctrl Pts',(6.57273261946951,-3.03366466604949,-2.67651404191294));
#24802=CARTESIAN_POINT('Ctrl Pts',(6.5247904394937,-3.47674859222144,-1.83867022779109));
#24803=CARTESIAN_POINT('Ctrl Pts',(6.90165719587644,2.84677340648494,-2.71056479661449));
#24804=CARTESIAN_POINT('Ctrl Pts',(6.87190753622973,2.44048989744138,-3.13623137002149));
#24805=CARTESIAN_POINT('Ctrl Pts',(6.79422746407799,1.13481420380713,-4.01482077066858));
#24806=CARTESIAN_POINT('Ctrl Pts',(6.68679773227946,-1.13481420380722,-4.01482077066861));
#24807=CARTESIAN_POINT('Ctrl Pts',(6.60911766012771,-2.44048989744134,-3.13623137002152));
#24808=CARTESIAN_POINT('Ctrl Pts',(6.579368000481,-2.8467734064849,-2.71056479661452));
#24809=CARTESIAN_POINT('Ctrl Pts',(8.61718818994175,2.84752960083224,-1.50590704659367));
#24810=CARTESIAN_POINT('Ctrl Pts',(8.56924596968449,2.48463487950633,-2.19211919452613));
#24811=CARTESIAN_POINT('Ctrl Pts',(8.47337333692217,1.24418392764402,-3.28820601234521));
#24812=CARTESIAN_POINT('Ctrl Pts',(8.32955848390258,-1.24418392764399,-3.28820601234522));
#24813=CARTESIAN_POINT('Ctrl Pts',(8.23368585114026,-2.48463487950632,-2.19211919452615));
#24814=CARTESIAN_POINT('Ctrl Pts',(8.18574363088299,-2.84752960083223,-1.5059070465937));
#24815=CARTESIAN_POINT('Ctrl Pts',(8.48020375253053,3.05726963691,-1.61682740302824));
#24816=CARTESIAN_POINT('Ctrl Pts',(8.43226153227327,2.66764523666483,-2.35358377028059));
#24817=CARTESIAN_POINT('Ctrl Pts',(8.33638889951095,1.33582658582575,-3.53040488095707));
#24818=CARTESIAN_POINT('Ctrl Pts',(8.19257404649136,-1.33582658582571,-3.53040488095709));
#24819=CARTESIAN_POINT('Ctrl Pts',(8.09670141372905,-2.66764523666481,-2.35358377028062));
#24820=CARTESIAN_POINT('Ctrl Pts',(8.04875919347178,-3.05726963690998,-1.61682740302827));
#24821=CARTESIAN_POINT('Ctrl Pts',(8.34321931511932,3.26700967298776,-1.7277477594628));
#24822=CARTESIAN_POINT('Ctrl Pts',(8.29527709486206,2.85065559382334,-2.51504834603505));
#24823=CARTESIAN_POINT('Ctrl Pts',(8.19940446209974,1.42746924400749,-3.77260374956895));
#24824=CARTESIAN_POINT('Ctrl Pts',(8.05558960908014,-1.42746924400744,-3.77260374956897));
#24825=CARTESIAN_POINT('Ctrl Pts',(7.95971697631782,-2.85065559382331,-2.51504834603509));
#24826=CARTESIAN_POINT('Ctrl Pts',(7.91177475606056,-3.26700967298774,-1.72774775946284));
#24827=CARTESIAN_POINT('Ctrl Pts',(8.20623487770811,3.47674970906552,-1.83866811589737));
#24828=CARTESIAN_POINT('Ctrl Pts',(8.15829265745084,3.03366595098184,-2.67651292178951));
#24829=CARTESIAN_POINT('Ctrl Pts',(8.06242002468851,1.51911190218921,-4.01480261818081));
#24830=CARTESIAN_POINT('Ctrl Pts',(7.91860517166893,-1.51911190218915,-4.01480261818084));
#24831=CARTESIAN_POINT('Ctrl Pts',(7.82273253890661,-3.0336659509818,-2.67651292178956));
#24832=CARTESIAN_POINT('Ctrl Pts',(7.77479031864935,-3.47674970906549,-1.83866811589743));
#24833=CARTESIAN_POINT('Ctrl Pts',(8.15165719587644,2.84676559888789,-2.71056162195416));
#24834=CARTESIAN_POINT('Ctrl Pts',(8.12190753622973,2.44047517949096,-3.13622513744625));
#24835=CARTESIAN_POINT('Ctrl Pts',(8.04422746407799,1.13477697746454,-4.0148026181808));
#24836=CARTESIAN_POINT('Ctrl Pts',(7.93679773227946,-1.13477697746461,-4.01480261818084));
#24837=CARTESIAN_POINT('Ctrl Pts',(7.85911766012771,-2.44047517949091,-3.13622513744629));
#24838=CARTESIAN_POINT('Ctrl Pts',(7.829368000481,-2.84676559888785,-2.71056162195421));
#24839=CARTESIAN_POINT('Ctrl Pts',(9.86719107484073,2.8475261883373,-1.50590321989084));
#24840=CARTESIAN_POINT('Ctrl Pts',(9.81924881778544,2.48463213407324,-2.19211508629638));
#24841=CARTESIAN_POINT('Ctrl Pts',(9.72337614822511,1.24414602360339,-3.28818693250078));
#24842=CARTESIAN_POINT('Ctrl Pts',(9.57956122160949,-1.24414602360339,-3.28818693250078));
#24843=CARTESIAN_POINT('Ctrl Pts',(9.48368855204915,-2.48463213407324,-2.19211508629638));
#24844=CARTESIAN_POINT('Ctrl Pts',(9.43574629499388,-2.8475261883373,-1.50590321989084));
#24845=CARTESIAN_POINT('Ctrl Pts',(9.73020571259453,3.05726770200041,-1.61682420880526));
#24846=CARTESIAN_POINT('Ctrl Pts',(9.68226345553925,2.66764379761156,-2.35358069044312));
#24847=CARTESIAN_POINT('Ctrl Pts',(9.58639078597891,1.33578664530418,-3.53038639224751));
#24848=CARTESIAN_POINT('Ctrl Pts',(9.4425758593633,-1.33578664530417,-3.53038639224751));
#24849=CARTESIAN_POINT('Ctrl Pts',(9.34670318980296,-2.66764379761156,-2.35358069044313));
#24850=CARTESIAN_POINT('Ctrl Pts',(9.29876093274769,-3.05726770200041,-1.61682420880527));
#24851=CARTESIAN_POINT('Ctrl Pts',(9.59322035034834,3.26700921566353,-1.72774519771967));
#24852=CARTESIAN_POINT('Ctrl Pts',(9.54527809329306,2.85065546114989,-2.51504629458986));
#24853=CARTESIAN_POINT('Ctrl Pts',(9.44940542373273,1.42742726700498,-3.77258585199426));
#24854=CARTESIAN_POINT('Ctrl Pts',(9.30559049711711,-1.42742726700496,-3.77258585199426));
#24855=CARTESIAN_POINT('Ctrl Pts',(9.20971782755677,-2.85065546114988,-2.51504629458988));
#24856=CARTESIAN_POINT('Ctrl Pts',(9.16177557050149,-3.26700921566353,-1.72774519771969));
#24857=CARTESIAN_POINT('Ctrl Pts',(9.45623498810215,3.47675072932665,-1.83866618663408));
#24858=CARTESIAN_POINT('Ctrl Pts',(9.40829273104687,3.03366712468821,-2.6765118987366));
#24859=CARTESIAN_POINT('Ctrl Pts',(9.31242006148653,1.51906788870579,-4.014785311741));
#24860=CARTESIAN_POINT('Ctrl Pts',(9.16860513487091,-1.51906788870575,-4.01478531174101));
#24861=CARTESIAN_POINT('Ctrl Pts',(9.07273246531058,-3.03366712468819,-2.67651189873662));
#24862=CARTESIAN_POINT('Ctrl Pts',(9.02479020825531,-3.47675072932664,-1.8386661866341));
#24863=CARTESIAN_POINT('Ctrl Pts',(9.40165719587644,2.84675858147378,-2.71055859525787));
#24864=CARTESIAN_POINT('Ctrl Pts',(9.37190753622973,2.44046195109913,-3.1362191953578));
#24865=CARTESIAN_POINT('Ctrl Pts',(9.29422746407799,1.13474351868581,-4.01478531174101));
#24866=CARTESIAN_POINT('Ctrl Pts',(9.18679773227947,-1.13474351868577,-4.01478531174101));
#24867=CARTESIAN_POINT('Ctrl Pts',(9.10911766012771,-2.4404619510991,-3.13621919535782));
#24868=CARTESIAN_POINT('Ctrl Pts',(9.079368000481,-2.84675858147374,-2.7105585952579));
#24869=CARTESIAN_POINT('Ctrl Pts',(11.102826855619,2.7325876658857,-1.7059759760899));
#24870=CARTESIAN_POINT('Ctrl Pts',(11.0564761776969,2.33512269759968,-2.34262495894918));
#24871=CARTESIAN_POINT('Ctrl Pts',(10.9637748218525,1.07966271388233,-3.32492883043245));
#24872=CARTESIAN_POINT('Ctrl Pts',(10.8247124167047,-1.31450087230183,-3.2393423413749));
#24873=CARTESIAN_POINT('Ctrl Pts',(10.7320006894791,-2.49670104301917,-2.16966721227558));
#24874=CARTESIAN_POINT('Ctrl Pts',(10.6856396401757,-2.84766280119442,-1.50605642114679));
#24875=CARTESIAN_POINT('Ctrl Pts',(10.965701366658,2.93405695958231,-1.83175484103065));
#24876=CARTESIAN_POINT('Ctrl Pts',(10.9193506887358,2.50728753844033,-2.515342929453));
#24877=CARTESIAN_POINT('Ctrl Pts',(10.8266493328915,1.15926450932041,-3.57007048550964));
#24878=CARTESIAN_POINT('Ctrl Pts',(10.6875869277437,-1.41141690746236,-3.47817384226539));
#24879=CARTESIAN_POINT('Ctrl Pts',(10.594875200518,-2.6807787953959,-2.32963328629069));
#24880=CARTESIAN_POINT('Ctrl Pts',(10.5485141512146,-3.05761639953827,-1.6170955388387));
#24881=CARTESIAN_POINT('Ctrl Pts',(10.828575877697,3.13552625327892,-1.9575337059714));
#24882=CARTESIAN_POINT('Ctrl Pts',(10.7822251997748,2.67945237928098,-2.68806089995681));
#24883=CARTESIAN_POINT('Ctrl Pts',(10.6895238439304,1.23886630475848,-3.81521214058682));
#24884=CARTESIAN_POINT('Ctrl Pts',(10.5504614387827,-1.50833294262289,-3.71700534315589));
#24885=CARTESIAN_POINT('Ctrl Pts',(10.4577497115571,-2.86485654777264,-2.48959936030581));
#24886=CARTESIAN_POINT('Ctrl Pts',(10.4113886622536,-3.26756999788213,-1.72813465653059));
#24887=CARTESIAN_POINT('Ctrl Pts',(10.6914503887359,3.33699554697554,-2.08331257091215));
#24888=CARTESIAN_POINT('Ctrl Pts',(10.6450997108137,2.85161722012163,-2.86077887046062));
#24889=CARTESIAN_POINT('Ctrl Pts',(10.5523983549694,1.31846810019657,-4.060353795664));
#24890=CARTESIAN_POINT('Ctrl Pts',(10.4133359498216,-1.60524897778342,-3.95583684404638));
#24891=CARTESIAN_POINT('Ctrl Pts',(10.320624222596,-3.04893430014939,-2.64956543432092));
#24892=CARTESIAN_POINT('Ctrl Pts',(10.2742631732926,-3.47752359622599,-1.83917377422248));
#24893=CARTESIAN_POINT('Ctrl Pts',(10.6516571958764,2.84853760141617,-2.71188542038896));
#24894=CARTESIAN_POINT('Ctrl Pts',(10.6455290770758,2.76494594567757,-2.79968926812744));
#24895=CARTESIAN_POINT('Ctrl Pts',(10.6394009582753,2.67728929704302,-2.88362738694732));
#24896=CARTESIAN_POINT('Ctrl Pts',(10.6332728394747,2.58595065464962,-2.96333396898109));
#24897=CARTESIAN_POINT('Ctrl Pts',(10.6271443176134,2.49460600469932,-3.04304579350383));
#24898=CARTESIAN_POINT('Ctrl Pts',(10.6210157957521,2.39957915068204,-3.11852529051356));
#24899=CARTESIAN_POINT('Ctrl Pts',(10.6148872738908,2.30128712085601,-3.18944612548672));
#24900=CARTESIAN_POINT('Ctrl Pts',(10.6087557427774,2.20294682727241,-3.26040178430055));
#24901=CARTESIAN_POINT('Ctrl Pts',(10.602624211664,2.1013384467335,-3.32679409720055));
#24902=CARTESIAN_POINT('Ctrl Pts',(10.5964926805506,1.99690932938873,-3.38833914037545));
#24903=CARTESIAN_POINT('Ctrl Pts',(10.5903597344877,1.89245611334498,-3.44989838605925));
#24904=CARTESIAN_POINT('Ctrl Pts',(10.5842267884249,1.78518117652743,-3.50660795423693));
#24905=CARTESIAN_POINT('Ctrl Pts',(10.5780938423621,1.67555727819519,-3.55822944840367));
#24906=CARTESIAN_POINT('Ctrl Pts',(10.571956787069,1.56585992905622,-3.6098855302876));
#24907=CARTESIAN_POINT('Ctrl Pts',(10.5658197317759,1.45381080309502,-3.65644657945933));
#24908=CARTESIAN_POINT('Ctrl Pts',(10.5596826764829,1.33990384989523,-3.69772182201906));
#24909=CARTESIAN_POINT('Ctrl Pts',(10.5574317208016,1.29812493619831,-3.71286079947636));
#24910=CARTESIAN_POINT('Ctrl Pts',(10.5551807651203,1.25609626319755,-3.72728916258503));
#24911=CARTESIAN_POINT('Ctrl Pts',(10.552929809439,1.21384274673912,-3.74099916949855));
#24912=CARTESIAN_POINT('Ctrl Pts',(10.5469118194765,1.10087684516881,-3.77765323811422));
#24913=CARTESIAN_POINT('Ctrl Pts',(10.5408938295139,0.986170791072762,-3.80921187257292));
#24914=CARTESIAN_POINT('Ctrl Pts',(10.5348758395513,0.870210701742948,-3.83552112946494));
#24915=CARTESIAN_POINT('Ctrl Pts',(10.5288613570294,0.754318196961284,-3.86181505263957));
#24916=CARTESIAN_POINT('Ctrl Pts',(10.5228468745075,0.637173487249866,-3.88286560447526));
#24917=CARTESIAN_POINT('Ctrl Pts',(10.5168323919856,0.519276265212455,-3.89856911704628));
#24918=CARTESIAN_POINT('Ctrl Pts',(10.5108202615803,0.401425149887673,-3.91426648835859));
#24919=CARTESIAN_POINT('Ctrl Pts',(10.504808131175,0.282822490030062,-3.92462093396961));
#24920=CARTESIAN_POINT('Ctrl Pts',(10.4987960007697,0.163976196133212,-3.92958023293859));
#24921=CARTESIAN_POINT('Ctrl Pts',(10.4927850693528,0.0451536035376617,
-3.93453854288355));
#24922=CARTESIAN_POINT('Ctrl Pts',(10.4867741379358,-0.0739121412827665,
-3.93410383408152));
#24923=CARTESIAN_POINT('Ctrl Pts',(10.4807632065188,-0.192710362649327,
-3.92827592158794));
#24924=CARTESIAN_POINT('Ctrl Pts',(10.4747504825599,-0.311544011269225,
-3.9224462711312));
#24925=CARTESIAN_POINT('Ctrl Pts',(10.468737758601,-0.430109591454027,-3.91122021779041));
#24926=CARTESIAN_POINT('Ctrl Pts',(10.4627250346421,-0.547898680884157,
-3.89464966787584));
#24927=CARTESIAN_POINT('Ctrl Pts',(10.4567115633265,-0.665702411011273,
-3.8780770583104));
#24928=CARTESIAN_POINT('Ctrl Pts',(10.4506980920108,-0.78272907699905,-3.85615868874641));
#24929=CARTESIAN_POINT('Ctrl Pts',(10.4446846206952,-0.898478527493888,
-3.82899795450878));
#24930=CARTESIAN_POINT('Ctrl Pts',(10.4386665678898,-1.01431616414513,-3.8018165272938));
#24931=CARTESIAN_POINT('Ctrl Pts',(10.4326485150844,-1.12887426660863,-3.76938484928543));
#24932=CARTESIAN_POINT('Ctrl Pts',(10.426630462279,-1.2416656642706,-3.73185682712661));
#24933=CARTESIAN_POINT('Ctrl Pts',(10.4223795667435,-1.32133669147319,-3.70534863469126));
#24934=CARTESIAN_POINT('Ctrl Pts',(10.418128671208,-1.40012652562735,-3.67629872628921));
#24935=CARTESIAN_POINT('Ctrl Pts',(10.4138777756725,-1.47786921651355,-3.64477592985929));
#24936=CARTESIAN_POINT('Ctrl Pts',(10.4076700973785,-1.59139861536529,-3.5987424817239));
#24937=CARTESIAN_POINT('Ctrl Pts',(10.4014624190846,-1.70282111743399,-3.54738213142518));
#24938=CARTESIAN_POINT('Ctrl Pts',(10.3952547407906,-1.81164015590211,-3.49090947254766));
#24939=CARTESIAN_POINT('Ctrl Pts',(10.3890514358049,-1.92038253137729,-3.43447659864811));
#24940=CARTESIAN_POINT('Ctrl Pts',(10.3828481308192,-2.02652479741291,-3.37293875908211));
#24941=CARTESIAN_POINT('Ctrl Pts',(10.3766448258335,-2.12959335724681,-3.30655729313288));
#24942=CARTESIAN_POINT('Ctrl Pts',(10.3704446314107,-2.23261023475236,-3.24020911326745));
#24943=CARTESIAN_POINT('Ctrl Pts',(10.364244436988,-2.33255619023717,-3.16902233521461));
#24944=CARTESIAN_POINT('Ctrl Pts',(10.3580442425652,-2.42898482509644,-3.09330272030579));
#24945=CARTESIAN_POINT('Ctrl Pts',(10.3518470240126,-2.52536717768228,-3.01761944808633));
#24946=CARTESIAN_POINT('Ctrl Pts',(10.34564980546,-2.61823530659864,-2.93740789034966));
#24947=CARTESIAN_POINT('Ctrl Pts',(10.3394525869073,-2.70717424489736,-2.85301535358021));
#24948=CARTESIAN_POINT('Ctrl Pts',(10.3360910580986,-2.75541698489033,-2.80723869729676));
#24949=CARTESIAN_POINT('Ctrl Pts',(10.3327295292898,-2.80250421571315,-2.76023260054377));
#24950=CARTESIAN_POINT('Ctrl Pts',(10.329368000481,-2.84837393363742,-2.71205732501636));
#24951=CARTESIAN_POINT('Origin',(11.0238490761436,0.781229937496414,-0.42649944676949));
#24952=CARTESIAN_POINT('Ctrl Pts',(4.24217562075336,-2.84754446865879,1.50592371916677));
#24953=CARTESIAN_POINT('Ctrl Pts',(4.19423356082101,-2.48464684011856,2.19213709545128));
#24954=CARTESIAN_POINT('Ctrl Pts',(4.0983610883836,-1.24435549640673,3.2882828077279));
#24955=CARTESIAN_POINT('Ctrl Pts',(3.95454655601384,1.24435549640671,3.2882828077279));
#24956=CARTESIAN_POINT('Ctrl Pts',(3.85867408357643,2.48464684011855,2.1921370954513));
#24957=CARTESIAN_POINT('Ctrl Pts',(3.81073202364408,2.84754446865879,1.50592371916679));
#24958=CARTESIAN_POINT('Ctrl Pts',(4.10519521274669,-3.05727806706812,1.61684131993722));
#24959=CARTESIAN_POINT('Ctrl Pts',(4.05725315281434,-2.66765150546796,2.35359719073546));
#24960=CARTESIAN_POINT('Ctrl Pts',(3.96138068037693,-1.33600750003101,3.53047863414712));
#24961=CARTESIAN_POINT('Ctrl Pts',(3.81756614800717,1.33600750003098,3.53047863414713));
#24962=CARTESIAN_POINT('Ctrl Pts',(3.72169367556977,2.66765150546794,2.35359719073547));
#24963=CARTESIAN_POINT('Ctrl Pts',(3.67375161563742,3.05727806706811,1.61684131993725));
#24964=CARTESIAN_POINT('Ctrl Pts',(3.96821480474003,-3.26701166547745,1.72775892070767));
#24965=CARTESIAN_POINT('Ctrl Pts',(3.92027274480768,-2.85065617081736,2.51505728601962));
#24966=CARTESIAN_POINT('Ctrl Pts',(3.82440027237027,-1.42765950365529,3.77267446056633));
#24967=CARTESIAN_POINT('Ctrl Pts',(3.68058574000051,1.42765950365525,3.77267446056634));
#24968=CARTESIAN_POINT('Ctrl Pts',(3.5847132675631,2.85065617081734,2.51505728601966));
#24969=CARTESIAN_POINT('Ctrl Pts',(3.53677120763075,3.26701166547743,1.7277589207077));
#24970=CARTESIAN_POINT('Ctrl Pts',(3.83123439673337,-3.47674526388677,1.83867652147811));
#24971=CARTESIAN_POINT('Ctrl Pts',(3.78329233680102,-3.03366083616676,2.67651738130379));
#24972=CARTESIAN_POINT('Ctrl Pts',(3.68741986436361,-1.51931150727957,4.01487028698555));
#24973=CARTESIAN_POINT('Ctrl Pts',(3.54360533199384,1.51931150727952,4.01487028698557));
#24974=CARTESIAN_POINT('Ctrl Pts',(3.44773285955643,3.03366083616673,2.67651738130383));
#24975=CARTESIAN_POINT('Ctrl Pts',(3.39979079962409,3.47674526388675,1.83867652147816));
#24976=CARTESIAN_POINT('Ctrl Pts',(3.77665719587644,-2.84679740187303,2.71057345644603));
#24977=CARTESIAN_POINT('Ctrl Pts',(3.74690753622973,-2.44053513068406,3.13624837122676));
#24978=CARTESIAN_POINT('Ctrl Pts',(3.66922746407795,-1.1349286129563,4.01487028698564));
#24979=CARTESIAN_POINT('Ctrl Pts',(3.56179773227949,1.13492861295628,4.01487028698554));
#24980=CARTESIAN_POINT('Ctrl Pts',(3.48411766012771,2.44053513068398,3.13624837122682));
#24981=CARTESIAN_POINT('Ctrl Pts',(3.454368000481,2.84679740187295,2.71057345644611));
#24982=CARTESIAN_POINT('Ctrl Pts',(5.49217968210715,-2.84753966457653,1.50591833191943));
#24983=CARTESIAN_POINT('Ctrl Pts',(5.44423757037064,-2.48464297555693,2.19213131100178));
#24984=CARTESIAN_POINT('Ctrl Pts',(5.34836504612908,-1.24429897509366,3.28825906217306));
#24985=CARTESIAN_POINT('Ctrl Pts',(5.204550410151,1.24429897509362,3.28825906217308));
#24986=CARTESIAN_POINT('Ctrl Pts',(5.10867788590944,2.4846429755569,2.19213131100181));
#24987=CARTESIAN_POINT('Ctrl Pts',(5.06073577417293,2.84753966457651,1.50591833191947));
#24988=CARTESIAN_POINT('Ctrl Pts',(5.35519797212004,-3.05727534312249,1.6168368231029));
#24989=CARTESIAN_POINT('Ctrl Pts',(5.30725586038353,-2.66764948005118,2.35359285399424));
#24990=CARTESIAN_POINT('Ctrl Pts',(5.21138333614197,-1.33594787926937,3.53045595032151));
#24991=CARTESIAN_POINT('Ctrl Pts',(5.0675687001639,1.33594787926931,3.53045595032154));
#24992=CARTESIAN_POINT('Ctrl Pts',(4.97169617592234,2.66764948005114,2.35359285399428));
#24993=CARTESIAN_POINT('Ctrl Pts',(4.92375406418583,3.05727534312247,1.61683682310294));
#24994=CARTESIAN_POINT('Ctrl Pts',(5.21821626213294,-3.26701102166844,1.72775531428636));
#24995=CARTESIAN_POINT('Ctrl Pts',(5.17027415039643,-2.85065598454542,2.51505439698671));
#24996=CARTESIAN_POINT('Ctrl Pts',(5.07440162615487,-1.42759678344509,3.77265283846997));
#24997=CARTESIAN_POINT('Ctrl Pts',(4.9305869901768,1.42759678344502,3.77265283847));
#24998=CARTESIAN_POINT('Ctrl Pts',(4.83471446593522,2.85065598454537,2.51505439698676));
#24999=CARTESIAN_POINT('Ctrl Pts',(4.78677235419872,3.26701102166841,1.72775531428642));
#25000=CARTESIAN_POINT('Ctrl Pts',(5.08123455214584,-3.4767467002144,1.83867380546982));
#25001=CARTESIAN_POINT('Ctrl Pts',(5.03329244040933,-3.03366248903967,2.67651593997917));
#25002=CARTESIAN_POINT('Ctrl Pts',(4.93741991616776,-1.51924568762079,4.01484972661843));
#25003=CARTESIAN_POINT('Ctrl Pts',(4.79360528018969,1.51924568762071,4.01484972661846));
#25004=CARTESIAN_POINT('Ctrl Pts',(4.69773275594812,3.03366248903961,2.67651593997923));
#25005=CARTESIAN_POINT('Ctrl Pts',(4.64979064421162,3.47674670021436,1.83867380546989));
#25006=CARTESIAN_POINT('Ctrl Pts',(5.02665719587644,-2.84678691836037,2.71056986067545));
#25007=CARTESIAN_POINT('Ctrl Pts',(4.99690753622973,-2.44051536841681,3.13624131191695));
#25008=CARTESIAN_POINT('Ctrl Pts',(4.919227464078,-1.1348786279445,4.01484972661831));
#25009=CARTESIAN_POINT('Ctrl Pts',(4.81179773227947,1.13487862794425,4.0148497266185));
#25010=CARTESIAN_POINT('Ctrl Pts',(4.73411766012771,2.44051536841673,3.13624131191701));
#25011=CARTESIAN_POINT('Ctrl Pts',(4.704368000481,2.8467869183603,2.71056986067553));
#25012=CARTESIAN_POINT('Ctrl Pts',(6.74218333694333,-2.84753534134887,1.50591348391091));
#25013=CARTESIAN_POINT('Ctrl Pts',(6.69424117858796,-2.48463949769956,2.19212610578529));
#25014=CARTESIAN_POINT('Ctrl Pts',(6.59836860772753,-1.24424897566079,3.2882368413454));
#25015=CARTESIAN_POINT('Ctrl Pts',(6.45455387851173,1.24424897566077,3.28823684134541));
#25016=CARTESIAN_POINT('Ctrl Pts',(6.3586813076513,2.48463949769954,2.1921261057853));
#25017=CARTESIAN_POINT('Ctrl Pts',(6.31073914929593,2.84753534134886,1.50591348391094));
#25018=CARTESIAN_POINT('Ctrl Pts',(6.60520045529636,-3.05727289182331,1.61683277637956));
#25019=CARTESIAN_POINT('Ctrl Pts',(6.55725829694099,-2.66764765724454,2.35358895159519));
#25020=CARTESIAN_POINT('Ctrl Pts',(6.46138572608056,-1.33589515421597,3.53043462216624));
#25021=CARTESIAN_POINT('Ctrl Pts',(6.31757099686476,1.33589515421593,3.53043462216624));
#25022=CARTESIAN_POINT('Ctrl Pts',(6.22169842600433,2.66764765724452,2.35358895159521));
#25023=CARTESIAN_POINT('Ctrl Pts',(6.17375626764897,3.05727289182329,1.6168327763796));
#25024=CARTESIAN_POINT('Ctrl Pts',(6.46821757364939,-3.26701044229775,1.72775206884821));
#25025=CARTESIAN_POINT('Ctrl Pts',(6.42027541529402,-2.85065581678953,2.5150517974051));
#25026=CARTESIAN_POINT('Ctrl Pts',(6.32440284443359,-1.42754133277114,3.77263240298708));
#25027=CARTESIAN_POINT('Ctrl Pts',(6.18058811521779,1.4275413327711,3.77263240298709));
#25028=CARTESIAN_POINT('Ctrl Pts',(6.08471554435736,2.8506558167895,2.51505179740513));
#25029=CARTESIAN_POINT('Ctrl Pts',(6.03677338600199,3.26701044229773,1.72775206884825));
#25030=CARTESIAN_POINT('Ctrl Pts',(6.33123469200243,-3.4767479927722,1.83867136131686));
#25031=CARTESIAN_POINT('Ctrl Pts',(6.28329253364706,-3.03366397633451,2.676514643215));
#25032=CARTESIAN_POINT('Ctrl Pts',(6.18741996278662,-1.51918751132632,4.01483018380791));
#25033=CARTESIAN_POINT('Ctrl Pts',(6.04360523357082,1.51918751132626,4.01483018380792));
#25034=CARTESIAN_POINT('Ctrl Pts',(5.94773266271039,3.03366397633447,2.67651464321504));
#25035=CARTESIAN_POINT('Ctrl Pts',(5.89979050435502,3.47674799277217,1.83867136131692));
#25036=CARTESIAN_POINT('Ctrl Pts',(6.27665719587644,-2.84677764951821,2.71056644286375));
#25037=CARTESIAN_POINT('Ctrl Pts',(6.24690753622973,-2.44049789590145,3.13623460198065));
#25038=CARTESIAN_POINT('Ctrl Pts',(6.16922746407796,-1.13483443443749,4.01483018380789));
#25039=CARTESIAN_POINT('Ctrl Pts',(6.06179773227948,1.13483443443743,4.01483018380793));
#25040=CARTESIAN_POINT('Ctrl Pts',(5.98411766012771,2.44049789590139,3.13623460198069));
#25041=CARTESIAN_POINT('Ctrl Pts',(5.954368000481,2.84677764951816,2.71056644286381));
#25042=CARTESIAN_POINT('Ctrl Pts',(7.99218664765765,-2.84753142517089,1.50590909237341));
#25043=CARTESIAN_POINT('Ctrl Pts',(7.94424444707283,-2.48463634719471,2.19212139087745));
#25044=CARTESIAN_POINT('Ctrl Pts',(7.84837183398294,-1.2442044285308,3.28821597875606));
#25045=CARTESIAN_POINT('Ctrl Pts',(7.70455702030822,1.24420442853079,3.28821597875607));
#25046=CARTESIAN_POINT('Ctrl Pts',(7.60868440721834,2.4846363471947,2.19212139087746));
#25047=CARTESIAN_POINT('Ctrl Pts',(7.56074220663351,2.84753142517089,1.50590909237343));
#25048=CARTESIAN_POINT('Ctrl Pts',(7.85520270466869,-3.05727067132307,1.61682911067984));
#25049=CARTESIAN_POINT('Ctrl Pts',(7.80726050408387,-2.6676460059526,2.35358541685185));
#25050=CARTESIAN_POINT('Ctrl Pts',(7.71138789099398,-1.33584819287788,3.53041451411671));
#25051=CARTESIAN_POINT('Ctrl Pts',(7.56757307731927,1.33584819287785,3.53041451411673));
#25052=CARTESIAN_POINT('Ctrl Pts',(7.47170046422939,2.66764600595259,2.35358541685187));
#25053=CARTESIAN_POINT('Ctrl Pts',(7.42375826364456,3.05727067132306,1.61682911067986));
#25054=CARTESIAN_POINT('Ctrl Pts',(7.71821876167974,-3.26700991747524,1.72774912898627));
#25055=CARTESIAN_POINT('Ctrl Pts',(7.67027656109492,-2.8506556647105,2.51504944282623));
#25056=CARTESIAN_POINT('Ctrl Pts',(7.57440394800502,-1.42749195722496,3.77261304947736));
#25057=CARTESIAN_POINT('Ctrl Pts',(7.43058913433032,1.42749195722492,3.77261304947737));
#25058=CARTESIAN_POINT('Ctrl Pts',(7.33471652124043,2.85065566471048,2.51504944282626));
#25059=CARTESIAN_POINT('Ctrl Pts',(7.2867743206556,3.26700991747522,1.7277491289863));
#25060=CARTESIAN_POINT('Ctrl Pts',(7.58123481869079,-3.47674916362741,1.83866914729269));
#25061=CARTESIAN_POINT('Ctrl Pts',(7.53329261810597,-3.0336653234684,2.67651346880062));
#25062=CARTESIAN_POINT('Ctrl Pts',(7.43742000501609,-1.51913572157204,4.01481158483801));
#25063=CARTESIAN_POINT('Ctrl Pts',(7.29360519134137,1.51913572157199,4.01481158483803));
#25064=CARTESIAN_POINT('Ctrl Pts',(7.19773257825148,3.03366532346837,2.67651346880066));
#25065=CARTESIAN_POINT('Ctrl Pts',(7.14979037766666,3.47674916362739,1.83866914729274));
#25066=CARTESIAN_POINT('Ctrl Pts',(7.52665719587644,-2.84676939580033,2.71056319011889));
#25067=CARTESIAN_POINT('Ctrl Pts',(7.49690753622974,-2.44048233697729,3.13622821610778));
#25068=CARTESIAN_POINT('Ctrl Pts',(7.41922746407797,-1.13479508100687,4.01481158483798));
#25069=CARTESIAN_POINT('Ctrl Pts',(7.31179773227947,1.13479508100694,4.01481158483804));
#25070=CARTESIAN_POINT('Ctrl Pts',(7.23411766012771,2.44048233697723,3.13622821610782));
#25071=CARTESIAN_POINT('Ctrl Pts',(7.204368000481,2.84676939580028,2.71056319011894));
#25072=CARTESIAN_POINT('Ctrl Pts',(9.24218966408072,-2.84752785710028,1.50590509120692));
#25073=CARTESIAN_POINT('Ctrl Pts',(9.19424742502024,-2.48463347664367,2.19211709526318));
#25074=CARTESIAN_POINT('Ctrl Pts',(9.0983747734547,-1.24416448608072,3.28819633497963));
#25075=CARTESIAN_POINT('Ctrl Pts',(8.95455988282867,1.24416448608072,3.28819633497963));
#25076=CARTESIAN_POINT('Ctrl Pts',(8.85868723126313,2.48463347664367,2.19211709526318));
#25077=CARTESIAN_POINT('Ctrl Pts',(8.81074499220265,2.84752785710028,1.50590509120692));
#25078=CARTESIAN_POINT('Ctrl Pts',(9.10520475409306,-3.05726864820132,1.61682577082915));
#25079=CARTESIAN_POINT('Ctrl Pts',(9.05726251503258,-2.66764450134284,2.35358219650886));
#25080=CARTESIAN_POINT('Ctrl Pts',(8.96138986346704,-1.33580609826714,3.53039551096818));
#25081=CARTESIAN_POINT('Ctrl Pts',(8.81757497284102,1.33580609826713,3.53039551096818));
#25082=CARTESIAN_POINT('Ctrl Pts',(8.72170232127548,2.66764450134284,2.35358219650887));
#25083=CARTESIAN_POINT('Ctrl Pts',(8.673760082215,3.05726864820131,1.61682577082916));
#25084=CARTESIAN_POINT('Ctrl Pts',(8.96821984410541,-3.26700943930236,1.72774645045138));
#25085=CARTESIAN_POINT('Ctrl Pts',(8.92027760504493,-2.85065552604202,2.51504729775454));
#25086=CARTESIAN_POINT('Ctrl Pts',(8.82440495347938,-1.42744771045355,3.77259468695673));
#25087=CARTESIAN_POINT('Ctrl Pts',(8.68059006285337,1.42744771045353,3.77259468695675));
#25088=CARTESIAN_POINT('Ctrl Pts',(8.58471741128782,2.85065552604201,2.51504729775456));
#25089=CARTESIAN_POINT('Ctrl Pts',(8.53677517222734,3.26700943930235,1.7277464504514));
#25090=CARTESIAN_POINT('Ctrl Pts',(8.83123493411776,-3.47675023040339,1.83866713007362));
#25091=CARTESIAN_POINT('Ctrl Pts',(8.78329269505728,-3.03366655074119,2.67651239900022));
#25092=CARTESIAN_POINT('Ctrl Pts',(8.68742004349173,-1.51908932263997,4.01479386294529));
#25093=CARTESIAN_POINT('Ctrl Pts',(8.54360515286572,1.51908932263994,4.0147938629453));
#25094=CARTESIAN_POINT('Ctrl Pts',(8.44773250130017,3.03366655074117,2.67651239900024));
#25095=CARTESIAN_POINT('Ctrl Pts',(8.39979026223969,3.47675023040338,1.83866713007365));
#25096=CARTESIAN_POINT('Ctrl Pts',(8.77665719587644,-2.84676199909996,2.71056009076467));
#25097=CARTESIAN_POINT('Ctrl Pts',(8.74690753622973,-2.44046839360025,3.13622213137543));
#25098=CARTESIAN_POINT('Ctrl Pts',(8.66922746407795,-1.13475981380474,4.01479386294536));
#25099=CARTESIAN_POINT('Ctrl Pts',(8.56179773227949,1.13475981380472,4.01479386294528));
#25100=CARTESIAN_POINT('Ctrl Pts',(8.48411766012771,2.4404683936002,3.13622213137546));
#25101=CARTESIAN_POINT('Ctrl Pts',(8.454368000481,2.84676199909991,2.71056009076472));
#25102=CARTESIAN_POINT('Ctrl Pts',(10.4921924265357,-2.84752458944047,1.50590142692301));
#25103=CARTESIAN_POINT('Ctrl Pts',(10.4442501522391,-2.48463084769168,2.19211316147804));
#25104=CARTESIAN_POINT('Ctrl Pts',(10.3483774654373,-1.244128467887,3.28817779179805));
#25105=CARTESIAN_POINT('Ctrl Pts',(10.204562504339,1.244128467887,3.28817779179805));
#25106=CARTESIAN_POINT('Ctrl Pts',(10.1086898175372,2.48463084769167,2.19211316147804));
#25107=CARTESIAN_POINT('Ctrl Pts',(10.0607475432405,2.84752458944047,1.50590142692301));
#25108=CARTESIAN_POINT('Ctrl Pts',(10.355206630966,-3.05726679541399,1.61682271217994));
#25109=CARTESIAN_POINT('Ctrl Pts',(10.3072643566693,-2.66764312332127,2.35357924747321));
#25110=CARTESIAN_POINT('Ctrl Pts',(10.2113916698675,-1.33576815041574,3.5303775137047));
#25111=CARTESIAN_POINT('Ctrl Pts',(10.0675767087691,1.33576815041572,3.53037751370471));
#25112=CARTESIAN_POINT('Ctrl Pts',(9.97170402196739,2.66764312332126,2.35357924747323));
#25113=CARTESIAN_POINT('Ctrl Pts',(9.92376174767071,3.05726679541398,1.61682271217996));
#25114=CARTESIAN_POINT('Ctrl Pts',(10.2182208353961,-3.2670090013875,1.72774399743689));
#25115=CARTESIAN_POINT('Ctrl Pts',(10.1702785610995,-2.85065539895085,2.51504533346838));
#25116=CARTESIAN_POINT('Ctrl Pts',(10.0744058742978,-1.42740783294447,3.77257723561135));
#25117=CARTESIAN_POINT('Ctrl Pts',(9.93059091319932,1.42740783294444,3.77257723561136));
#25118=CARTESIAN_POINT('Ctrl Pts',(9.83471822639758,2.85065539895083,2.5150453334684));
#25119=CARTESIAN_POINT('Ctrl Pts',(9.78677595210091,3.26700900138749,1.72774399743691));
#25120=CARTESIAN_POINT('Ctrl Pts',(10.0812350398263,-3.47675120736102,1.83866528269383));
#25121=CARTESIAN_POINT('Ctrl Pts',(10.0332927655296,-3.03366767458044,2.67651141946355));
#25122=CARTESIAN_POINT('Ctrl Pts',(9.93742007872794,-1.5190475154732,4.014776957518));
#25123=CARTESIAN_POINT('Ctrl Pts',(9.79360511762951,1.51904751547316,4.01477695751801));
#25124=CARTESIAN_POINT('Ctrl Pts',(9.69773243082778,3.03366767458041,2.67651141946358));
#25125=CARTESIAN_POINT('Ctrl Pts',(9.6497901565311,3.476751207361,1.83866528269385));
#25126=CARTESIAN_POINT('Ctrl Pts',(10.0266571958764,-2.84675533252353,2.71055713420083));
#25127=CARTESIAN_POINT('Ctrl Pts',(9.99690753622973,-2.44045582656577,3.13621632697281));
#25128=CARTESIAN_POINT('Ctrl Pts',(9.91922746407798,-1.13472802780763,4.01477695751801));
#25129=CARTESIAN_POINT('Ctrl Pts',(9.81179773227947,1.13472802780759,4.01477695751801));
#25130=CARTESIAN_POINT('Ctrl Pts',(9.73411766012771,2.44045582656573,3.13621632697284));
#25131=CARTESIAN_POINT('Ctrl Pts',(9.704368000481,2.84675533252349,2.71055713420087));
#25132=CARTESIAN_POINT('Origin',(3.02384907614375,0.,0.));
#25133=CARTESIAN_POINT('Ctrl Pts',(3.02384907614375,-0.0276919032690645,
3.22173788916774));
#25134=CARTESIAN_POINT('Ctrl Pts',(3.02384907614375,0.0782496652778502,
3.23412501519642));
#25135=CARTESIAN_POINT('Ctrl Pts',(3.02384907614376,0.184548923165627,3.24130018160313));
#25136=CARTESIAN_POINT('Ctrl Pts',(3.02384907614376,0.29078337533849,3.24328412261045));
#25137=CARTESIAN_POINT('Ctrl Pts',(3.02384907614375,0.398194429544279,3.24529003680042));
#25138=CARTESIAN_POINT('Ctrl Pts',(3.02384907614375,0.505540080276519,3.24198944432028));
#25139=CARTESIAN_POINT('Ctrl Pts',(3.02384907614375,0.612409252876001,3.23335728668128));
#25140=CARTESIAN_POINT('Ctrl Pts',(3.02384907614375,0.693096022241249,3.226839963719));
#25141=CARTESIAN_POINT('Ctrl Pts',(3.02384907614375,0.773511806360213,3.21728254875187));
#25142=CARTESIAN_POINT('Ctrl Pts',(3.02384907614375,0.85348463331301,3.204655194923));
#25143=CARTESIAN_POINT('Ctrl Pts',(3.02384907614375,0.948602940134049,3.18963643715743));
#25144=CARTESIAN_POINT('Ctrl Pts',(3.02384907614375,1.04309503128853,3.17027579824669));
#25145=CARTESIAN_POINT('Ctrl Pts',(3.02384907614375,1.13674268826725,3.14672432130043));
#25146=CARTESIAN_POINT('Ctrl Pts',(3.02384907614375,1.15921157599613,3.14107361408119));
#25147=CARTESIAN_POINT('Ctrl Pts',(3.02384907614375,1.18163183734145,3.13518149603407));
#25148=CARTESIAN_POINT('Ctrl Pts',(3.02384907614375,1.20400041713338,3.12904975582881));
#25149=CARTESIAN_POINT('Ctrl Pts',(3.02384907614375,1.22668855383874,3.12283041775225));
#25150=CARTESIAN_POINT('Ctrl Pts',(3.02384907614375,1.2493272800887,3.11636326663925));
#25151=CARTESIAN_POINT('Ctrl Pts',(3.02384907614375,1.27187893963434,3.10966082396874));
#25152=CARTESIAN_POINT('Ctrl Pts',(3.02384907614375,1.37566821122701,3.07881424076025));
#25153=CARTESIAN_POINT('Ctrl Pts',(3.02384907614375,1.47776583675392,3.04294833556332));
#25154=CARTESIAN_POINT('Ctrl Pts',(3.02384907614375,1.57787399167337,3.00235617549659));
#25155=CARTESIAN_POINT('Ctrl Pts',(3.02384907614375,1.67945971186073,2.96116488775727));
#25156=CARTESIAN_POINT('Ctrl Pts',(3.02384907614375,1.7789975445046,2.91510663424764));
#25157=CARTESIAN_POINT('Ctrl Pts',(3.02384907614375,1.87617830805873,2.86443319661672));
#25158=CARTESIAN_POINT('Ctrl Pts',(3.02384907614376,1.97420990098541,2.81331610689286));
#25159=CARTESIAN_POINT('Ctrl Pts',(3.02384907614375,2.06984379102712,2.75750242565906));
#25160=CARTESIAN_POINT('Ctrl Pts',(3.02384907614375,2.16275277600094,2.69719875918404));
#25161=CARTESIAN_POINT('Ctrl Pts',(3.02384907614375,2.22372524842834,2.65762386077722));
#25162=CARTESIAN_POINT('Ctrl Pts',(3.02384907614376,2.2835239426704,2.6161141717626));
#25163=CARTESIAN_POINT('Ctrl Pts',(3.02384907614376,2.34205147232849,2.57271690759623));
#25164=CARTESIAN_POINT('Ctrl Pts',(3.02384907614376,2.36251670760645,2.55754225001588));
#25165=CARTESIAN_POINT('Ctrl Pts',(3.02384907614375,2.38282647584896,2.54213672662517));
#25166=CARTESIAN_POINT('Ctrl Pts',(3.02384907614375,2.40297645819471,2.52650211691943));
#25167=CARTESIAN_POINT('Ctrl Pts',(3.02384907614375,2.41529317891841,2.51694542758514));
#25168=CARTESIAN_POINT('Ctrl Pts',(3.02384907614376,2.42754254591775,2.50730907271123));
#25169=CARTESIAN_POINT('Ctrl Pts',(3.02384907614376,2.43972290434689,2.49759447327991));
#25170=CARTESIAN_POINT('Ctrl Pts',(3.02384907614376,2.52887669079367,2.42648873955667));
#25171=CARTESIAN_POINT('Ctrl Pts',(3.02384907614376,2.61435347499606,2.35118026513924));
#25172=CARTESIAN_POINT('Ctrl Pts',(3.02384907614375,2.69583042064229,2.2719376795413));
#25173=CARTESIAN_POINT('Ctrl Pts',(3.02384907614375,2.74846100361106,2.22075039652654));
#25174=CARTESIAN_POINT('Ctrl Pts',(3.02384907614375,2.79942249209335,2.16792047495247));
#25175=CARTESIAN_POINT('Ctrl Pts',(3.02384907614375,2.84862442584919,2.11350930842726));
#25176=CARTESIAN_POINT('Origin',(3.02384907614375,0.,0.));
#25177=CARTESIAN_POINT('Origin',(11.0238490761438,0.,0.));
#25178=CARTESIAN_POINT('Origin',(11.0238490761438,0.,0.));
#25179=CARTESIAN_POINT('',(11.0238490761438,-1.74837398213582,3.52379982655521));
#25180=CARTESIAN_POINT('Ctrl Pts',(10.7710409564111,2.84675014301221,2.71055471688623));
#25181=CARTESIAN_POINT('Ctrl Pts',(10.8007906160578,2.44044604391822,3.13621158123827));
#25182=CARTESIAN_POINT('Ctrl Pts',(10.8784706882095,1.13470328440395,4.01476313548051));
#25183=CARTESIAN_POINT('Ctrl Pts',(10.9627400614538,-0.645450738027376,
4.01476313548051));
#25184=CARTESIAN_POINT('Ctrl Pts',(11.0172597750513,-1.6320315860502,3.5819951336082));
#25185=CARTESIAN_POINT('Ctrl Pts',(11.0238490761438,-1.74837398213582,3.52379982655521));
#25186=CARTESIAN_POINT('Origin',(11.0238490761438,0.,0.));
#25187=CARTESIAN_POINT('Origin',(11.0238490761438,0.,0.));
#25188=CARTESIAN_POINT('Ctrl Pts',(3.27104142627809,2.84862444224244,2.71179420072006));
#25189=CARTESIAN_POINT('Ctrl Pts',(3.27715668774982,2.76525344421169,2.79937188736806));
#25190=CARTESIAN_POINT('Ctrl Pts',(3.28327194922155,2.67782612651348,2.88311705070648));
#25191=CARTESIAN_POINT('Ctrl Pts',(3.28938721069328,2.58672031412161,2.96266215024775));
#25192=CARTESIAN_POINT('Ctrl Pts',(3.2955017508867,2.49562524741036,3.04219786766276));
#25193=CARTESIAN_POINT('Ctrl Pts',(3.30161629108012,2.40085282539269,3.11753427018141));
#25194=CARTESIAN_POINT('Ctrl Pts',(3.30773083127354,2.30281533001728,3.18834291691427));
#25195=CARTESIAN_POINT('Ctrl Pts',(3.31384732070615,2.20474658151039,3.25917413656108));
#25196=CARTESIAN_POINT('Ctrl Pts',(3.31996381013877,2.10341097249983,3.32547449962782));
#25197=CARTESIAN_POINT('Ctrl Pts',(3.32608029957138,1.9992515439133,3.38695767085452));
#25198=CARTESIAN_POINT('Ctrl Pts',(3.33219730689569,1.89508329600264,3.44844604794711));
#25199=CARTESIAN_POINT('Ctrl Pts',(3.33831431421999,1.78809106810152,3.50511623957712));
#25200=CARTESIAN_POINT('Ctrl Pts',(3.3444313215443,1.67874377661223,3.55672719399249));
#25201=CARTESIAN_POINT('Ctrl Pts',(3.35055243180748,1.56932314121,3.60837276608605));
#25202=CARTESIAN_POINT('Ctrl Pts',(3.35667354207066,1.45754461577093,3.65495216542421));
#25203=CARTESIAN_POINT('Ctrl Pts',(3.36279465233384,1.3438989665517,3.6962717118336));
#25204=CARTESIAN_POINT('Ctrl Pts',(3.36866578384342,1.23489446845073,3.73590381784961));
#25205=CARTESIAN_POINT('Ctrl Pts',(3.37453691535301,1.12417263389366,3.77069712601642));
#25206=CARTESIAN_POINT('Ctrl Pts',(3.3804080468626,1.01218020680333,3.80052367825219));
#25207=CARTESIAN_POINT('Ctrl Pts',(3.38643801180143,0.897158015992873,3.8311571368852));
#25208=CARTESIAN_POINT('Ctrl Pts',(3.39246797674025,0.780671237445417,3.85658409951363));
#25209=CARTESIAN_POINT('Ctrl Pts',(3.39849794167908,0.663216026372143,3.87667815305361));
#25210=CARTESIAN_POINT('Ctrl Pts',(3.40452465430829,0.545824165702508,3.89676136870576));
#25211=CARTESIAN_POINT('Ctrl Pts',(3.4105513669375,0.427465289416703,3.9115173384845));
#25212=CARTESIAN_POINT('Ctrl Pts',(3.41657807956671,0.308646188344926,3.92087063423676));
#25213=CARTESIAN_POINT('Ctrl Pts',(3.42260266217985,0.189869081409907,3.93022062426143));
#25214=CARTESIAN_POINT('Ctrl Pts',(3.42862724479299,0.0706324551248737,
3.93417171365013));
#25215=CARTESIAN_POINT('Ctrl Pts',(3.43465182740613,-0.0485516510990651,
3.93270031113172));
#25216=CARTESIAN_POINT('Ctrl Pts',(3.44067540027944,-0.167715781675204,
3.93122915522521));
#25217=CARTESIAN_POINT('Ctrl Pts',(3.44669897315274,-0.286827026949468,
3.92433732371218));
#25218=CARTESIAN_POINT('Ctrl Pts',(3.45272254602604,-0.405373546364642,
3.91205333398048));
#25219=CARTESIAN_POINT('Ctrl Pts',(3.45874784422619,-0.523954020958503,
3.89976582575604));
#25220=CARTESIAN_POINT('Ctrl Pts',(3.46477314242635,-0.641969065040415,
3.88208311012611));
#25221=CARTESIAN_POINT('Ctrl Pts',(3.4707984406265,-0.758912075489745,3.85908557325124));
#25222=CARTESIAN_POINT('Ctrl Pts',(3.47682460754683,-0.875871946640201,
3.83608472061945));
#25223=CARTESIAN_POINT('Ctrl Pts',(3.48285077446715,-0.991759101557666,
3.80776760026451));
#25224=CARTESIAN_POINT('Ctrl Pts',(3.48887694138748,-1.10607806193011,3.77426553397041));
#25225=CARTESIAN_POINT('Ctrl Pts',(3.49490708634063,-1.22047248728432,3.74074135207261));
#25226=CARTESIAN_POINT('Ctrl Pts',(3.50093723129378,-1.33329628462377,3.70202550216554));
#25227=CARTESIAN_POINT('Ctrl Pts',(3.50696737624693,-1.44406988066063,3.6582989462001));
#25228=CARTESIAN_POINT('Ctrl Pts',(3.50935832703864,-1.48799158058714,3.64096137895805));
#25229=CARTESIAN_POINT('Ctrl Pts',(3.51174927783036,-1.5315911802373,3.62283660276241));
#25230=CARTESIAN_POINT('Ctrl Pts',(3.51414022862207,-1.57483971028089,3.60393796934997));
#25231=CARTESIAN_POINT('Ctrl Pts',(3.52037156636177,-1.68755478512931,3.55468402066156));
#25232=CARTESIAN_POINT('Ctrl Pts',(3.52660290410147,-1.79799449153025,3.500122072768));
#25233=CARTESIAN_POINT('Ctrl Pts',(3.53283424184117,-1.90566526104715,3.44048381958673));
#25234=CARTESIAN_POINT('Ctrl Pts',(3.53906170132088,-2.01326901843035,3.38088268406157));
#25235=CARTESIAN_POINT('Ctrl Pts',(3.54528916080058,-2.11810698215066,3.3162117102347));
#25236=CARTESIAN_POINT('Ctrl Pts',(3.55151662028029,-2.21970999651663,3.24674860920339));
#25237=CARTESIAN_POINT('Ctrl Pts',(3.55774120404693,-2.32126609269433,3.17731758480752));
#25238=CARTESIAN_POINT('Ctrl Pts',(3.56396578781357,-2.41958993974689,3.10309903624059));
#25239=CARTESIAN_POINT('Ctrl Pts',(3.57019037158021,-2.51424092827549,3.02441424983159));
#25240=CARTESIAN_POINT('Ctrl Pts',(3.57641202806786,-2.60884740461503,2.94576646707299));
#25241=CARTESIAN_POINT('Ctrl Pts',(3.58263368455552,-2.69978420852058,2.86265685207649));
#25242=CARTESIAN_POINT('Ctrl Pts',(3.58885534104317,-2.78664338671542,2.77544728562356));
#25243=CARTESIAN_POINT('Ctrl Pts',(3.59034694463095,-2.80746733642786,2.75453933249758));
#25244=CARTESIAN_POINT('Ctrl Pts',(3.59183854821873,-2.8280570709332,2.73339590333766));
#25245=CARTESIAN_POINT('Ctrl Pts',(3.59333015180651,-2.84840726832521,2.71202231439052));
#25246=CARTESIAN_POINT('Origin',(11.0238490761438,0.,0.));
#25247=CARTESIAN_POINT('Ctrl Pts',(3.89604095641107,-2.84679354424148,-2.71057216472783));
#25248=CARTESIAN_POINT('Ctrl Pts',(3.92579061605778,-2.44052785873738,-3.13624583529209));
#25249=CARTESIAN_POINT('Ctrl Pts',(4.00347068820956,-1.13491021990779,-4.01486290103005));
#25250=CARTESIAN_POINT('Ctrl Pts',(4.11090042000803,1.13491021990785,-4.01486290102993));
#25251=CARTESIAN_POINT('Ctrl Pts',(4.1885804921598,2.44052785873742,-3.13624583529207));
#25252=CARTESIAN_POINT('Ctrl Pts',(4.21833015180651,2.84679354424151,-2.71057216472779));
#25253=CARTESIAN_POINT('Origin',(11.0238490761438,0.,0.));
#25254=CARTESIAN_POINT('Ctrl Pts',(4.52104095641107,2.84678837447174,2.71057037657591));
#25255=CARTESIAN_POINT('Ctrl Pts',(4.55079061605777,2.44051811330425,3.13624232474605));
#25256=CARTESIAN_POINT('Ctrl Pts',(4.62847068820955,1.13488557063109,4.01485267650142));
#25257=CARTESIAN_POINT('Ctrl Pts',(4.73590042000803,-1.13488557063111,4.01485267650135));
#25258=CARTESIAN_POINT('Ctrl Pts',(4.8135804921598,-2.44051811330426,3.13624232474605));
#25259=CARTESIAN_POINT('Ctrl Pts',(4.84333015180651,-2.84678837447173,2.71057037657592));
#25260=CARTESIAN_POINT('Origin',(11.0238490761438,0.,0.));
#25261=CARTESIAN_POINT('Ctrl Pts',(5.14604095641107,-2.84678351585588,-2.71056863339249));
#25262=CARTESIAN_POINT('Ctrl Pts',(5.17579061605778,-2.44050895442134,-3.13623890248327));
#25263=CARTESIAN_POINT('Ctrl Pts',(5.25347068820956,-1.13486240492507,-4.01484270909931));
#25264=CARTESIAN_POINT('Ctrl Pts',(5.36090042000802,1.13486240492515,-4.01484270909921));
#25265=CARTESIAN_POINT('Ctrl Pts',(5.4385804921598,2.44050895442139,-3.13623890248322));
#25266=CARTESIAN_POINT('Ctrl Pts',(5.46833015180651,2.84678351585592,-2.71056863339245));
#25267=CARTESIAN_POINT('Origin',(11.0238490761438,0.,0.));
#25268=CARTESIAN_POINT('Ctrl Pts',(5.77104095641107,2.84677894112342,2.71056693350226));
#25269=CARTESIAN_POINT('Ctrl Pts',(5.80079061605777,2.44050033068152,3.13623556521482));
#25270=CARTESIAN_POINT('Ctrl Pts',(5.87847068820954,1.13484059276487,4.01483298924472));
#25271=CARTESIAN_POINT('Ctrl Pts',(5.98590042000804,-1.13484059276507,4.01483298924472));
#25272=CARTESIAN_POINT('Ctrl Pts',(6.0635804921598,-2.44050033068153,3.13623556521481));
#25273=CARTESIAN_POINT('Ctrl Pts',(6.0933301518065,-2.84677894112342,2.71056693350226));
#25274=CARTESIAN_POINT('Origin',(11.0238490761438,0.,0.));
#25275=CARTESIAN_POINT('Ctrl Pts',(6.39604095641106,-2.8467746261001,-2.7105652753122));
#25276=CARTESIAN_POINT('Ctrl Pts',(6.42579061605777,-2.44049219651438,-3.13623230981321));
#25277=CARTESIAN_POINT('Ctrl Pts',(6.50347068820954,-1.13482001888854,-4.01482350782885));
#25278=CARTESIAN_POINT('Ctrl Pts',(6.61090042000804,1.13482001888872,-4.01482350782888));
#25279=CARTESIAN_POINT('Ctrl Pts',(6.6885804921598,2.44049219651441,-3.13623230981319));
#25280=CARTESIAN_POINT('Ctrl Pts',(6.71833015180651,2.84677462610012,-2.71056527531218));
#25281=CARTESIAN_POINT('Origin',(11.0238490761438,0.,0.));
#25282=CARTESIAN_POINT('Ctrl Pts',(7.02104095641106,2.84677054928067,2.71056365730649));
#25283=CARTESIAN_POINT('Ctrl Pts',(7.05079061605777,2.4404845113808,3.13622913330255));
#25284=CARTESIAN_POINT('Ctrl Pts',(7.12847068820954,1.13480058075977,4.01481425618423));
#25285=CARTESIAN_POINT('Ctrl Pts',(7.23590042000803,-1.13480058075978,4.01481425618427));
#25286=CARTESIAN_POINT('Ctrl Pts',(7.3135804921598,-2.4404845113808,3.13622913330254));
#25287=CARTESIAN_POINT('Ctrl Pts',(7.34333015180651,-2.84677054928066,2.7105636573065));
#25288=CARTESIAN_POINT('Origin',(11.0238490761438,0.,0.));
#25289=CARTESIAN_POINT('Ctrl Pts',(7.64604095641107,-2.84676669147043,-2.71056207804189));
#25290=CARTESIAN_POINT('Ctrl Pts',(7.67579061605778,-2.44047723909725,-3.1362260328494));
#25291=CARTESIAN_POINT('Ctrl Pts',(7.75347068820955,-1.13478218685908,-4.01480522605852));
#25292=CARTESIAN_POINT('Ctrl Pts',(7.86090042000803,1.13478218685912,-4.01480522605852));
#25293=CARTESIAN_POINT('Ctrl Pts',(7.9385804921598,2.4404772390973,-3.13622603284936));
#25294=CARTESIAN_POINT('Ctrl Pts',(7.96833015180651,2.84676669147048,-2.71056207804184));
#25295=CARTESIAN_POINT('Origin',(11.0238490761438,0.,0.));
#25296=CARTESIAN_POINT('Ctrl Pts',(8.27104095641106,2.84676303548313,2.71056053614337));
#25297=CARTESIAN_POINT('Ctrl Pts',(8.30079061605777,2.44047034726616,3.1362230057544));
#25298=CARTESIAN_POINT('Ctrl Pts',(8.37847068820953,1.13476475524287,4.01479640958965));
#25299=CARTESIAN_POINT('Ctrl Pts',(8.48590042000803,-1.13476475524271,4.01479640958985));
#25300=CARTESIAN_POINT('Ctrl Pts',(8.56358049215979,-2.44047034726616,3.1362230057544));
#25301=CARTESIAN_POINT('Ctrl Pts',(8.59333015180651,-2.84676303548312,2.71056053614338));
#25302=CARTESIAN_POINT('Origin',(11.0238490761438,0.,0.));
#25303=CARTESIAN_POINT('Ctrl Pts',(8.89604095641106,-2.84675956588473,-2.71055903030038));
#25304=CARTESIAN_POINT('Ctrl Pts',(8.92579061605777,-2.44046380679322,-3.1362200494445));
#25305=CARTESIAN_POINT('Ctrl Pts',(9.00347068820953,-1.13474821232218,-4.01478779928378));
#25306=CARTESIAN_POINT('Ctrl Pts',(9.11090042000803,1.13474821232205,-4.01478779928393));
#25307=CARTESIAN_POINT('Ctrl Pts',(9.18858049215979,2.44046380679323,-3.1362200494445));
#25308=CARTESIAN_POINT('Ctrl Pts',(9.21833015180651,2.84675956588473,-2.71055903030039));
#25309=CARTESIAN_POINT('Origin',(11.0238490761438,0.,0.));
#25310=CARTESIAN_POINT('Ctrl Pts',(9.52104095641107,2.84675626877589,2.71055755926284));
#25311=CARTESIAN_POINT('Ctrl Pts',(9.55079061605777,2.44045759147703,3.13621716146554));
#25312=CARTESIAN_POINT('Ctrl Pts',(9.62847068820954,1.1347324918254,4.01477938799309));
#25313=CARTESIAN_POINT('Ctrl Pts',(9.73590042000802,-1.13473249182541,4.01477938799308));
#25314=CARTESIAN_POINT('Ctrl Pts',(9.81358049215979,-2.44045759147703,3.13621716146554));
#25315=CARTESIAN_POINT('Ctrl Pts',(9.84333015180651,-2.84675626877588,2.71055755926285));
#25316=CARTESIAN_POINT('Origin',(11.0238490761438,0.,0.));
#25317=CARTESIAN_POINT('Ctrl Pts',(10.1460409564111,-2.84675313160574,-2.7105561218378));
#25318=CARTESIAN_POINT('Ctrl Pts',(10.1757906160578,-2.44045167765816,-3.13621433947552));
#25319=CARTESIAN_POINT('Ctrl Pts',(10.2534706882095,-1.13471753391067,-4.01477116889627));
#25320=CARTESIAN_POINT('Ctrl Pts',(10.360900420008,1.13471753391068,-4.01477116889624));
#25321=CARTESIAN_POINT('Ctrl Pts',(10.4385804921598,2.44045167765817,-3.13621433947552));
#25322=CARTESIAN_POINT('Ctrl Pts',(10.4683301518065,2.84675313160573,-2.71055612183781));
#25323=CARTESIAN_POINT('Ctrl Pts',(4.27290740952806,3.47674578943201,-1.83867552770464));
#25324=CARTESIAN_POINT('Ctrl Pts',(4.22496533064083,3.03366144096162,-2.67651685389203));
#25325=CARTESIAN_POINT('Ctrl Pts',(4.12909283924855,1.51928728527458,-4.01486290102995));
#25326=CARTESIAN_POINT('Ctrl Pts',(3.98527826896903,-1.51928728527452,-4.01486290102998));
#25327=CARTESIAN_POINT('Ctrl Pts',(3.88940577757674,-3.03366144096159,-2.67651685389207));
#25328=CARTESIAN_POINT('Ctrl Pts',(3.84146369868952,-3.47674578943198,-1.8386755277047));
#25329=CARTESIAN_POINT('Ctrl Pts',(4.13592652513338,3.26701142991145,-1.72775760113624));
#25330=CARTESIAN_POINT('Ctrl Pts',(4.08798444624615,2.85065610267767,-2.51505622890088));
#25331=CARTESIAN_POINT('Ctrl Pts',(3.99211195485387,1.42763642409474,-3.77266667786349));
#25332=CARTESIAN_POINT('Ctrl Pts',(3.84829738457435,-1.4276364240947,-3.7726666778635));
#25333=CARTESIAN_POINT('Ctrl Pts',(3.75242489318206,-2.85065610267764,-2.51505622890092));
#25334=CARTESIAN_POINT('Ctrl Pts',(3.70448281429483,-3.26701142991143,-1.72775760113627));
#25335=CARTESIAN_POINT('Ctrl Pts',(3.99894564073869,3.05727707039089,-1.61683967456782));
#25336=CARTESIAN_POINT('Ctrl Pts',(3.95100356185146,2.66765076439372,-2.35359560390975));
#25337=CARTESIAN_POINT('Ctrl Pts',(3.85513107045918,1.33598556291491,-3.53047045469701));
#25338=CARTESIAN_POINT('Ctrl Pts',(3.71131650017966,-1.33598556291488,-3.53047045469702));
#25339=CARTESIAN_POINT('Ctrl Pts',(3.61544400878737,-2.6676507643937,-2.35359560390977));
#25340=CARTESIAN_POINT('Ctrl Pts',(3.56750192990014,-3.05727707039087,-1.61683967456785));
#25341=CARTESIAN_POINT('Ctrl Pts',(3.86196475634401,2.84754271087033,-1.50592174799941));
#25342=CARTESIAN_POINT('Ctrl Pts',(3.81402267745678,2.48464542610977,-2.19213497891861));
#25343=CARTESIAN_POINT('Ctrl Pts',(3.71815018606449,1.24433470173507,-3.28827423153054));
#25344=CARTESIAN_POINT('Ctrl Pts',(3.57433561578498,-1.24433470173505,-3.28827423153055));
#25345=CARTESIAN_POINT('Ctrl Pts',(3.47846312439269,-2.48464542610976,-2.19213497891862));
#25346=CARTESIAN_POINT('Ctrl Pts',(3.43052104550547,-2.84754271087032,-1.50592174799943));
#25347=CARTESIAN_POINT('Ctrl Pts',(5.52290755913492,3.47674717210332,-1.83867291315533));
#25348=CARTESIAN_POINT('Ctrl Pts',(5.47496543037874,3.03366303203899,-2.67651546652179));
#25349=CARTESIAN_POINT('Ctrl Pts',(5.3790928891175,1.51922432968233,-4.01484270909923));
#25350=CARTESIAN_POINT('Ctrl Pts',(5.23527821910008,-1.51922432968225,-4.01484270909927));
#25351=CARTESIAN_POINT('Ctrl Pts',(5.13940567783883,-3.03366303203894,-2.67651546652185));
#25352=CARTESIAN_POINT('Ctrl Pts',(5.09146354908265,-3.47674717210328,-1.83867291315541));
#25353=CARTESIAN_POINT('Ctrl Pts',(5.3859254213967,3.2670108101514,-1.72775412943732));
#25354=CARTESIAN_POINT('Ctrl Pts',(5.33798329264052,2.85065592331588,-2.51505344789686));
#25355=CARTESIAN_POINT('Ctrl Pts',(5.24211075137927,1.4275764277431,-3.77264548798055));
#25356=CARTESIAN_POINT('Ctrl Pts',(5.09829608136185,-1.42757642774303,-3.77264548798058));
#25357=CARTESIAN_POINT('Ctrl Pts',(5.00242354010061,-2.85065592331583,-2.51505344789692));
#25358=CARTESIAN_POINT('Ctrl Pts',(4.95448141134442,-3.26701081015137,-1.72775412943738));
#25359=CARTESIAN_POINT('Ctrl Pts',(5.24894328365846,3.05727444819947,-1.61683534571931));
#25360=CARTESIAN_POINT('Ctrl Pts',(5.20100115490228,2.66764881459276,-2.35359142927193));
#25361=CARTESIAN_POINT('Ctrl Pts',(5.10512861364104,1.33592852580386,-3.53044826686187));
#25362=CARTESIAN_POINT('Ctrl Pts',(4.96131394362362,-1.33592852580381,-3.53044826686189));
#25363=CARTESIAN_POINT('Ctrl Pts',(4.86544140236237,-2.66764881459272,-2.35359142927197));
#25364=CARTESIAN_POINT('Ctrl Pts',(4.81749927360619,-3.05727444819945,-1.61683534571936));
#25365=CARTESIAN_POINT('Ctrl Pts',(5.11196114592024,2.84753808624755,-1.5059165620013));
#25366=CARTESIAN_POINT('Ctrl Pts',(5.06401901716406,2.48464170586964,-2.192129410647));
#25367=CARTESIAN_POINT('Ctrl Pts',(4.96814647590282,1.24428062386463,-3.28825104574319));
#25368=CARTESIAN_POINT('Ctrl Pts',(4.82433180588539,-1.24428062386459,-3.2882510457432));
#25369=CARTESIAN_POINT('Ctrl Pts',(4.72845926462415,-2.48464170586961,-2.19212941064703));
#25370=CARTESIAN_POINT('Ctrl Pts',(4.68051713586797,-2.84753808624753,-1.50591656200134));
#25371=CARTESIAN_POINT('Ctrl Pts',(6.77290769409362,3.47674841939408,-1.83867055459827));
#25372=CARTESIAN_POINT('Ctrl Pts',(6.72496552035121,3.03366446720085,-2.67651421526794));
#25373=CARTESIAN_POINT('Ctrl Pts',(6.62909293410373,1.51916853850403,-4.01482350782886));
#25374=CARTESIAN_POINT('Ctrl Pts',(6.48527817411384,-1.51916853850395,-4.01482350782889));
#25375=CARTESIAN_POINT('Ctrl Pts',(6.38940558786636,-3.0336644672008,-2.676514215268));
#25376=CARTESIAN_POINT('Ctrl Pts',(6.34146341412395,-3.47674841939404,-1.83867055459834));
#25377=CARTESIAN_POINT('Ctrl Pts',(6.63592442572804,3.26701025106974,-1.72775099765761));
#25378=CARTESIAN_POINT('Ctrl Pts',(6.58798225198562,2.85065576139054,-2.51505093944593));
#25379=CARTESIAN_POINT('Ctrl Pts',(6.49210966573815,1.42752324577464,-3.7726254459903));
#25380=CARTESIAN_POINT('Ctrl Pts',(6.34829490574825,-1.42752324577457,-3.77262544599032));
#25381=CARTESIAN_POINT('Ctrl Pts',(6.25242231950077,-2.85065576139049,-2.51505093944599));
#25382=CARTESIAN_POINT('Ctrl Pts',(6.20448014575836,-3.26701025106971,-1.72775099765767));
#25383=CARTESIAN_POINT('Ctrl Pts',(6.49894115736244,3.0572720827454,-1.61683144071695));
#25384=CARTESIAN_POINT('Ctrl Pts',(6.45099898362002,2.66764705558023,-2.35358766362393));
#25385=CARTESIAN_POINT('Ctrl Pts',(6.35512639737254,1.33587795304525,-3.53042738415174));
#25386=CARTESIAN_POINT('Ctrl Pts',(6.21131163738265,-1.3358779530452,-3.53042738415176));
#25387=CARTESIAN_POINT('Ctrl Pts',(6.11543905113517,-2.66764705558019,-2.35358766362397));
#25388=CARTESIAN_POINT('Ctrl Pts',(6.06749687739276,-3.05727208274538,-1.616831440717));
#25389=CARTESIAN_POINT('Ctrl Pts',(6.36195788899684,2.84753391442106,-1.5059118837763));
#25390=CARTESIAN_POINT('Ctrl Pts',(6.31401571525443,2.48463834976992,-2.19212438780192));
#25391=CARTESIAN_POINT('Ctrl Pts',(6.21814312900695,1.24423266031586,-3.28822932231318));
#25392=CARTESIAN_POINT('Ctrl Pts',(6.07432836901706,-1.24423266031582,-3.2882293223132));
#25393=CARTESIAN_POINT('Ctrl Pts',(5.97845578276958,-2.4846383497699,-2.19212438780196));
#25394=CARTESIAN_POINT('Ctrl Pts',(5.93051360902717,-2.84753391442104,-1.50591188377634));
#25395=CARTESIAN_POINT('Ctrl Pts',(8.02290781660591,3.47674955165342,-1.83866841355563));
#25396=CARTESIAN_POINT('Ctrl Pts',(7.97496560202607,3.03366576988594,-2.67651307964991));
#25397=CARTESIAN_POINT('Ctrl Pts',(7.87909297494116,1.51911875599997,-4.01480522605851));
#25398=CARTESIAN_POINT('Ctrl Pts',(7.73527813327642,-1.51911875599992,-4.01480522605853));
#25399=CARTESIAN_POINT('Ctrl Pts',(7.6394055061915,-3.03366576988591,-2.67651307964995));
#25400=CARTESIAN_POINT('Ctrl Pts',(7.59146329161166,-3.4767495516534,-1.83866841355567));
#25401=CARTESIAN_POINT('Ctrl Pts',(7.88592352188379,3.26700974354634,-1.727748154704));
#25402=CARTESIAN_POINT('Ctrl Pts',(7.83798130730395,2.85065561428405,-2.51504866256101));
#25403=CARTESIAN_POINT('Ctrl Pts',(7.74210868021904,1.42747577981153,-3.77260645240789));
#25404=CARTESIAN_POINT('Ctrl Pts',(7.59829383855429,-1.4274757798115,-3.77260645240791));
#25405=CARTESIAN_POINT('Ctrl Pts',(7.50242121146939,-2.85065561428403,-2.51504866256103));
#25406=CARTESIAN_POINT('Ctrl Pts',(7.45447899688955,-3.26700974354632,-1.72774815470403));
#25407=CARTESIAN_POINT('Ctrl Pts',(7.74893922716167,3.05726993543926,-1.61682789585237));
#25408=CARTESIAN_POINT('Ctrl Pts',(7.70099701258182,2.66764545868216,-2.35358424547209));
#25409=CARTESIAN_POINT('Ctrl Pts',(7.60512438549692,1.3358328036231,-3.53040767875727));
#25410=CARTESIAN_POINT('Ctrl Pts',(7.46130954383218,-1.33583280362307,-3.53040767875728));
#25411=CARTESIAN_POINT('Ctrl Pts',(7.36543691674726,-2.66764545868214,-2.35358424547211));
#25412=CARTESIAN_POINT('Ctrl Pts',(7.31749470216742,-3.05726993543925,-1.61682789585239));
#25413=CARTESIAN_POINT('Ctrl Pts',(7.61195493243955,2.84753012733218,-1.50590763700073));
#25414=CARTESIAN_POINT('Ctrl Pts',(7.56401271785971,2.48463530308027,-2.19211982838319));
#25415=CARTESIAN_POINT('Ctrl Pts',(7.46814009077479,1.24418982743467,-3.28820890510665));
#25416=CARTESIAN_POINT('Ctrl Pts',(7.32432524911005,-1.24418982743466,-3.28820890510666));
#25417=CARTESIAN_POINT('Ctrl Pts',(7.22845262202514,-2.48463530308026,-2.1921198283832));
#25418=CARTESIAN_POINT('Ctrl Pts',(7.1805104074453,-2.84753012733217,-1.50590763700075));
#25419=CARTESIAN_POINT('Ctrl Pts',(9.27290792843865,3.47675058521116,-1.83866645914951));
#25420=CARTESIAN_POINT('Ctrl Pts',(9.22496567658123,3.03366695890456,-2.67651204323431));
#25421=CARTESIAN_POINT('Ctrl Pts',(9.12909301221873,1.51907406221497,-4.01478779928389));
#25422=CARTESIAN_POINT('Ctrl Pts',(8.98527809599884,-1.51907406221493,-4.0147877992839));
#25423=CARTESIAN_POINT('Ctrl Pts',(8.88940543163634,-3.03366695890454,-2.67651204323434));
#25424=CARTESIAN_POINT('Ctrl Pts',(8.84146317977892,-3.47675058521115,-1.83866645914954));
#25425=CARTESIAN_POINT('Ctrl Pts',(9.13592269682874,3.26700928026235,-1.72774555957507));
#25426=CARTESIAN_POINT('Ctrl Pts',(9.08798044497131,2.85065547989676,-2.51504658435239));
#25427=CARTESIAN_POINT('Ctrl Pts',(8.99210778060883,1.42743315547921,-3.77258842044544));
#25428=CARTESIAN_POINT('Ctrl Pts',(8.84829286438891,-1.42743315547918,-3.77258842044545));
#25429=CARTESIAN_POINT('Ctrl Pts',(8.75242020002643,-2.85065547989675,-2.51504658435239));
#25430=CARTESIAN_POINT('Ctrl Pts',(8.70447794816901,-3.26700928026234,-1.72774555957508));
#25431=CARTESIAN_POINT('Ctrl Pts',(8.99893746521881,3.05726797531354,-1.61682466000062));
#25432=CARTESIAN_POINT('Ctrl Pts',(8.95099521336139,2.66764400088895,-2.35358112547045));
#25433=CARTESIAN_POINT('Ctrl Pts',(8.85512254899891,1.33579224874343,-3.530389041607));
#25434=CARTESIAN_POINT('Ctrl Pts',(8.71130763277899,-1.33579224874342,-3.530389041607));
#25435=CARTESIAN_POINT('Ctrl Pts',(8.61543496841651,-2.66764400088894,-2.35358112547046));
#25436=CARTESIAN_POINT('Ctrl Pts',(8.56749271655908,-3.05726797531354,-1.61682466000063));
#25437=CARTESIAN_POINT('Ctrl Pts',(8.8619522336089,2.84752667036473,-1.50590376042617));
#25438=CARTESIAN_POINT('Ctrl Pts',(8.81400998175148,2.48463252188115,-2.19211566658852));
#25439=CARTESIAN_POINT('Ctrl Pts',(8.718137317389,1.24415134200766,-3.28818966276855));
#25440=CARTESIAN_POINT('Ctrl Pts',(8.57432240116908,-1.24415134200766,-3.28818966276855));
#25441=CARTESIAN_POINT('Ctrl Pts',(8.47844973680659,-2.48463252188115,-2.19211566658852));
#25442=CARTESIAN_POINT('Ctrl Pts',(8.43050748494917,-2.84752667036473,-1.50590376042617));
#25443=CARTESIAN_POINT('Ctrl Pts',(10.5229080310278,3.47675153333854,-1.83866466628547));
#25444=CARTESIAN_POINT('Ctrl Pts',(10.474965744974,3.03366804954435,-2.67651109266735));
#25445=CARTESIAN_POINT('Ctrl Pts',(10.3790930464151,1.51903371577996,-4.01477116889625));
#25446=CARTESIAN_POINT('Ctrl Pts',(10.2352780618025,-1.51903371577993,-4.01477116889626));
#25447=CARTESIAN_POINT('Ctrl Pts',(10.1394053632436,-3.03366804954433,-2.67651109266738));
#25448=CARTESIAN_POINT('Ctrl Pts',(10.0914630771898,-3.47675153333853,-1.8386646662855));
#25449=CARTESIAN_POINT('Ctrl Pts',(10.3859219399691,3.26700885526974,-1.72774317894903));
#25450=CARTESIAN_POINT('Ctrl Pts',(10.3379796539154,2.85065535652278,-2.51504467809219));
#25451=CARTESIAN_POINT('Ctrl Pts',(10.2421069553564,1.42739466807426,-3.77257127375762));
#25452=CARTESIAN_POINT('Ctrl Pts',(10.0982919707438,-1.42739466807423,-3.77257127375763));
#25453=CARTESIAN_POINT('Ctrl Pts',(10.0024192721849,-2.85065535652277,-2.5150446780922));
#25454=CARTESIAN_POINT('Ctrl Pts',(9.95447698613115,-3.26700885526973,-1.72774317894905));
#25455=CARTESIAN_POINT('Ctrl Pts',(10.2489358489105,3.05726617720095,-1.61682169161259));
#25456=CARTESIAN_POINT('Ctrl Pts',(10.2009935628567,2.6676426635012,-2.35357826351702));
#25457=CARTESIAN_POINT('Ctrl Pts',(10.1051208642979,1.33575562036855,-3.53037137861899));
#25458=CARTESIAN_POINT('Ctrl Pts',(9.96130587968519,-1.33575562036854,-3.53037137861899));
#25459=CARTESIAN_POINT('Ctrl Pts',(9.86543318112631,-2.66764266350119,-2.35357826351704));
#25460=CARTESIAN_POINT('Ctrl Pts',(9.81749089507251,-3.05726617720095,-1.6168216916126));
#25461=CARTESIAN_POINT('Ctrl Pts',(10.1119497578518,2.84752349913215,-1.50590020427614));
#25462=CARTESIAN_POINT('Ctrl Pts',(10.0640074717981,2.48462997047963,-2.19211184894187));
#25463=CARTESIAN_POINT('Ctrl Pts',(9.96813477323921,1.24411657266284,-3.28817148348035));
#25464=CARTESIAN_POINT('Ctrl Pts',(9.82431978862655,-1.24411657266284,-3.28817148348035));
#25465=CARTESIAN_POINT('Ctrl Pts',(9.72844709006768,-2.48462997047963,-2.19211184894187));
#25466=CARTESIAN_POINT('Ctrl Pts',(9.68050480401388,-2.84752349913215,-1.50590020427614));
#25467=CARTESIAN_POINT('Ctrl Pts',(3.64838128925859,-3.47740286631016,1.83922164452567));
#25468=CARTESIAN_POINT('Ctrl Pts',(3.60379518879799,-3.06521053407891,2.61855938315106));
#25469=CARTESIAN_POINT('Ctrl Pts',(3.51463169441755,-1.69992623500153,3.88752819359771));
#25470=CARTESIAN_POINT('Ctrl Pts',(3.38089080611729,1.09279645395022,4.09974510230776));
#25471=CARTESIAN_POINT('Ctrl Pts',(3.29173601827763,2.63403351313429,3.0518682259016));
#25472=CARTESIAN_POINT('Ctrl Pts',(3.24715862435781,3.1592487603224,2.34397402547678));
#25473=CARTESIAN_POINT('Ctrl Pts',(3.51131387403993,-3.26754097150884,1.72822428410498));
#25474=CARTESIAN_POINT('Ctrl Pts',(3.46672777357933,-2.88022452142018,2.46052884860418));
#25475=CARTESIAN_POINT('Ctrl Pts',(3.37756427919888,-1.59733537785462,3.65291516077772));
#25476=CARTESIAN_POINT('Ctrl Pts',(3.24382339089863,1.02684598940094,3.85232474048881));
#25477=CARTESIAN_POINT('Ctrl Pts',(3.15466860305897,2.47506911203139,2.86768742396558));
#25478=CARTESIAN_POINT('Ctrl Pts',(3.11009120913914,2.9685875236238,2.20251476715576));
#25479=CARTESIAN_POINT('Ctrl Pts',(3.37424645882128,-3.05767907670752,1.61722692368431));
#25480=CARTESIAN_POINT('Ctrl Pts',(3.32966035836067,-2.69523850876146,2.30249831405731));
#25481=CARTESIAN_POINT('Ctrl Pts',(3.24049686398023,-1.4947445207077,3.41830212795774));
#25482=CARTESIAN_POINT('Ctrl Pts',(3.10675597567997,0.960895524851675,3.60490437866986));
#25483=CARTESIAN_POINT('Ctrl Pts',(3.01760118784032,2.31610471092849,2.68350662202955));
#25484=CARTESIAN_POINT('Ctrl Pts',(2.97302379392049,2.77792628692519,2.06105550883474));
#25485=CARTESIAN_POINT('Ctrl Pts',(3.23717904360261,-2.84781718190621,1.50622956326363));
#25486=CARTESIAN_POINT('Ctrl Pts',(3.192592943142,-2.51025249610272,2.14446777951043));
#25487=CARTESIAN_POINT('Ctrl Pts',(3.10342944876156,-1.39215366356079,3.18368909513775));
#25488=CARTESIAN_POINT('Ctrl Pts',(2.96968856046131,0.8949450603024,3.35748401685091));
#25489=CARTESIAN_POINT('Ctrl Pts',(2.88053377262165,2.15714030982559,2.49932582009352));
#25490=CARTESIAN_POINT('Ctrl Pts',(2.83595637870183,2.5872650502266,1.91959625051372));
#25491=CARTESIAN_POINT('Ctrl Pts',(4.89790748632074,-3.47674649915261,1.83867418566579));
#25492=CARTESIAN_POINT('Ctrl Pts',(4.84996538183595,-3.03366225767408,2.67651614172047));
#25493=CARTESIAN_POINT('Ctrl Pts',(4.7540928648461,-1.51925482848182,4.01485267650136));
#25494=CARTESIAN_POINT('Ctrl Pts',(4.61027824337146,1.51925482848179,4.01485267650137));
#25495=CARTESIAN_POINT('Ctrl Pts',(4.51440572638162,3.03366225767406,2.67651614172049));
#25496=CARTESIAN_POINT('Ctrl Pts',(4.46646362189683,3.47674649915259,1.83867418566581));
#25497=CARTESIAN_POINT('Ctrl Pts',(4.76092595858921,-3.26701111179121,1.72775581912512));
#25498=CARTESIAN_POINT('Ctrl Pts',(4.71298385410442,-2.85065601062904,2.51505480138416));
#25499=CARTESIAN_POINT('Ctrl Pts',(4.61711133711457,-1.42760549482174,3.77265593264611));
#25500=CARTESIAN_POINT('Ctrl Pts',(4.47329671563993,1.42760549482173,3.77265593264612));
#25501=CARTESIAN_POINT('Ctrl Pts',(4.37742419865009,2.85065601062903,2.51505480138416));
#25502=CARTESIAN_POINT('Ctrl Pts',(4.32948209416529,3.26701111179121,1.72775581912514));
#25503=CARTESIAN_POINT('Ctrl Pts',(4.62394443085768,-3.05727572442982,1.61683745258446));
#25504=CARTESIAN_POINT('Ctrl Pts',(4.57600232637288,-2.66764976358399,2.35359346104786));
#25505=CARTESIAN_POINT('Ctrl Pts',(4.48012980938304,-1.33595616116168,3.53045918879086));
#25506=CARTESIAN_POINT('Ctrl Pts',(4.33631518790839,1.33595616116167,3.53045918879086));
#25507=CARTESIAN_POINT('Ctrl Pts',(4.24044267091855,2.66764976358399,2.35359346104786));
#25508=CARTESIAN_POINT('Ctrl Pts',(4.19250056643376,3.05727572442982,1.61683745258447));
#25509=CARTESIAN_POINT('Ctrl Pts',(4.48696290312614,-2.84754033706844,1.50591908604379));
#25510=CARTESIAN_POINT('Ctrl Pts',(4.43902079864135,-2.48464351653895,2.19213212071155));
#25511=CARTESIAN_POINT('Ctrl Pts',(4.34314828165151,-1.24430682750162,3.28826244493561));
#25512=CARTESIAN_POINT('Ctrl Pts',(4.19933366017687,1.24430682750162,3.28826244493561));
#25513=CARTESIAN_POINT('Ctrl Pts',(4.10346114318702,2.48464351653896,2.19213212071155));
#25514=CARTESIAN_POINT('Ctrl Pts',(4.05551903870224,2.84754033706845,1.50591908604379));
#25515=CARTESIAN_POINT('Ctrl Pts',(6.14790762829603,-3.47674781129169,1.8386717044864));
#25516=CARTESIAN_POINT('Ctrl Pts',(6.09996547648614,-3.03366376752034,2.67651482526888));
#25517=CARTESIAN_POINT('Ctrl Pts',(6.0040929121712,-1.51919561710872,4.01483298924471));
#25518=CARTESIAN_POINT('Ctrl Pts',(5.86027819604637,1.51919561710867,4.01483298924473));
#25519=CARTESIAN_POINT('Ctrl Pts',(5.76440563173143,3.03366376752031,2.67651482526892));
#25520=CARTESIAN_POINT('Ctrl Pts',(5.71646347992155,3.47674781129167,1.83867170448645));
#25521=CARTESIAN_POINT('Ctrl Pts',(6.01092491115509,-3.26701052364405,1.72775252452145));
#25522=CARTESIAN_POINT('Ctrl Pts',(5.96298275934521,-2.85065584035111,2.51505216238105));
#25523=CARTESIAN_POINT('Ctrl Pts',(5.86711019503026,-1.42754905962654,3.77263533004504));
#25524=CARTESIAN_POINT('Ctrl Pts',(5.72329547890544,1.4275490596265,3.77263533004505));
#25525=CARTESIAN_POINT('Ctrl Pts',(5.62742291459049,2.85065584035108,2.51505216238109));
#25526=CARTESIAN_POINT('Ctrl Pts',(5.57948076278061,3.26701052364403,1.72775252452148));
#25527=CARTESIAN_POINT('Ctrl Pts',(5.87394219401415,-3.0572732359964,1.6168333445565));
#25528=CARTESIAN_POINT('Ctrl Pts',(5.82600004220427,-2.66764791318189,2.35358949949323));
#25529=CARTESIAN_POINT('Ctrl Pts',(5.73012747788933,-1.33590250214437,3.53043767084536));
#25530=CARTESIAN_POINT('Ctrl Pts',(5.58631276176449,1.33590250214434,3.53043767084537));
#25531=CARTESIAN_POINT('Ctrl Pts',(5.49044019744956,2.66764791318187,2.35358949949325));
#25532=CARTESIAN_POINT('Ctrl Pts',(5.44249804563967,3.05727323599639,1.61683334455652));
#25533=CARTESIAN_POINT('Ctrl Pts',(5.73695947687322,-2.84753594834877,1.50591416459154));
#25534=CARTESIAN_POINT('Ctrl Pts',(5.68901732506333,-2.48463998601266,2.19212683660541));
#25535=CARTESIAN_POINT('Ctrl Pts',(5.59314476074839,-1.24425594466219,3.28824001164569));
#25536=CARTESIAN_POINT('Ctrl Pts',(5.44933004462356,1.24425594466217,3.28824001164569));
#25537=CARTESIAN_POINT('Ctrl Pts',(5.35345748030862,2.48463998601265,2.19212683660542));
#25538=CARTESIAN_POINT('Ctrl Pts',(5.30551532849874,2.84753594834877,1.50591416459156));
#25539=CARTESIAN_POINT('Ctrl Pts',(7.39790775678633,-3.47674899880063,1.83866945897147));
#25540=CARTESIAN_POINT('Ctrl Pts',(7.34996556214635,-3.03366513383357,2.67651363411353));
#25541=CARTESIAN_POINT('Ctrl Pts',(7.2540929550013,-1.51914295842827,4.01481425618425));
#25542=CARTESIAN_POINT('Ctrl Pts',(7.11027815321627,1.51914295842826,4.01481425618426));
#25543=CARTESIAN_POINT('Ctrl Pts',(7.01440554607122,3.03366513383357,2.67651363411354));
#25544=CARTESIAN_POINT('Ctrl Pts',(6.96646335143124,3.47674899880063,1.83866945897148));
#25545=CARTESIAN_POINT('Ctrl Pts',(7.26092396320754,-3.26700999135715,1.72774954284456));
#25546=CARTESIAN_POINT('Ctrl Pts',(7.21298176856756,-2.85065568612663,2.51504977427734));
#25547=CARTESIAN_POINT('Ctrl Pts',(7.1171091614225,-1.4274988574663,3.77261582384055));
#25548=CARTESIAN_POINT('Ctrl Pts',(6.97329435963748,1.42749885746629,3.77261582384056));
#25549=CARTESIAN_POINT('Ctrl Pts',(6.87742175249243,2.85065568612662,2.51504977427735));
#25550=CARTESIAN_POINT('Ctrl Pts',(6.82947955785245,3.26700999135715,1.72774954284456));
#25551=CARTESIAN_POINT('Ctrl Pts',(7.12394016962874,-3.05727098391365,1.61682962671764));
#25552=CARTESIAN_POINT('Ctrl Pts',(7.07599797498876,-2.66764623841967,2.35358591444117));
#25553=CARTESIAN_POINT('Ctrl Pts',(6.98012536784371,-1.33585475650433,3.53041739149685));
#25554=CARTESIAN_POINT('Ctrl Pts',(6.83631056605869,1.33585475650433,3.53041739149685));
#25555=CARTESIAN_POINT('Ctrl Pts',(6.74043795891363,2.66764623841968,2.35358591444116));
#25556=CARTESIAN_POINT('Ctrl Pts',(6.69249576427365,3.05727098391365,1.61682962671763));
#25557=CARTESIAN_POINT('Ctrl Pts',(6.98695637604995,-2.84753197647016,1.50590971059071));
#25558=CARTESIAN_POINT('Ctrl Pts',(6.93901418140997,-2.48463679071273,2.19212205460498));
#25559=CARTESIAN_POINT('Ctrl Pts',(6.84314157426491,-1.24421065554235,3.28821895915314));
#25560=CARTESIAN_POINT('Ctrl Pts',(6.69932677247989,1.24421065554236,3.28821895915314));
#25561=CARTESIAN_POINT('Ctrl Pts',(6.60345416533484,2.48463679071275,2.19212205460497));
#25562=CARTESIAN_POINT('Ctrl Pts',(6.55551197069486,2.84753197647017,1.5059097105907));
#25563=CARTESIAN_POINT('Ctrl Pts',(8.64790787376072,-3.47675007987806,1.83866741470954));
#25564=CARTESIAN_POINT('Ctrl Pts',(8.59996564012927,-3.03366637757612,2.67651254993933));
#25565=CARTESIAN_POINT('Ctrl Pts',(8.50409299399277,-1.51909582299121,4.01479640958979));
#25566=CARTESIAN_POINT('Ctrl Pts',(8.3602781142248,1.51909582299119,4.0147964095898));
#25567=CARTESIAN_POINT('Ctrl Pts',(8.2644054680883,3.03366637757611,2.67651254993935));
#25568=CARTESIAN_POINT('Ctrl Pts',(8.21646323445685,3.47675007987805,1.83866741470956));
#25569=CARTESIAN_POINT('Ctrl Pts',(8.5109231002196,-3.26700950677417,1.72774682840093));
#25570=CARTESIAN_POINT('Ctrl Pts',(8.46298086658815,-2.85065554561516,2.51504760041851));
#25571=CARTESIAN_POINT('Ctrl Pts',(8.36710822045164,-1.42745390994202,3.77259732121807));
#25572=CARTESIAN_POINT('Ctrl Pts',(8.22329334068369,1.42745390994201,3.77259732121807));
#25573=CARTESIAN_POINT('Ctrl Pts',(8.12742069454718,2.85065554561515,2.51504760041852));
#25574=CARTESIAN_POINT('Ctrl Pts',(8.07947846091573,3.26700950677417,1.72774682840094));
#25575=CARTESIAN_POINT('Ctrl Pts',(8.37393832667846,-3.05726893367027,1.61682624209231));
#25576=CARTESIAN_POINT('Ctrl Pts',(8.32599609304702,-2.6676447136542,2.35358265089769));
#25577=CARTESIAN_POINT('Ctrl Pts',(8.2301234469105,-1.33581199689285,3.53039823284634));
#25578=CARTESIAN_POINT('Ctrl Pts',(8.08630856714256,1.33581199689285,3.53039823284634));
#25579=CARTESIAN_POINT('Ctrl Pts',(7.99043592100605,2.6676447136542,2.35358265089769));
#25580=CARTESIAN_POINT('Ctrl Pts',(7.9424936873746,3.05726893367027,1.61682624209231));
#25581=CARTESIAN_POINT('Ctrl Pts',(8.23695355313735,-2.84752836056638,1.50590565578368));
#25582=CARTESIAN_POINT('Ctrl Pts',(8.1890113195059,-2.48463388169324,2.19211770137688));
#25583=CARTESIAN_POINT('Ctrl Pts',(8.09313867336938,-1.24417008384366,3.28819914447461));
#25584=CARTESIAN_POINT('Ctrl Pts',(7.94932379360143,1.24417008384367,3.28819914447461));
#25585=CARTESIAN_POINT('Ctrl Pts',(7.85345114746493,2.48463388169325,2.19211770137687));
#25586=CARTESIAN_POINT('Ctrl Pts',(7.80550891383348,2.84752836056639,1.50590565578368));
#25587=CARTESIAN_POINT('Ctrl Pts',(9.89790798080964,-3.47675106922323,1.83866554390586));
#25588=CARTESIAN_POINT('Ctrl Pts',(9.84996571149522,-3.0336675156804,2.67651155795465));
#25589=CARTESIAN_POINT('Ctrl Pts',(9.75409302967573,-1.51905338615236,4.01477938799308));
#25590=CARTESIAN_POINT('Ctrl Pts',(9.61027807854184,1.51905338615236,4.01477938799308));
#25591=CARTESIAN_POINT('Ctrl Pts',(9.51440539672235,3.0336675156804,2.67651155795466));
#25592=CARTESIAN_POINT('Ctrl Pts',(9.46646312740793,3.47675106922323,1.83866554390586));
#25593=CARTESIAN_POINT('Ctrl Pts',(9.76092231045756,-3.26700906330698,1.72774434428311));
#25594=CARTESIAN_POINT('Ctrl Pts',(9.71298004114314,-2.85065541692697,2.5150456111997));
#25595=CARTESIAN_POINT('Ctrl Pts',(9.61710735932365,-1.42741343323025,3.77257974085613));
#25596=CARTESIAN_POINT('Ctrl Pts',(9.47329240818975,1.42741343323025,3.77257974085613));
#25597=CARTESIAN_POINT('Ctrl Pts',(9.37741972637027,2.85065541692698,2.51504561119969));
#25598=CARTESIAN_POINT('Ctrl Pts',(9.32947745705584,3.26700906330699,1.72774434428311));
#25599=CARTESIAN_POINT('Ctrl Pts',(9.62393664010546,-3.05726705739074,1.61682314466038));
#25600=CARTESIAN_POINT('Ctrl Pts',(9.57599437079105,-2.66764331817354,2.35357966444475));
#25601=CARTESIAN_POINT('Ctrl Pts',(9.48012168897155,-1.33577348030816,3.53038009371919));
#25602=CARTESIAN_POINT('Ctrl Pts',(9.33630673783765,1.33577348030817,3.53038009371917));
#25603=CARTESIAN_POINT('Ctrl Pts',(9.24043405601817,2.66764331817355,2.35357966444474));
#25604=CARTESIAN_POINT('Ctrl Pts',(9.19249178670375,3.05726705739074,1.61682314466037));
#25605=CARTESIAN_POINT('Ctrl Pts',(9.48695096975338,-2.84752505147449,1.50590194503763));
#25606=CARTESIAN_POINT('Ctrl Pts',(9.43900870043896,-2.48463121942011,2.1921137176898));
#25607=CARTESIAN_POINT('Ctrl Pts',(9.34313601861947,-1.24413352738605,3.28818044658224));
#25608=CARTESIAN_POINT('Ctrl Pts',(9.19932106748558,1.24413352738608,3.28818044658223));
#25609=CARTESIAN_POINT('Ctrl Pts',(9.10344838566609,2.48463121942012,2.19211371768978));
#25610=CARTESIAN_POINT('Ctrl Pts',(9.05550611635167,2.8475250514745,1.50590194503761));
#25611=CARTESIAN_POINT('Ctrl Pts',(11.1479080792332,-3.47675197885198,1.8386638238398));
#25612=CARTESIAN_POINT('Ctrl Pts',(11.0999657771109,-3.03366856198811,2.67651064606967));
#25613=CARTESIAN_POINT('Ctrl Pts',(11.0040930624836,-1.51901497956362,4.01476313548051));
#25614=CARTESIAN_POINT('Ctrl Pts',(10.860278045734,1.51901497956361,4.01476313548052));
#25615=CARTESIAN_POINT('Ctrl Pts',(10.7644053311067,3.0336685619881,2.67651064606967));
#25616=CARTESIAN_POINT('Ctrl Pts',(10.7164630289844,3.47675197885198,1.83866382383981));
#25617=CARTESIAN_POINT('Ctrl Pts',(11.0109215843298,-3.2670086555702,1.72774206032147));
#25618=CARTESIAN_POINT('Ctrl Pts',(10.9629792822076,-2.85065529851772,2.5150437824221));
#25619=CARTESIAN_POINT('Ctrl Pts',(10.8671065675802,-1.42737679200625,3.77256301095426));
#25620=CARTESIAN_POINT('Ctrl Pts',(10.7232915508306,1.42737679200625,3.77256301095426));
#25621=CARTESIAN_POINT('Ctrl Pts',(10.6274188362032,2.85065529851772,2.5150437824221));
#25622=CARTESIAN_POINT('Ctrl Pts',(10.579476534081,3.2670086555702,1.72774206032147));
#25623=CARTESIAN_POINT('Ctrl Pts',(10.8739350894265,-3.05726533228842,1.61682029680313));
#25624=CARTESIAN_POINT('Ctrl Pts',(10.8259927873042,-2.66764203504732,2.35357691877453));
#25625=CARTESIAN_POINT('Ctrl Pts',(10.7301200726769,-1.33573860444888,3.53036288642801));
#25626=CARTESIAN_POINT('Ctrl Pts',(10.5863050559272,1.33573860444889,3.53036288642801));
#25627=CARTESIAN_POINT('Ctrl Pts',(10.4904323412999,2.66764203504733,2.35357691877453));
#25628=CARTESIAN_POINT('Ctrl Pts',(10.4424900391776,3.05726533228843,1.61682029680313));
#25629=CARTESIAN_POINT('Ctrl Pts',(10.7369485945231,-2.84752200900663,1.5058985332848));
#25630=CARTESIAN_POINT('Ctrl Pts',(10.6890062924008,-2.48462877157693,2.19211005512697));
#25631=CARTESIAN_POINT('Ctrl Pts',(10.5931335777734,-1.24410041689152,3.28816276190175));
#25632=CARTESIAN_POINT('Ctrl Pts',(10.4493185610239,1.24410041689153,3.28816276190174));
#25633=CARTESIAN_POINT('Ctrl Pts',(10.3534458463965,2.48462877157694,2.19211005512695));
#25634=CARTESIAN_POINT('Ctrl Pts',(10.3055035442743,2.84752200900664,1.50589853328477));
#25635=CARTESIAN_POINT('Origin',(11.0238490761438,-0.429849779945933,0.997913274973232));
#25636=CARTESIAN_POINT('Ctrl Pts',(11.1020448718976,-1.95024171098983,-2.73386013557053));
#25637=CARTESIAN_POINT('Ctrl Pts',(11.0712404028977,-2.37355302340116,-2.43188441726037));
#25638=CARTESIAN_POINT('Ctrl Pts',(11.0404359338978,-2.72516811805232,-2.03009223981615));
#25639=CARTESIAN_POINT('Ctrl Pts',(11.0096314648979,-2.96834053891712,-1.57047394666944));
#25640=CARTESIAN_POINT('Ctrl Pts',(11.0759796066463,-1.92402331790621,-2.69710704016389));
#25641=CARTESIAN_POINT('Ctrl Pts',(11.0451751376464,-2.34164377552606,-2.3991909817614));
#25642=CARTESIAN_POINT('Ctrl Pts',(11.0143706686465,-2.68853187520334,-2.00280036310181));
#25643=CARTESIAN_POINT('Ctrl Pts',(10.9835661996466,-2.9284351678973,-1.54936102357415));
#25644=CARTESIAN_POINT('Ctrl Pts',(11.049914341395,-1.8978049248226,-2.66035394475725));
#25645=CARTESIAN_POINT('Ctrl Pts',(11.0191098723951,-2.30973452765096,-2.36649754626242));
#25646=CARTESIAN_POINT('Ctrl Pts',(10.9883054033952,-2.65189563235436,-1.97550848638747));
#25647=CARTESIAN_POINT('Ctrl Pts',(10.9575009343953,-2.88852979687749,-1.52824810047886));
#25648=CARTESIAN_POINT('Ctrl Pts',(11.0238490761438,-1.87158653173898,-2.62360084935061));
#25649=CARTESIAN_POINT('Ctrl Pts',(10.9930446071439,-2.27782527977586,-2.33380411076345));
#25650=CARTESIAN_POINT('Ctrl Pts',(10.962240138144,-2.61525938950538,-1.94821660967313));
#25651=CARTESIAN_POINT('Ctrl Pts',(10.9314356691441,-2.84862442585768,-1.50713517738357));
#25652=CARTESIAN_POINT('Origin',(11.0238490761448,-0.860372781371823,-0.291674745319531));
#25653=CARTESIAN_POINT('Origin',(11.0238490761438,0.,0.));
#25654=CARTESIAN_POINT('',(12.0768490761438,5.,-6.12323399573677E-16));
#25655=CARTESIAN_POINT('Origin',(12.0768490761438,0.,0.));
#25656=CARTESIAN_POINT('',(11.0238490761438,5.,-6.12323399573677E-16));
#25657=CARTESIAN_POINT('',(11.0238490761438,5.,6.12323399573677E-16));
#25658=CARTESIAN_POINT('Origin',(11.0238490761438,0.,0.));
#25659=CARTESIAN_POINT('Origin',(11.0238490761438,0.,0.));
#25660=CARTESIAN_POINT('Origin',(12.0768490761438,0.,0.));
#28039=UNCERTAINTY_MEASURE_WITH_UNIT(LENGTH_MEASURE(0.01),#28056,
'DISTANCE_ACCURACY_VALUE',
'Maximum model space distance between geometric entities at asserted c
onnectivities');
#28043=UNCERTAINTY_MEASURE_WITH_UNIT(LENGTH_MEASURE(0.01),#28056,
'DISTANCE_ACCURACY_VALUE',
'Maximum model space distance between geometric entities at asserted c
onnectivities');
#28051=(
GEOMETRIC_REPRESENTATION_CONTEXT(3)
GLOBAL_UNCERTAINTY_ASSIGNED_CONTEXT((#28039))
GLOBAL_UNIT_ASSIGNED_CONTEXT((#28056,#28058,#28059))
REPRESENTATION_CONTEXT('','3D')
);
#28055=(
GEOMETRIC_REPRESENTATION_CONTEXT(3)
GLOBAL_UNCERTAINTY_ASSIGNED_CONTEXT((#28043))
GLOBAL_UNIT_ASSIGNED_CONTEXT((#28056,#28058,#28059))
REPRESENTATION_CONTEXT('','3D')
);
#28056=(
LENGTH_UNIT()
NAMED_UNIT(*)
SI_UNIT(.MILLI.,.METRE.)
);
#28058=(
NAMED_UNIT(*)
PLANE_ANGLE_UNIT()
SI_UNIT($,.RADIAN.)
);
#28059=(
NAMED_UNIT(*)
SI_UNIT($,.STERADIAN.)
SOLID_ANGLE_UNIT()
);
#28067=SHAPE_DEFINITION_REPRESENTATION(#28078,#28099);
#28078=PRODUCT_DEFINITION_SHAPE('',$,#28111);
#28099=SHAPE_REPRESENTATION('',(#4014),#28051);
#28103=PRODUCT_DEFINITION_CONTEXT('part definition',#28138,'design');
#28111=PRODUCT_DEFINITION('Screw_02','Screw_02',#28122,#28103);
#28122=PRODUCT_DEFINITION_FORMATION('',$,#28147);
#28138=APPLICATION_CONTEXT(
'Core Data for Automotive Mechanical Design Process');
#28139=PRODUCT_CONTEXT('part definition',#28138,'mechanical');
#28147=PRODUCT('Screw_02','Screw_02',$,(#28139));
#28152=PRESENTATION_STYLE_ASSIGNMENT((#28155));
#28155=SURFACE_STYLE_USAGE(.BOTH.,#28158);
#28158=SURFACE_SIDE_STYLE('',(#28161));
#28161=SURFACE_STYLE_FILL_AREA(#28164);
#28164=FILL_AREA_STYLE('Opaque(160,160,160)',(#28167));
#28167=FILL_AREA_STYLE_COLOUR('Opaque(160,160,160)',#28170);
#28170=COLOUR_RGB('Opaque(160,160,160)', 0.66274510, 0.83137255, 0.94901961);
ENDSEC;
END-ISO-10303-21;
